ISO-10303-21;
HEADER;
/* Generated by software containing ST-Developer
 * from STEP Tools, Inc. (www.steptools.com) 
 */

FILE_DESCRIPTION(
/* description */ ('Independent four-jaw lathe chuck,200mm body,40mm bore,36\X2\2013\X0\7
6mm nominal opposed jaw opening. Four shared machined T-jaws and model
ed partial M12x1.75 feed screws, native independent screw/slider links
, removable bolted bronze-bearing cartridges, fully captured ring/wash
er/head thrust stacks and registered bolted backplate. Custom spindle 
interface; no compatibility, speed, grip force or safety rating assign
ed.'),
/* implementation_level */ '2;1');

FILE_NAME(
/* name */ 'Socket head cap screw M8x40.step',
/* time_stamp */ '2026-11-09T20:24:54-08:00',
/* author */ (''),
/* organization */ (''),
/* preprocessor_version */ 'ST-DEVELOPER v20.2',
/* originating_system */ 'Autodesk Translation Framework v15.17.0.0',
/* authorisation */ '');

FILE_SCHEMA (('AUTOMOTIVE_DESIGN { 1 0 10303 214 3 1 1 }'));
ENDSEC;

DATA;
#10=MECHANICAL_DESIGN_GEOMETRIC_PRESENTATION_REPRESENTATION('',(#246),#69491);
#212=CONICAL_SURFACE('',#15793,3.5,0.785398163397448);
#213=CONICAL_SURFACE('',#15796,3.5,0.785398163397448);
#224=SHAPE_REPRESENTATION_RELATIONSHIP('SRR','None',#69581,#235);
#235=ADVANCED_BREP_SHAPE_REPRESENTATION('',(#257),#69490);
#246=STYLED_ITEM('',(#69640),#257);
#257=MANIFOLD_SOLID_BREP('Body1',#14741);
#296=B_SPLINE_SURFACE_WITH_KNOTS('',3,3,((#67508,#67509,#67510,#67511,#67512,
#67513,#67514,#67515,#67516,#67517,#67518,#67519,#67520,#67521,#67522,#67523,
#67524,#67525,#67526,#67527,#67528,#67529,#67530,#67531,#67532,#67533,#67534,
#67535,#67536,#67537,#67538,#67539,#67540,#67541,#67542,#67543,#67544,#67545,
#67546,#67547,#67548,#67549,#67550,#67551,#67552,#67553,#67554,#67555,#67556,
#67557,#67558,#67559,#67560,#67561,#67562,#67563,#67564,#67565,#67566,#67567,
#67568,#67569,#67570,#67571,#67572,#67573,#67574,#67575,#67576,#67577,#67578,
#67579,#67580,#67581,#67582,#67583,#67584,#67585,#67586,#67587,#67588,#67589,
#67590,#67591,#67592,#67593,#67594,#67595,#67596,#67597,#67598,#67599,#67600,
#67601,#67602,#67603,#67604,#67605,#67606,#67607,#67608,#67609,#67610,#67611,
#67612,#67613,#67614,#67615,#67616,#67617,#67618,#67619,#67620,#67621,#67622,
#67623,#67624,#67625,#67626,#67627,#67628,#67629,#67630,#67631,#67632,#67633,
#67634,#67635,#67636,#67637,#67638,#67639,#67640,#67641,#67642,#67643,#67644,
#67645,#67646,#67647,#67648,#67649,#67650,#67651,#67652,#67653,#67654,#67655,
#67656,#67657,#67658,#67659,#67660,#67661,#67662,#67663,#67664,#67665,#67666,
#67667,#67668,#67669,#67670,#67671,#67672,#67673,#67674,#67675,#67676,#67677,
#67678,#67679,#67680,#67681,#67682,#67683,#67684,#67685,#67686,#67687,#67688,
#67689,#67690,#67691,#67692,#67693,#67694,#67695,#67696,#67697,#67698,#67699,
#67700,#67701,#67702,#67703,#67704,#67705,#67706,#67707,#67708,#67709,#67710),
(#67711,#67712,#67713,#67714,#67715,#67716,#67717,#67718,#67719,#67720,
#67721,#67722,#67723,#67724,#67725,#67726,#67727,#67728,#67729,#67730,#67731,
#67732,#67733,#67734,#67735,#67736,#67737,#67738,#67739,#67740,#67741,#67742,
#67743,#67744,#67745,#67746,#67747,#67748,#67749,#67750,#67751,#67752,#67753,
#67754,#67755,#67756,#67757,#67758,#67759,#67760,#67761,#67762,#67763,#67764,
#67765,#67766,#67767,#67768,#67769,#67770,#67771,#67772,#67773,#67774,#67775,
#67776,#67777,#67778,#67779,#67780,#67781,#67782,#67783,#67784,#67785,#67786,
#67787,#67788,#67789,#67790,#67791,#67792,#67793,#67794,#67795,#67796,#67797,
#67798,#67799,#67800,#67801,#67802,#67803,#67804,#67805,#67806,#67807,#67808,
#67809,#67810,#67811,#67812,#67813,#67814,#67815,#67816,#67817,#67818,#67819,
#67820,#67821,#67822,#67823,#67824,#67825,#67826,#67827,#67828,#67829,#67830,
#67831,#67832,#67833,#67834,#67835,#67836,#67837,#67838,#67839,#67840,#67841,
#67842,#67843,#67844,#67845,#67846,#67847,#67848,#67849,#67850,#67851,#67852,
#67853,#67854,#67855,#67856,#67857,#67858,#67859,#67860,#67861,#67862,#67863,
#67864,#67865,#67866,#67867,#67868,#67869,#67870,#67871,#67872,#67873,#67874,
#67875,#67876,#67877,#67878,#67879,#67880,#67881,#67882,#67883,#67884,#67885,
#67886,#67887,#67888,#67889,#67890,#67891,#67892,#67893,#67894,#67895,#67896,
#67897,#67898,#67899,#67900,#67901,#67902,#67903,#67904,#67905,#67906,#67907,
#67908,#67909,#67910,#67911,#67912,#67913),(#67914,#67915,#67916,#67917,
#67918,#67919,#67920,#67921,#67922,#67923,#67924,#67925,#67926,#67927,#67928,
#67929,#67930,#67931,#67932,#67933,#67934,#67935,#67936,#67937,#67938,#67939,
#67940,#67941,#67942,#67943,#67944,#67945,#67946,#67947,#67948,#67949,#67950,
#67951,#67952,#67953,#67954,#67955,#67956,#67957,#67958,#67959,#67960,#67961,
#67962,#67963,#67964,#67965,#67966,#67967,#67968,#67969,#67970,#67971,#67972,
#67973,#67974,#67975,#67976,#67977,#67978,#67979,#67980,#67981,#67982,#67983,
#67984,#67985,#67986,#67987,#67988,#67989,#67990,#67991,#67992,#67993,#67994,
#67995,#67996,#67997,#67998,#67999,#68000,#68001,#68002,#68003,#68004,#68005,
#68006,#68007,#68008,#68009,#68010,#68011,#68012,#68013,#68014,#68015,#68016,
#68017,#68018,#68019,#68020,#68021,#68022,#68023,#68024,#68025,#68026,#68027,
#68028,#68029,#68030,#68031,#68032,#68033,#68034,#68035,#68036,#68037,#68038,
#68039,#68040,#68041,#68042,#68043,#68044,#68045,#68046,#68047,#68048,#68049,
#68050,#68051,#68052,#68053,#68054,#68055,#68056,#68057,#68058,#68059,#68060,
#68061,#68062,#68063,#68064,#68065,#68066,#68067,#68068,#68069,#68070,#68071,
#68072,#68073,#68074,#68075,#68076,#68077,#68078,#68079,#68080,#68081,#68082,
#68083,#68084,#68085,#68086,#68087,#68088,#68089,#68090,#68091,#68092,#68093,
#68094,#68095,#68096,#68097,#68098,#68099,#68100,#68101,#68102,#68103,#68104,
#68105,#68106,#68107,#68108,#68109,#68110,#68111,#68112,#68113,#68114,#68115,
#68116),(#68117,#68118,#68119,#68120,#68121,#68122,#68123,#68124,#68125,
#68126,#68127,#68128,#68129,#68130,#68131,#68132,#68133,#68134,#68135,#68136,
#68137,#68138,#68139,#68140,#68141,#68142,#68143,#68144,#68145,#68146,#68147,
#68148,#68149,#68150,#68151,#68152,#68153,#68154,#68155,#68156,#68157,#68158,
#68159,#68160,#68161,#68162,#68163,#68164,#68165,#68166,#68167,#68168,#68169,
#68170,#68171,#68172,#68173,#68174,#68175,#68176,#68177,#68178,#68179,#68180,
#68181,#68182,#68183,#68184,#68185,#68186,#68187,#68188,#68189,#68190,#68191,
#68192,#68193,#68194,#68195,#68196,#68197,#68198,#68199,#68200,#68201,#68202,
#68203,#68204,#68205,#68206,#68207,#68208,#68209,#68210,#68211,#68212,#68213,
#68214,#68215,#68216,#68217,#68218,#68219,#68220,#68221,#68222,#68223,#68224,
#68225,#68226,#68227,#68228,#68229,#68230,#68231,#68232,#68233,#68234,#68235,
#68236,#68237,#68238,#68239,#68240,#68241,#68242,#68243,#68244,#68245,#68246,
#68247,#68248,#68249,#68250,#68251,#68252,#68253,#68254,#68255,#68256,#68257,
#68258,#68259,#68260,#68261,#68262,#68263,#68264,#68265,#68266,#68267,#68268,
#68269,#68270,#68271,#68272,#68273,#68274,#68275,#68276,#68277,#68278,#68279,
#68280,#68281,#68282,#68283,#68284,#68285,#68286,#68287,#68288,#68289,#68290,
#68291,#68292,#68293,#68294,#68295,#68296,#68297,#68298,#68299,#68300,#68301,
#68302,#68303,#68304,#68305,#68306,#68307,#68308,#68309,#68310,#68311,#68312,
#68313,#68314,#68315,#68316,#68317,#68318,#68319)),.UNSPECIFIED.,.F.,.F.,
 .F.,(4,4),(4,1,1,1,1,1,1,1,1,1,1,1,1,1,1,1,1,1,1,1,1,1,1,1,1,1,1,1,1,1,
1,1,1,1,1,1,1,1,1,1,1,1,1,1,1,1,1,1,1,1,1,1,1,1,1,1,1,1,1,1,1,1,1,1,1,1,
1,1,1,1,1,1,1,1,1,1,1,1,1,1,1,1,1,1,1,1,1,1,1,1,1,1,1,1,1,1,1,1,1,1,1,1,
1,1,1,1,1,1,1,1,1,1,1,1,1,1,1,1,1,1,1,1,1,1,1,1,1,1,1,1,1,1,1,1,1,1,1,1,
1,1,1,1,1,1,1,1,1,1,1,1,1,1,1,1,1,1,1,1,1,1,1,1,1,1,1,1,1,1,1,1,1,1,1,1,
1,1,1,1,1,1,1,1,1,1,1,1,1,1,1,1,1,1,1,1,1,1,1,1,1,1,4),(0.,0.0820126057383863),
(11.6152142277549,12.614925558795,13.614636889835,14.6143482208751,15.6140595519151,
16.6137708829551,17.6134822139952,18.6131935450352,19.6129048760753,20.6126162071153,
21.6123275381553,22.6120388691954,23.6117502002354,24.6114615312754,25.6111728623155,
26.6108841933555,27.6105955243956,28.6103068554356,29.6100181864756,30.6097295175157,
31.6094408485557,32.6091521795958,33.6088635106358,34.6085748416758,35.6082861727159,
36.6079975037559,37.6077088347959,38.607420165836,39.607131496876,40.6068428279161,
41.6065541589561,42.6062654899961,43.6059768210362,44.6056881520762,45.6053994831162,
46.6051108141563,47.6048221451963,48.6045334762364,49.6042448072764,50.6039561383164,
51.6036674693565,52.6033788003965,53.6030901314366,54.6028014624766,55.6025127935166,
56.6022241245567,57.6019354555967,58.6016467866367,59.6013581176768,60.6010694487168,
61.6007807797569,62.6004921107969,63.6002034418369,64.599914772877,65.599626103917,
66.5993374349571,67.5990487659971,68.5987600970371,69.5984714280772,70.5981827591172,
71.5978940901573,72.5976054211973,73.5973167522373,74.5970280832774,75.5967394143174,
76.5964507453574,77.5961620763975,78.5958734074375,79.5955847384776,80.5952960695176,
81.5950074005576,82.5947187315977,83.5944300626377,84.5941413936777,85.5938527247178,
86.5935640557578,87.5932753867979,88.5929867178379,89.5926980488779,90.592409379918,
91.592120710958,92.5918320419981,93.5915433730381,94.5912547040781,95.5909660351182,
96.5906773661582,97.5903886971983,98.5901000282383,99.5898113592783,100.589522690318,
101.589234021358,102.588945352398,103.588656683438,104.588368014479,105.588079345519,
106.587790676559,107.587502007599,108.587213338639,109.586924669679,110.586636000719,
111.586347331759,112.586058662799,113.585769993839,114.585481324879,115.585192655919,
116.584903986959,117.584615317999,118.584326649039,119.584037980079,120.583749311119,
121.583460642159,122.583171973199,123.582883304239,124.582594635279,125.582305966319,
126.582017297359,127.581728628399,128.581439959439,129.581151290479,130.58086262152,
131.58057395256,132.5802852836,133.57999661464,134.57970794568,135.57941927672,
136.57913060776,137.5788419388,138.57855326984,139.57826460088,140.57797593192,
141.57768726296,142.577398594,143.57710992504,144.57682125608,145.57653258712,
146.57624391816,147.5759552492,148.57566658024,149.57537791128,150.57508924232,
151.57480057336,152.5745119044,153.57422323544,154.57393456648,155.57364589752,
156.57335722856,157.573068559601,158.572779890641,159.572491221681,160.572202552721,
161.571913883761,162.571625214801,163.571336545841,164.571047876881,165.570759207921,
166.570470538961,167.570181870001,168.569893201041,169.569604532081,170.569315863121,
171.569027194161,172.568738525201,173.568449856241,174.568161187281,175.567872518321,
176.567583849361,177.567295180401,178.567006511441,179.566717842481,180.566429173521,
181.566140504561,182.565851835602,183.565563166642,184.565274497682,185.564985828722,
186.564697159762,187.564408490802,188.564119821842,189.563831152882,190.563542483922,
191.563253814962,192.562965146002,193.562676477042,194.562387808082,195.562099139122,
196.561810470162,197.561521801202,198.561233132242,199.560944463282,200.560655794322,
201.560367125362,202.560078456402,203.559789787442,204.559501118482,205.559212449522,
206.558923780562,207.558635111602,208.558346442642,209.558057773683,210.557769104723,
211.557480435763),.UNSPECIFIED.);
#297=B_SPLINE_SURFACE_WITH_KNOTS('',3,3,((#68438,#68439,#68440,#68441,#68442,
#68443,#68444,#68445,#68446,#68447,#68448,#68449,#68450,#68451,#68452,#68453,
#68454,#68455,#68456,#68457,#68458,#68459,#68460,#68461,#68462,#68463,#68464,
#68465,#68466,#68467,#68468,#68469,#68470,#68471,#68472,#68473,#68474,#68475,
#68476,#68477,#68478,#68479,#68480,#68481,#68482,#68483,#68484,#68485,#68486,
#68487,#68488,#68489,#68490,#68491,#68492,#68493,#68494,#68495,#68496,#68497,
#68498,#68499,#68500,#68501,#68502,#68503,#68504,#68505,#68506,#68507,#68508,
#68509,#68510,#68511,#68512,#68513,#68514,#68515,#68516,#68517,#68518,#68519,
#68520,#68521,#68522,#68523,#68524,#68525,#68526,#68527,#68528,#68529,#68530,
#68531,#68532,#68533,#68534,#68535,#68536,#68537,#68538,#68539,#68540,#68541,
#68542,#68543,#68544,#68545,#68546,#68547,#68548,#68549,#68550,#68551,#68552,
#68553,#68554,#68555,#68556,#68557,#68558,#68559,#68560,#68561,#68562,#68563,
#68564,#68565,#68566,#68567,#68568,#68569,#68570,#68571,#68572,#68573,#68574,
#68575,#68576,#68577,#68578,#68579,#68580,#68581,#68582,#68583,#68584,#68585,
#68586,#68587,#68588,#68589,#68590,#68591,#68592,#68593,#68594,#68595,#68596,
#68597,#68598,#68599,#68600,#68601,#68602,#68603,#68604,#68605,#68606,#68607,
#68608,#68609,#68610,#68611,#68612,#68613,#68614,#68615,#68616,#68617,#68618,
#68619,#68620,#68621,#68622,#68623,#68624,#68625,#68626,#68627,#68628,#68629,
#68630,#68631,#68632,#68633,#68634,#68635,#68636,#68637,#68638,#68639,#68640,
#68641,#68642,#68643),(#68644,#68645,#68646,#68647,#68648,#68649,#68650,
#68651,#68652,#68653,#68654,#68655,#68656,#68657,#68658,#68659,#68660,#68661,
#68662,#68663,#68664,#68665,#68666,#68667,#68668,#68669,#68670,#68671,#68672,
#68673,#68674,#68675,#68676,#68677,#68678,#68679,#68680,#68681,#68682,#68683,
#68684,#68685,#68686,#68687,#68688,#68689,#68690,#68691,#68692,#68693,#68694,
#68695,#68696,#68697,#68698,#68699,#68700,#68701,#68702,#68703,#68704,#68705,
#68706,#68707,#68708,#68709,#68710,#68711,#68712,#68713,#68714,#68715,#68716,
#68717,#68718,#68719,#68720,#68721,#68722,#68723,#68724,#68725,#68726,#68727,
#68728,#68729,#68730,#68731,#68732,#68733,#68734,#68735,#68736,#68737,#68738,
#68739,#68740,#68741,#68742,#68743,#68744,#68745,#68746,#68747,#68748,#68749,
#68750,#68751,#68752,#68753,#68754,#68755,#68756,#68757,#68758,#68759,#68760,
#68761,#68762,#68763,#68764,#68765,#68766,#68767,#68768,#68769,#68770,#68771,
#68772,#68773,#68774,#68775,#68776,#68777,#68778,#68779,#68780,#68781,#68782,
#68783,#68784,#68785,#68786,#68787,#68788,#68789,#68790,#68791,#68792,#68793,
#68794,#68795,#68796,#68797,#68798,#68799,#68800,#68801,#68802,#68803,#68804,
#68805,#68806,#68807,#68808,#68809,#68810,#68811,#68812,#68813,#68814,#68815,
#68816,#68817,#68818,#68819,#68820,#68821,#68822,#68823,#68824,#68825,#68826,
#68827,#68828,#68829,#68830,#68831,#68832,#68833,#68834,#68835,#68836,#68837,
#68838,#68839,#68840,#68841,#68842,#68843,#68844,#68845,#68846,#68847,#68848,
#68849),(#68850,#68851,#68852,#68853,#68854,#68855,#68856,#68857,#68858,
#68859,#68860,#68861,#68862,#68863,#68864,#68865,#68866,#68867,#68868,#68869,
#68870,#68871,#68872,#68873,#68874,#68875,#68876,#68877,#68878,#68879,#68880,
#68881,#68882,#68883,#68884,#68885,#68886,#68887,#68888,#68889,#68890,#68891,
#68892,#68893,#68894,#68895,#68896,#68897,#68898,#68899,#68900,#68901,#68902,
#68903,#68904,#68905,#68906,#68907,#68908,#68909,#68910,#68911,#68912,#68913,
#68914,#68915,#68916,#68917,#68918,#68919,#68920,#68921,#68922,#68923,#68924,
#68925,#68926,#68927,#68928,#68929,#68930,#68931,#68932,#68933,#68934,#68935,
#68936,#68937,#68938,#68939,#68940,#68941,#68942,#68943,#68944,#68945,#68946,
#68947,#68948,#68949,#68950,#68951,#68952,#68953,#68954,#68955,#68956,#68957,
#68958,#68959,#68960,#68961,#68962,#68963,#68964,#68965,#68966,#68967,#68968,
#68969,#68970,#68971,#68972,#68973,#68974,#68975,#68976,#68977,#68978,#68979,
#68980,#68981,#68982,#68983,#68984,#68985,#68986,#68987,#68988,#68989,#68990,
#68991,#68992,#68993,#68994,#68995,#68996,#68997,#68998,#68999,#69000,#69001,
#69002,#69003,#69004,#69005,#69006,#69007,#69008,#69009,#69010,#69011,#69012,
#69013,#69014,#69015,#69016,#69017,#69018,#69019,#69020,#69021,#69022,#69023,
#69024,#69025,#69026,#69027,#69028,#69029,#69030,#69031,#69032,#69033,#69034,
#69035,#69036,#69037,#69038,#69039,#69040,#69041,#69042,#69043,#69044,#69045,
#69046,#69047,#69048,#69049,#69050,#69051,#69052,#69053,#69054,#69055),
(#69056,#69057,#69058,#69059,#69060,#69061,#69062,#69063,#69064,#69065,
#69066,#69067,#69068,#69069,#69070,#69071,#69072,#69073,#69074,#69075,#69076,
#69077,#69078,#69079,#69080,#69081,#69082,#69083,#69084,#69085,#69086,#69087,
#69088,#69089,#69090,#69091,#69092,#69093,#69094,#69095,#69096,#69097,#69098,
#69099,#69100,#69101,#69102,#69103,#69104,#69105,#69106,#69107,#69108,#69109,
#69110,#69111,#69112,#69113,#69114,#69115,#69116,#69117,#69118,#69119,#69120,
#69121,#69122,#69123,#69124,#69125,#69126,#69127,#69128,#69129,#69130,#69131,
#69132,#69133,#69134,#69135,#69136,#69137,#69138,#69139,#69140,#69141,#69142,
#69143,#69144,#69145,#69146,#69147,#69148,#69149,#69150,#69151,#69152,#69153,
#69154,#69155,#69156,#69157,#69158,#69159,#69160,#69161,#69162,#69163,#69164,
#69165,#69166,#69167,#69168,#69169,#69170,#69171,#69172,#69173,#69174,#69175,
#69176,#69177,#69178,#69179,#69180,#69181,#69182,#69183,#69184,#69185,#69186,
#69187,#69188,#69189,#69190,#69191,#69192,#69193,#69194,#69195,#69196,#69197,
#69198,#69199,#69200,#69201,#69202,#69203,#69204,#69205,#69206,#69207,#69208,
#69209,#69210,#69211,#69212,#69213,#69214,#69215,#69216,#69217,#69218,#69219,
#69220,#69221,#69222,#69223,#69224,#69225,#69226,#69227,#69228,#69229,#69230,
#69231,#69232,#69233,#69234,#69235,#69236,#69237,#69238,#69239,#69240,#69241,
#69242,#69243,#69244,#69245,#69246,#69247,#69248,#69249,#69250,#69251,#69252,
#69253,#69254,#69255,#69256,#69257,#69258,#69259,#69260,#69261)),
 .UNSPECIFIED.,.F.,.F.,.F.,(4,4),(4,1,1,1,1,1,1,1,1,1,1,1,1,1,1,1,1,1,1,
1,1,1,1,1,1,1,1,1,1,1,1,1,1,1,1,1,1,1,1,1,1,1,1,1,1,1,1,1,1,1,1,1,1,1,1,
1,1,1,1,1,1,1,1,1,1,1,1,1,1,1,1,1,1,1,1,1,1,1,1,1,1,1,1,1,1,1,1,1,1,1,1,
1,1,1,1,1,1,1,1,1,1,1,1,1,1,1,1,1,1,1,1,1,1,1,1,1,1,1,1,1,1,1,1,1,1,1,1,
1,1,1,1,1,1,1,1,1,1,1,1,1,1,1,1,1,1,1,1,1,1,1,1,1,1,1,1,1,1,1,1,1,1,1,1,
1,1,1,1,1,1,1,1,1,1,1,1,1,1,1,1,1,1,1,1,1,1,1,1,1,1,1,1,1,1,1,1,1,1,1,1,
1,1,1,1,4),(0.,0.0820126057383863),(8.31473274985819,9.30982372426964,10.3049146986811,
11.3000056730925,12.295096647504,13.2901876219154,14.2852785963269,15.2803695707383,
16.2754605451498,17.2705515195612,18.2656424939726,19.2607334683841,20.2558244427955,
21.250915417207,22.2460063916184,23.2410973660299,24.2361883404413,25.2312793148528,
26.2263702892642,27.2214612636757,28.2165522380871,29.2116432124985,30.20673418691,
31.2018251613214,32.1969161357329,33.1920071101443,34.1870980845558,35.1821890589672,
36.1772800333787,37.1723710077901,38.1674619822016,39.162552956613,40.1576439310244,
41.1527349054359,42.1478258798473,43.1429168542588,44.1380078286702,45.1330988030817,
46.1281897774931,47.1232807519046,48.118371726316,49.1134627007275,50.1085536751389,
51.1036446495503,52.0987356239618,53.0938265983732,54.0889175727847,55.0840085471961,
56.0790995216076,57.074190496019,58.0692814704305,59.0643724448419,60.0594634192534,
61.0545543936648,62.0496453680762,63.0447363424877,64.0398273168991,65.0349182913106,
66.030009265722,67.0251002401335,68.0201912145449,69.0152821889564,70.0103731633678,
71.0054641377792,72.0005551121907,72.9956460866021,73.9907370610136,74.985828035425,
75.9809190098365,76.9760099842479,77.9711009586594,78.9661919330708,79.9612829074823,
80.9563738818937,81.9514648563052,82.9465558307166,83.941646805128,84.9367377795395,
85.9318287539509,86.9269197283624,87.9220107027738,88.9171016771853,89.9121926515967,
90.9072836260082,91.9023746004196,92.897465574831,93.8925565492425,94.8876475236539,
95.8827384980654,96.8778294724768,97.8729204468883,98.8680114212997,99.8631023957112,
100.858193370123,101.853284344534,102.848375318946,103.843466293357,104.838557267768,
105.83364824218,106.828739216591,107.823830191003,108.818921165414,109.814012139826,
110.809103114237,111.804194088649,112.79928506306,113.794376037471,114.789467011883,
115.784557986294,116.779648960706,117.774739935117,118.769830909529,119.76492188394,
120.760012858352,121.755103832763,122.750194807174,123.745285781586,124.740376755997,
125.735467730409,126.73055870482,127.725649679232,128.720740653643,129.715831628055,
130.710922602466,131.706013576877,132.701104551289,133.6961955257,134.691286500112,
135.686377474523,136.681468448935,137.676559423346,138.671650397758,139.666741372169,
140.66183234658,141.656923320992,142.652014295403,143.647105269815,144.642196244226,
145.637287218638,146.632378193049,147.627469167461,148.622560141872,149.617651116283,
150.612742090695,151.607833065106,152.602924039518,153.598015013929,154.593105988341,
155.588196962752,156.583287937164,157.578378911575,158.573469885986,159.568560860398,
160.563651834809,161.558742809221,162.553833783632,163.548924758044,164.544015732455,
165.539106706867,166.534197681278,167.529288655689,168.524379630101,169.519470604512,
170.514561578924,171.509652553335,172.504743527747,173.499834502158,174.49492547657,
175.490016450981,176.485107425392,177.480198399804,178.475289374215,179.470380348627,
180.465471323038,181.46056229745,182.455653271861,183.450744246273,184.445835220684,
185.440926195095,186.436017169507,187.431108143918,188.42619911833,189.421290092741,
190.416381067153,191.411472041564,192.406563015976,193.401653990387,194.396744964798,
195.39183593921,196.386926913621,197.382017888033,198.377108862444,199.372199836856,
200.367290811267,201.362381785679,202.35747276009,203.352563734501,204.347654708913,
205.342745683324,206.337836657736,207.332927632147,208.328018606559,209.32310958097,
210.318200555382),.UNSPECIFIED.);
#363=FACE_BOUND('',#2146,.T.);
#364=FACE_BOUND('',#2149,.T.);
#512=PLANE('',#15800);
#513=PLANE('',#15801);
#514=PLANE('',#15802);
#515=PLANE('',#15803);
#516=PLANE('',#15804);
#517=PLANE('',#15805);
#518=PLANE('',#15806);
#519=PLANE('',#15807);
#520=PLANE('',#15811);
#521=PLANE('',#15812);
#1222=FACE_OUTER_BOUND('',#2068,.T.);
#1223=FACE_OUTER_BOUND('',#2069,.T.);
#1224=FACE_OUTER_BOUND('',#2070,.T.);
#1225=FACE_OUTER_BOUND('',#2071,.T.);
#1226=FACE_OUTER_BOUND('',#2072,.T.);
#1227=FACE_OUTER_BOUND('',#2073,.T.);
#1228=FACE_OUTER_BOUND('',#2074,.T.);
#1229=FACE_OUTER_BOUND('',#2075,.T.);
#1230=FACE_OUTER_BOUND('',#2076,.T.);
#1231=FACE_OUTER_BOUND('',#2077,.T.);
#1232=FACE_OUTER_BOUND('',#2078,.T.);
#1233=FACE_OUTER_BOUND('',#2079,.T.);
#1234=FACE_OUTER_BOUND('',#2080,.T.);
#1235=FACE_OUTER_BOUND('',#2081,.T.);
#1236=FACE_OUTER_BOUND('',#2082,.T.);
#1237=FACE_OUTER_BOUND('',#2083,.T.);
#1238=FACE_OUTER_BOUND('',#2084,.T.);
#1239=FACE_OUTER_BOUND('',#2085,.T.);
#1240=FACE_OUTER_BOUND('',#2086,.T.);
#1241=FACE_OUTER_BOUND('',#2087,.T.);
#1242=FACE_OUTER_BOUND('',#2088,.T.);
#1243=FACE_OUTER_BOUND('',#2089,.T.);
#1244=FACE_OUTER_BOUND('',#2090,.T.);
#1245=FACE_OUTER_BOUND('',#2091,.T.);
#1246=FACE_OUTER_BOUND('',#2092,.T.);
#1247=FACE_OUTER_BOUND('',#2093,.T.);
#1248=FACE_OUTER_BOUND('',#2094,.T.);
#1249=FACE_OUTER_BOUND('',#2095,.T.);
#1250=FACE_OUTER_BOUND('',#2096,.T.);
#1251=FACE_OUTER_BOUND('',#2097,.T.);
#1252=FACE_OUTER_BOUND('',#2098,.T.);
#1253=FACE_OUTER_BOUND('',#2099,.T.);
#1254=FACE_OUTER_BOUND('',#2100,.T.);
#1255=FACE_OUTER_BOUND('',#2101,.T.);
#1256=FACE_OUTER_BOUND('',#2102,.T.);
#1257=FACE_OUTER_BOUND('',#2103,.T.);
#1258=FACE_OUTER_BOUND('',#2104,.T.);
#1259=FACE_OUTER_BOUND('',#2105,.T.);
#1260=FACE_OUTER_BOUND('',#2106,.T.);
#1261=FACE_OUTER_BOUND('',#2107,.T.);
#1262=FACE_OUTER_BOUND('',#2108,.T.);
#1263=FACE_OUTER_BOUND('',#2109,.T.);
#1264=FACE_OUTER_BOUND('',#2110,.T.);
#1265=FACE_OUTER_BOUND('',#2111,.T.);
#1266=FACE_OUTER_BOUND('',#2112,.T.);
#1267=FACE_OUTER_BOUND('',#2113,.T.);
#1268=FACE_OUTER_BOUND('',#2114,.T.);
#1269=FACE_OUTER_BOUND('',#2115,.T.);
#1270=FACE_OUTER_BOUND('',#2116,.T.);
#1271=FACE_OUTER_BOUND('',#2117,.T.);
#1272=FACE_OUTER_BOUND('',#2118,.T.);
#1273=FACE_OUTER_BOUND('',#2119,.T.);
#1274=FACE_OUTER_BOUND('',#2120,.T.);
#1275=FACE_OUTER_BOUND('',#2121,.T.);
#1276=FACE_OUTER_BOUND('',#2122,.T.);
#1277=FACE_OUTER_BOUND('',#2123,.T.);
#1278=FACE_OUTER_BOUND('',#2124,.T.);
#1279=FACE_OUTER_BOUND('',#2125,.T.);
#1280=FACE_OUTER_BOUND('',#2126,.T.);
#1281=FACE_OUTER_BOUND('',#2127,.T.);
#1282=FACE_OUTER_BOUND('',#2128,.T.);
#1283=FACE_OUTER_BOUND('',#2129,.T.);
#1284=FACE_OUTER_BOUND('',#2130,.T.);
#1285=FACE_OUTER_BOUND('',#2131,.T.);
#1286=FACE_OUTER_BOUND('',#2132,.T.);
#1287=FACE_OUTER_BOUND('',#2133,.T.);
#1288=FACE_OUTER_BOUND('',#2134,.T.);
#1289=FACE_OUTER_BOUND('',#2135,.T.);
#1290=FACE_OUTER_BOUND('',#2136,.T.);
#1291=FACE_OUTER_BOUND('',#2137,.T.);
#1292=FACE_OUTER_BOUND('',#2138,.T.);
#1293=FACE_OUTER_BOUND('',#2139,.T.);
#1294=FACE_OUTER_BOUND('',#2140,.T.);
#1295=FACE_OUTER_BOUND('',#2141,.T.);
#1296=FACE_OUTER_BOUND('',#2142,.T.);
#1297=FACE_OUTER_BOUND('',#2143,.T.);
#1298=FACE_OUTER_BOUND('',#2144,.T.);
#1299=FACE_OUTER_BOUND('',#2145,.T.);
#1300=FACE_OUTER_BOUND('',#2147,.T.);
#1301=FACE_OUTER_BOUND('',#2148,.T.);
#1302=FACE_OUTER_BOUND('',#2150,.T.);
#2068=EDGE_LOOP('',(#12911,#12912,#12913,#12914));
#2069=EDGE_LOOP('',(#12915,#12916,#12917,#12918));
#2070=EDGE_LOOP('',(#12919,#12920,#12921,#12922));
#2071=EDGE_LOOP('',(#12923,#12924,#12925,#12926));
#2072=EDGE_LOOP('',(#12927,#12928,#12929,#12930));
#2073=EDGE_LOOP('',(#12931,#12932,#12933,#12934));
#2074=EDGE_LOOP('',(#12935,#12936,#12937,#12938));
#2075=EDGE_LOOP('',(#12939,#12940,#12941,#12942));
#2076=EDGE_LOOP('',(#12943,#12944,#12945,#12946));
#2077=EDGE_LOOP('',(#12947,#12948,#12949,#12950));
#2078=EDGE_LOOP('',(#12951,#12952,#12953,#12954));
#2079=EDGE_LOOP('',(#12955,#12956,#12957,#12958));
#2080=EDGE_LOOP('',(#12959,#12960,#12961,#12962));
#2081=EDGE_LOOP('',(#12963,#12964,#12965,#12966));
#2082=EDGE_LOOP('',(#12967,#12968,#12969,#12970));
#2083=EDGE_LOOP('',(#12971,#12972,#12973,#12974));
#2084=EDGE_LOOP('',(#12975,#12976,#12977,#12978));
#2085=EDGE_LOOP('',(#12979,#12980,#12981,#12982));
#2086=EDGE_LOOP('',(#12983,#12984,#12985,#12986));
#2087=EDGE_LOOP('',(#12987,#12988,#12989,#12990));
#2088=EDGE_LOOP('',(#12991,#12992,#12993,#12994));
#2089=EDGE_LOOP('',(#12995,#12996,#12997,#12998));
#2090=EDGE_LOOP('',(#12999,#13000,#13001,#13002));
#2091=EDGE_LOOP('',(#13003,#13004,#13005,#13006));
#2092=EDGE_LOOP('',(#13007,#13008,#13009,#13010));
#2093=EDGE_LOOP('',(#13011,#13012,#13013,#13014));
#2094=EDGE_LOOP('',(#13015,#13016,#13017,#13018));
#2095=EDGE_LOOP('',(#13019,#13020,#13021,#13022));
#2096=EDGE_LOOP('',(#13023,#13024,#13025,#13026));
#2097=EDGE_LOOP('',(#13027,#13028,#13029,#13030));
#2098=EDGE_LOOP('',(#13031,#13032,#13033,#13034));
#2099=EDGE_LOOP('',(#13035,#13036,#13037,#13038,#13039));
#2100=EDGE_LOOP('',(#13040,#13041,#13042));
#2101=EDGE_LOOP('',(#13043,#13044,#13045,#13046,#13047));
#2102=EDGE_LOOP('',(#13048,#13049,#13050,#13051));
#2103=EDGE_LOOP('',(#13052,#13053,#13054,#13055));
#2104=EDGE_LOOP('',(#13056,#13057,#13058,#13059));
#2105=EDGE_LOOP('',(#13060,#13061,#13062,#13063));
#2106=EDGE_LOOP('',(#13064,#13065,#13066,#13067));
#2107=EDGE_LOOP('',(#13068,#13069,#13070,#13071));
#2108=EDGE_LOOP('',(#13072,#13073,#13074,#13075));
#2109=EDGE_LOOP('',(#13076,#13077,#13078,#13079));
#2110=EDGE_LOOP('',(#13080,#13081,#13082,#13083));
#2111=EDGE_LOOP('',(#13084,#13085,#13086,#13087));
#2112=EDGE_LOOP('',(#13088,#13089,#13090,#13091));
#2113=EDGE_LOOP('',(#13092,#13093,#13094,#13095));
#2114=EDGE_LOOP('',(#13096,#13097,#13098,#13099));
#2115=EDGE_LOOP('',(#13100,#13101,#13102,#13103));
#2116=EDGE_LOOP('',(#13104,#13105,#13106,#13107));
#2117=EDGE_LOOP('',(#13108,#13109,#13110,#13111));
#2118=EDGE_LOOP('',(#13112,#13113,#13114,#13115));
#2119=EDGE_LOOP('',(#13116,#13117,#13118,#13119));
#2120=EDGE_LOOP('',(#13120,#13121,#13122,#13123));
#2121=EDGE_LOOP('',(#13124,#13125,#13126,#13127));
#2122=EDGE_LOOP('',(#13128,#13129,#13130,#13131));
#2123=EDGE_LOOP('',(#13132,#13133,#13134,#13135));
#2124=EDGE_LOOP('',(#13136,#13137,#13138,#13139));
#2125=EDGE_LOOP('',(#13140,#13141,#13142,#13143));
#2126=EDGE_LOOP('',(#13144,#13145,#13146,#13147));
#2127=EDGE_LOOP('',(#13148,#13149,#13150,#13151));
#2128=EDGE_LOOP('',(#13152,#13153,#13154,#13155));
#2129=EDGE_LOOP('',(#13156,#13157,#13158,#13159));
#2130=EDGE_LOOP('',(#13160,#13161,#13162,#13163));
#2131=EDGE_LOOP('',(#13164,#13165,#13166,#13167));
#2132=EDGE_LOOP('',(#13168,#13169,#13170,#13171,#13172,#13173,#13174,#13175,
#13176));
#2133=EDGE_LOOP('',(#13177,#13178,#13179));
#2134=EDGE_LOOP('',(#13180,#13181,#13182,#13183,#13184,#13185,#13186,#13187,
#13188,#13189,#13190,#13191,#13192,#13193,#13194,#13195,#13196,#13197,#13198,
#13199,#13200,#13201,#13202,#13203,#13204,#13205,#13206,#13207,#13208,#13209,
#13210,#13211,#13212,#13213,#13214,#13215,#13216,#13217,#13218,#13219,#13220,
#13221,#13222,#13223,#13224,#13225,#13226,#13227,#13228,#13229,#13230,#13231,
#13232,#13233,#13234,#13235,#13236,#13237,#13238,#13239,#13240,#13241,#13242,
#13243,#13244,#13245,#13246,#13247));
#2135=EDGE_LOOP('',(#13248,#13249,#13250,#13251));
#2136=EDGE_LOOP('',(#13252,#13253,#13254,#13255,#13256,#13257,#13258,#13259,
#13260,#13261,#13262,#13263,#13264,#13265,#13266,#13267,#13268,#13269,#13270,
#13271,#13272,#13273,#13274,#13275,#13276,#13277,#13278,#13279,#13280,#13281,
#13282,#13283,#13284,#13285,#13286,#13287,#13288,#13289,#13290,#13291,#13292,
#13293,#13294,#13295,#13296,#13297,#13298,#13299,#13300,#13301,#13302,#13303,
#13304,#13305,#13306,#13307,#13308,#13309,#13310,#13311,#13312,#13313,#13314,
#13315,#13316,#13317,#13318));
#2137=EDGE_LOOP('',(#13319,#13320,#13321));
#2138=EDGE_LOOP('',(#13322,#13323,#13324,#13325));
#2139=EDGE_LOOP('',(#13326,#13327,#13328,#13329));
#2140=EDGE_LOOP('',(#13330,#13331,#13332,#13333));
#2141=EDGE_LOOP('',(#13334,#13335,#13336,#13337));
#2142=EDGE_LOOP('',(#13338,#13339,#13340,#13341));
#2143=EDGE_LOOP('',(#13342,#13343,#13344,#13345));
#2144=EDGE_LOOP('',(#13346,#13347,#13348,#13349,#13350,#13351));
#2145=EDGE_LOOP('',(#13352));
#2146=EDGE_LOOP('',(#13353,#13354,#13355,#13356));
#2147=EDGE_LOOP('',(#13357,#13358,#13359,#13360));
#2148=EDGE_LOOP('',(#13361));
#2149=EDGE_LOOP('',(#13362,#13363,#13364,#13365,#13366,#13367));
#2150=EDGE_LOOP('',(#13368));
#2338=CIRCLE('',#15726,3.933);
#2339=CIRCLE('',#15758,3.933);
#2340=CIRCLE('',#15760,3.22275);
#2341=CIRCLE('',#15762,3.22275);
#2342=CIRCLE('',#15794,3.933);
#2343=CIRCLE('',#15795,3.);
#2344=CIRCLE('',#15798,3.22275);
#2345=CIRCLE('',#15808,6.5);
#2346=CIRCLE('',#15810,6.5);
#3392=B_SPLINE_CURVE_WITH_KNOTS('',3,(#64835,#64836,#64837,#64838,#64839,
#64840,#64841,#64842,#64843,#64844),.UNSPECIFIED.,.F.,.F.,(4,3,3,4),(-4.09274904019422,
-3.99884532416016,-2.99913399312012,-2.06120159751576),.UNSPECIFIED.);
#3393=B_SPLINE_CURVE_WITH_KNOTS('',3,(#64847,#64848,#64849,#64850,#64851,
#64852,#64853),.UNSPECIFIED.,.F.,.F.,(4,3,4),(0.,0.995090974411437,1.11004521091154),
 .UNSPECIFIED.);
#3394=B_SPLINE_CURVE_WITH_KNOTS('',3,(#64858,#64859,#64860,#64861,#64862,
#64863,#64864,#64865,#64866,#64867,#64868,#64869,#64870,#64871,#64872,#64873,
#64874,#64875,#64876,#64877,#64878,#64879),.UNSPECIFIED.,.F.,.F.,(4,3,3,
3,3,3,3,4),(-10.3759343473738,-9.99711331040039,-8.99740197936035,-7.99769064832031,
-6.99797931728027,-5.99826798624023,-4.99855665520019,-4.09274904019422),
 .UNSPECIFIED.);
#3395=B_SPLINE_CURVE_WITH_KNOTS('',3,(#64880,#64881,#64882,#64883,#64884,
#64885,#64886,#64887,#64888,#64889,#64890,#64891,#64892,#64893,#64894,#64895,
#64896,#64897,#64898,#64899,#64900,#64901),.UNSPECIFIED.,.F.,.F.,(4,3,3,
3,3,3,3,4),(1.11004521091154,1.99018194882289,2.98527292323434,3.98036389764579,
4.97545487205724,5.97054584646869,6.96563682088014,7.39323051809113),
 .UNSPECIFIED.);
#3396=B_SPLINE_CURVE_WITH_KNOTS('',3,(#64906,#64907,#64908,#64909,#64910,
#64911,#64912,#64913,#64914,#64915,#64916,#64917,#64918,#64919,#64920,#64921,
#64922,#64923,#64924,#64925,#64926,#64927),.UNSPECIFIED.,.F.,.F.,(4,3,3,
3,3,3,3,4),(-16.6591196545534,-15.9953812966406,-14.9956699656006,-13.9959586345605,
-12.9962473035205,-11.9965359724805,-10.9968246414404,-10.3759343473738),
 .UNSPECIFIED.);
#3397=B_SPLINE_CURVE_WITH_KNOTS('',3,(#64928,#64929,#64930,#64931,#64932,
#64933,#64934,#64935,#64936,#64937,#64938,#64939,#64940,#64941,#64942,#64943,
#64944,#64945,#64946,#64947,#64948,#64949),.UNSPECIFIED.,.F.,.F.,(4,3,3,
3,3,3,3,4),(7.39323051809113,7.96072779529158,8.95581876970303,9.95090974411446,
10.9460007185259,11.9410916929373,12.9361826673488,13.6764158252707),
 .UNSPECIFIED.);
#3398=B_SPLINE_CURVE_WITH_KNOTS('',3,(#64954,#64955,#64956,#64957,#64958,
#64959,#64960,#64961,#64962,#64963,#64964,#64965,#64966,#64967,#64968,#64969,
#64970,#64971,#64972,#64973,#64974,#64975),.UNSPECIFIED.,.F.,.F.,(4,3,3,
3,3,3,3,4),(-22.942304961733,-21.9936492828808,-20.9939379518408,-19.9942266208008,
-18.9945152897607,-17.9948039587207,-16.9950926276807,-16.6591196545534),
 .UNSPECIFIED.);
#3399=B_SPLINE_CURVE_WITH_KNOTS('',3,(#64976,#64977,#64978,#64979,#64980,
#64981,#64982,#64983,#64984,#64985,#64986,#64987,#64988,#64989,#64990,#64991,
#64992,#64993,#64994,#64995,#64996,#64997,#64998,#64999,#65000),
 .UNSPECIFIED.,.F.,.F.,(4,3,3,3,3,3,3,3,4),(13.6764158252707,13.9312736417602,
14.9263646161717,15.9214555905831,16.9165465649946,17.911637539406,18.9067285138175,
19.9018194882289,19.9596011324503),.UNSPECIFIED.);
#3400=B_SPLINE_CURVE_WITH_KNOTS('',3,(#65005,#65006,#65007,#65008,#65009,
#65010,#65011,#65012,#65013,#65014,#65015,#65016,#65017,#65018,#65019,#65020,
#65021,#65022,#65023,#65024,#65025,#65026,#65027,#65028,#65029),
 .UNSPECIFIED.,.F.,.F.,(4,3,3,3,3,3,3,3,4),(-29.2254902689126,-28.9916286001611,
-27.9919172691211,-26.992205938081,-25.992494607041,-24.992783276001,-23.9930719449609,
-22.9933606139209,-22.942304961733),.UNSPECIFIED.);
#3401=B_SPLINE_CURVE_WITH_KNOTS('',3,(#65030,#65031,#65032,#65033,#65034,
#65035,#65036,#65037,#65038,#65039,#65040,#65041,#65042,#65043,#65044,#65045,
#65046,#65047,#65048,#65049,#65050,#65051),.UNSPECIFIED.,.F.,.F.,(4,3,3,
3,3,3,3,4),(19.9596011324503,20.8969104626403,21.8920014370518,22.8870924114632,
23.8821833858747,24.8772743602861,25.8723653346976,26.2427864396299),
 .UNSPECIFIED.);
#3402=B_SPLINE_CURVE_WITH_KNOTS('',3,(#65056,#65057,#65058,#65059,#65060,
#65061,#65062,#65063,#65064,#65065,#65066,#65067,#65068,#65069,#65070,#65071,
#65072,#65073,#65074,#65075,#65076,#65077),.UNSPECIFIED.,.F.,.F.,(4,3,3,
3,3,3,3,4),(-35.5086755760921,-34.9898965864014,-33.9901852553613,-32.9904739243213,
-31.9907625932812,-30.9910512622412,-29.9913399312012,-29.2254902689126),
 .UNSPECIFIED.);
#3403=B_SPLINE_CURVE_WITH_KNOTS('',3,(#65078,#65079,#65080,#65081,#65082,
#65083,#65084,#65085,#65086,#65087,#65088,#65089,#65090,#65091,#65092,#65093,
#65094,#65095,#65096,#65097,#65098,#65099),.UNSPECIFIED.,.F.,.F.,(4,3,3,
3,3,3,3,4),(26.2427864396299,26.867456309109,27.8625472835205,28.8576382579319,
29.8527292323434,30.8478202067548,31.8429111811663,32.5259717468095),
 .UNSPECIFIED.);
#3404=B_SPLINE_CURVE_WITH_KNOTS('',3,(#65104,#65105,#65106,#65107,#65108,
#65109,#65110,#65111,#65112,#65113,#65114,#65115,#65116,#65117,#65118,#65119,
#65120,#65121,#65122,#65123,#65124,#65125),.UNSPECIFIED.,.F.,.F.,(4,3,3,
3,3,3,3,4),(-41.7918608832717,-40.9881645726416,-39.9884532416015,-38.9887419105615,
-37.9890305795215,-36.9893192484814,-35.9896079174414,-35.5086755760921),
 .UNSPECIFIED.);
#3405=B_SPLINE_CURVE_WITH_KNOTS('',3,(#65126,#65127,#65128,#65129,#65130,
#65131,#65132,#65133,#65134,#65135,#65136,#65137,#65138,#65139,#65140,#65141,
#65142,#65143,#65144,#65145,#65146,#65147),.UNSPECIFIED.,.F.,.F.,(4,3,3,
3,3,3,3,4),(32.5259717468095,32.8380021555777,33.8330931299892,34.8281841044006,
35.823275078812,36.8183660532235,37.8134570276349,38.8091570539891),
 .UNSPECIFIED.);
#3406=B_SPLINE_CURVE_WITH_KNOTS('',3,(#65152,#65153,#65154,#65155,#65156,
#65157,#65158,#65159,#65160,#65161,#65162,#65163,#65164,#65165,#65166,#65167,
#65168,#65169,#65170,#65171,#65172,#65173,#65174,#65175,#65176),
 .UNSPECIFIED.,.F.,.F.,(4,3,3,3,3,3,3,3,4),(-48.0750461904513,-47.9861438899218,
-46.9864325588818,-45.9867212278418,-44.9870098968017,-43.9872985657617,
-42.9875872347217,-41.9878759036816,-41.7918608832717),.UNSPECIFIED.);
#3407=B_SPLINE_CURVE_WITH_KNOTS('',3,(#65177,#65178,#65179,#65180,#65181,
#65182,#65183,#65184,#65185,#65186,#65187,#65188,#65189,#65190,#65191,#65192,
#65193,#65194,#65195,#65196,#65197,#65198),.UNSPECIFIED.,.F.,.F.,(4,3,3,
3,3,3,3,4),(38.8091570539891,39.8036389764578,40.7987299508693,41.7938209252807,
42.7889118996922,43.7840028741036,44.7790938485151,45.0923423611687),
 .UNSPECIFIED.);
#3408=B_SPLINE_CURVE_WITH_KNOTS('',3,(#65203,#65204,#65205,#65206,#65207,
#65208,#65209,#65210,#65211,#65212,#65213,#65214,#65215,#65216,#65217,#65218,
#65219,#65220,#65221,#65222,#65223,#65224),.UNSPECIFIED.,.F.,.F.,(4,3,3,
3,3,3,3,4),(-54.3582314976309,-53.9844118761621,-52.9847005451221,-51.984989214082,
-50.985277883042,-49.9855665520019,-48.9858552209619,-48.0750461904513),
 .UNSPECIFIED.);
#3409=B_SPLINE_CURVE_WITH_KNOTS('',3,(#65225,#65226,#65227,#65228,#65229,
#65230,#65231,#65232,#65233,#65234,#65235,#65236,#65237,#65238,#65239,#65240,
#65241,#65242,#65243,#65244,#65245,#65246),.UNSPECIFIED.,.F.,.F.,(4,3,3,
3,3,3,3,4),(45.0923423611687,45.7741848229265,46.769275797338,47.7643667717494,
48.7594577461608,49.7545487205723,50.7496396949837,51.3755276683482),
 .UNSPECIFIED.);
#3410=B_SPLINE_CURVE_WITH_KNOTS('',3,(#65251,#65252,#65253,#65254,#65255,
#65256,#65257,#65258,#65259,#65260,#65261,#65262,#65263,#65264,#65265,#65266,
#65267,#65268,#65269,#65270,#65271,#65272),.UNSPECIFIED.,.F.,.F.,(4,3,3,
3,3,3,3,4),(-60.6414168048105,-59.9826798624023,-58.9829685313623,-57.9832572003222,
-56.9835458692822,-55.9838345382421,-54.9841232072021,-54.3582314976309),
 .UNSPECIFIED.);
#3411=B_SPLINE_CURVE_WITH_KNOTS('',3,(#65273,#65274,#65275,#65276,#65277,
#65278,#65279,#65280,#65281,#65282,#65283,#65284,#65285,#65286,#65287,#65288,
#65289,#65290,#65291,#65292,#65293,#65294),.UNSPECIFIED.,.F.,.F.,(4,3,3,
3,3,3,3,4),(51.3755276683482,51.7447306693952,52.7398216438066,53.7349126182181,
54.7300035926295,55.725094567041,56.7201855414524,57.6587129755278),
 .UNSPECIFIED.);
#3412=B_SPLINE_CURVE_WITH_KNOTS('',3,(#65299,#65300,#65301,#65302,#65303,
#65304,#65305,#65306,#65307,#65308,#65309,#65310,#65311,#65312,#65313,#65314,
#65315,#65316,#65317,#65318,#65319,#65320),.UNSPECIFIED.,.F.,.F.,(4,3,3,
3,3,3,3,4),(-66.9246021119901,-65.9809478486425,-64.9812365176025,-63.9815251865625,
-62.9818138555224,-61.9821025244824,-60.9823911934423,-60.6414168048105),
 .UNSPECIFIED.);
#3413=B_SPLINE_CURVE_WITH_KNOTS('',3,(#65321,#65322,#65323,#65324,#65325,
#65326,#65327,#65328,#65329,#65330,#65331,#65332,#65333,#65334,#65335,#65336,
#65337,#65338,#65339,#65340,#65341,#65342,#65343,#65344,#65345),
 .UNSPECIFIED.,.F.,.F.,(4,3,3,3,3,3,3,3,4),(57.6587129755278,57.7152765158638,
58.7103674902753,59.7054584646867,60.7005494390982,61.6956404135096,62.690731387921,
63.6858223623325,63.9418982827074),.UNSPECIFIED.);
#3414=B_SPLINE_CURVE_WITH_KNOTS('',3,(#65350,#65351,#65352,#65353,#65354,
#65355,#65356,#65357,#65358,#65359,#65360,#65361,#65362,#65363,#65364,#65365,
#65366,#65367,#65368,#65369,#65370,#65371,#65372,#65373,#65374),
 .UNSPECIFIED.,.F.,.F.,(4,3,3,3,3,3,3,3,4),(-73.2077874191697,-72.9789271659228,
-71.9792158348828,-70.9795045038427,-69.9797931728027,-68.9800818417627,
-67.9803705107226,-66.9806591796826,-66.9246021119901),.UNSPECIFIED.);
#3415=B_SPLINE_CURVE_WITH_KNOTS('',3,(#65375,#65376,#65377,#65378,#65379,
#65380,#65381,#65382,#65383,#65384,#65385,#65386,#65387,#65388,#65389,#65390,
#65391,#65392,#65393,#65394,#65395,#65396),.UNSPECIFIED.,.F.,.F.,(4,3,3,
3,3,3,3,4),(63.9418982827074,64.6809133367439,65.6760043111554,66.6710952855668,
67.6661862599783,68.6612772343897,69.6563682088012,70.225083589887),
 .UNSPECIFIED.);
#3416=B_SPLINE_CURVE_WITH_KNOTS('',3,(#65401,#65402,#65403,#65404,#65405,
#65406,#65407,#65408,#65409,#65410,#65411,#65412,#65413,#65414,#65415,#65416,
#65417,#65418,#65419,#65420,#65421,#65422),.UNSPECIFIED.,.F.,.F.,(4,3,3,
3,3,3,3,4),(-79.4909727263493,-78.977195152163,-77.977483821123,-76.977772490083,
-75.9780611590429,-74.9783498280029,-73.9786384969629,-73.2077874191697),
 .UNSPECIFIED.);
#3417=B_SPLINE_CURVE_WITH_KNOTS('',3,(#65423,#65424,#65425,#65426,#65427,
#65428,#65429,#65430,#65431,#65432,#65433,#65434,#65435,#65436,#65437,#65438,
#65439,#65440,#65441,#65442,#65443,#65444),.UNSPECIFIED.,.F.,.F.,(4,3,3,
3,3,3,3,4),(70.225083589887,70.6514591832126,71.646550157624,72.6416411320355,
73.6367321064469,74.6318230808584,75.6269140552698,76.5082688970666),
 .UNSPECIFIED.);
#3418=B_SPLINE_CURVE_WITH_KNOTS('',3,(#65449,#65450,#65451,#65452,#65453,
#65454,#65455,#65456,#65457,#65458,#65459,#65460,#65461,#65462,#65463,#65464,
#65465,#65466,#65467,#65468,#65469,#65470),.UNSPECIFIED.,.F.,.F.,(4,3,3,
3,3,3,3,4),(-85.7741580335289,-84.9754631384033,-83.9757518073632,-82.9760404763232,
-81.9763291452832,-80.9766178142431,-79.9769064832031,-79.4909727263493),
 .UNSPECIFIED.);
#3419=B_SPLINE_CURVE_WITH_KNOTS('',3,(#65471,#65472,#65473,#65474,#65475,
#65476,#65477,#65478,#65479,#65480,#65481,#65482,#65483,#65484,#65485,#65486,
#65487,#65488,#65489,#65490,#65491,#65492,#65493,#65494,#65495),
 .UNSPECIFIED.,.F.,.F.,(4,3,3,3,3,3,3,3,4),(76.5082688970666,76.6220050296813,
77.6170960040927,78.6121869785042,79.6072779529156,80.6023689273271,81.5974599017385,
82.59255087615,82.7914542042462),.UNSPECIFIED.);
#3420=B_SPLINE_CURVE_WITH_KNOTS('',3,(#65500,#65501,#65502,#65503,#65504,
#65505,#65506,#65507,#65508,#65509,#65510,#65511,#65512,#65513,#65514,#65515,
#65516,#65517,#65518,#65519,#65520,#65521,#65522,#65523,#65524),
 .UNSPECIFIED.,.F.,.F.,(4,3,3,3,3,3,3,3,4),(-92.0573433407085,-91.9734424556835,
-90.9737311246435,-89.9740197936035,-88.9743084625634,-87.9745971315234,
-86.9748858004833,-85.9751744694433,-85.7741580335289),.UNSPECIFIED.);
#3421=B_SPLINE_CURVE_WITH_KNOTS('',3,(#65525,#65526,#65527,#65528,#65529,
#65530,#65531,#65532,#65533,#65534,#65535,#65536,#65537,#65538,#65539,#65540,
#65541,#65542,#65543,#65544,#65545,#65546),.UNSPECIFIED.,.F.,.F.,(4,3,3,
3,3,3,3,4),(82.7914542042462,83.5876418505614,84.5827328249729,85.5778237993843,
86.5729147737958,87.5680057482072,88.5630967226186,89.0746395114258),
 .UNSPECIFIED.);
#3422=B_SPLINE_CURVE_WITH_KNOTS('',3,(#65551,#65552,#65553,#65554,#65555,
#65556,#65557,#65558,#65559,#65560,#65561,#65562,#65563,#65564,#65565,#65566,
#65567,#65568,#65569,#65570,#65571,#65572),.UNSPECIFIED.,.F.,.F.,(4,3,3,
3,3,3,3,4),(-98.3405286478881,-97.9717104419238,-96.9719991108837,-95.9722877798437,
-94.9725764488037,-93.9728651177636,-92.9731537867236,-92.0573433407085),
 .UNSPECIFIED.);
#3423=B_SPLINE_CURVE_WITH_KNOTS('',3,(#65573,#65574,#65575,#65576,#65577,
#65578,#65579,#65580,#65581,#65582,#65583,#65584,#65585,#65586,#65587,#65588,
#65589,#65590,#65591,#65592,#65593,#65594),.UNSPECIFIED.,.F.,.F.,(4,3,3,
3,3,3,3,4),(89.0746395114258,89.5581876970301,90.5532786714415,91.548369645853,
92.5434606202644,93.5385515946759,94.5336425690873,95.3578248186054),
 .UNSPECIFIED.);
#3424=B_SPLINE_CURVE_WITH_KNOTS('',3,(#65599,#65600,#65601,#65602,#65603,
#65604,#65605,#65606,#65607,#65608,#65609,#65610,#65611,#65612,#65613,#65614,
#65615,#65616,#65617,#65618,#65619,#65620),.UNSPECIFIED.,.F.,.F.,(4,3,3,
3,3,3,3,4),(-104.623713955068,-103.969978428164,-102.970267097124,-101.970555766084,
-100.970844435044,-99.9711331040039,-98.9714217729638,-98.3405286478881),
 .UNSPECIFIED.);
#3425=B_SPLINE_CURVE_WITH_KNOTS('',3,(#65621,#65622,#65623,#65624,#65625,
#65626,#65627,#65628,#65629,#65630,#65631,#65632,#65633,#65634,#65635,#65636,
#65637,#65638,#65639,#65640,#65641,#65642,#65643,#65644,#65645),
 .UNSPECIFIED.,.F.,.F.,(4,3,3,3,3,3,3,3,4),(95.3578248186054,95.5287335434987,
96.5238245179102,97.5189154923216,98.5140064667331,99.5090974411445,100.504188415556,
101.499279389967,101.641010125785),.UNSPECIFIED.);
#3426=B_SPLINE_CURVE_WITH_KNOTS('',3,(#65650,#65651,#65652,#65653,#65654,
#65655,#65656,#65657,#65658,#65659,#65660,#65661,#65662,#65663,#65664,#65665,
#65666,#65667,#65668,#65669,#65670,#65671),.UNSPECIFIED.,.F.,.F.,(4,3,3,
3,3,3,3,4),(-110.906899262247,-109.968246414404,-108.968535083364,-107.968823752324,
-106.969112421284,-105.969401090244,-104.969689759204,-104.623713955068),
 .UNSPECIFIED.);
#3427=B_SPLINE_CURVE_WITH_KNOTS('',3,(#65672,#65673,#65674,#65675,#65676,
#65677,#65678,#65679,#65680,#65681,#65682,#65683,#65684,#65685,#65686,#65687,
#65688,#65689,#65690,#65691,#65692,#65693),.UNSPECIFIED.,.F.,.F.,(4,3,3,
3,3,3,3,4),(101.641010125785,102.494370364379,103.48946133879,104.484552313202,
105.479643287613,106.474734262025,107.469825236436,107.924195432965),
 .UNSPECIFIED.);
#3428=B_SPLINE_CURVE_WITH_KNOTS('',3,(#65698,#65699,#65700,#65701,#65702,
#65703,#65704,#65705,#65706,#65707,#65708,#65709,#65710,#65711,#65712,#65713,
#65714,#65715,#65716,#65717,#65718,#65719,#65720,#65721,#65722),
 .UNSPECIFIED.,.F.,.F.,(4,3,3,3,3,3,3,3,4),(-117.190084569427,-116.966225731684,
-115.966514400644,-114.966803069604,-113.967091738564,-112.967380407524,
-111.967669076484,-110.967957745444,-110.906899262247),.UNSPECIFIED.);
#3429=B_SPLINE_CURVE_WITH_KNOTS('',3,(#65723,#65724,#65725,#65726,#65727,
#65728,#65729,#65730,#65731,#65732,#65733,#65734,#65735,#65736,#65737,#65738,
#65739,#65740,#65741,#65742,#65743,#65744),.UNSPECIFIED.,.F.,.F.,(4,3,3,
3,3,3,3,4),(107.924195432965,108.464916210848,109.460007185259,110.45509815967,
111.450189134082,112.445280108493,113.440371082905,114.207380740144),
 .UNSPECIFIED.);
#3430=B_SPLINE_CURVE_WITH_KNOTS('',3,(#65749,#65750,#65751,#65752,#65753,
#65754,#65755,#65756,#65757,#65758,#65759,#65760,#65761,#65762,#65763,#65764,
#65765,#65766,#65767,#65768,#65769,#65770),.UNSPECIFIED.,.F.,.F.,(4,3,3,
3,3,3,3,4),(-123.473269876606,-122.964493717925,-121.964782386885,-120.965071055845,
-119.965359724805,-118.965648393765,-117.965937062725,-117.190084569427),
 .UNSPECIFIED.);
#3431=B_SPLINE_CURVE_WITH_KNOTS('',3,(#65771,#65772,#65773,#65774,#65775,
#65776,#65777,#65778,#65779,#65780,#65781,#65782,#65783,#65784,#65785,#65786,
#65787,#65788,#65789,#65790,#65791,#65792,#65793,#65794,#65795),
 .UNSPECIFIED.,.F.,.F.,(4,3,3,3,3,3,3,3,4),(114.207380740144,114.435462057316,
115.430553031728,116.425644006139,117.420734980551,118.415825954962,119.410916929373,
120.406007903785,120.490566047324),.UNSPECIFIED.);
#3432=B_SPLINE_CURVE_WITH_KNOTS('',3,(#65800,#65801,#65802,#65803,#65804,
#65805,#65806,#65807,#65808,#65809,#65810,#65811,#65812,#65813,#65814,#65815,
#65816,#65817,#65818,#65819,#65820,#65821),.UNSPECIFIED.,.F.,.F.,(4,3,3,
3,3,3,3,4),(-129.756455183786,-128.962761704165,-127.963050373125,-126.963339042085,
-125.963627711045,-124.963916380005,-123.964205048965,-123.473269876606),
 .UNSPECIFIED.);
#3433=B_SPLINE_CURVE_WITH_KNOTS('',3,(#65822,#65823,#65824,#65825,#65826,
#65827,#65828,#65829,#65830,#65831,#65832,#65833,#65834,#65835,#65836,#65837,
#65838,#65839,#65840,#65841,#65842,#65843),.UNSPECIFIED.,.F.,.F.,(4,3,3,
3,3,3,3,4),(120.490566047324,121.401098878196,122.396189852608,123.391280827019,
124.386371801431,125.381462775842,126.376553750254,126.773751354503),
 .UNSPECIFIED.);
#3434=B_SPLINE_CURVE_WITH_KNOTS('',3,(#65848,#65849,#65850,#65851,#65852,
#65853,#65854,#65855,#65856,#65857,#65858,#65859,#65860,#65861,#65862,#65863,
#65864,#65865,#65866,#65867,#65868,#65869,#65870,#65871,#65872),
 .UNSPECIFIED.,.F.,.F.,(4,3,3,3,3,3,3,3,4),(-136.039640490966,-135.960741021445,
-134.961029690405,-133.961318359365,-132.961607028325,-131.961895697285,
-130.962184366245,-129.962473035205,-129.756455183786),.UNSPECIFIED.);
#3435=B_SPLINE_CURVE_WITH_KNOTS('',3,(#65873,#65874,#65875,#65876,#65877,
#65878,#65879,#65880,#65881,#65882,#65883,#65884,#65885,#65886,#65887,#65888,
#65889,#65890,#65891,#65892,#65893,#65894),.UNSPECIFIED.,.F.,.F.,(4,3,3,
3,3,3,3,4),(126.773751354503,127.371644724665,128.366735699076,129.361826673488,
130.356917647899,131.352008622311,132.347099596722,133.056936661683),
 .UNSPECIFIED.);
#3436=B_SPLINE_CURVE_WITH_KNOTS('',3,(#65899,#65900,#65901,#65902,#65903,
#65904,#65905,#65906,#65907,#65908,#65909,#65910,#65911,#65912,#65913,#65914,
#65915,#65916,#65917,#65918,#65919,#65920),.UNSPECIFIED.,.F.,.F.,(4,3,3,
3,3,3,3,4),(-142.322825798145,-141.959009007685,-140.959297676645,-139.959586345605,
-138.959875014565,-137.960163683525,-136.960452352485,-136.039640490966),
 .UNSPECIFIED.);
#3437=B_SPLINE_CURVE_WITH_KNOTS('',3,(#65921,#65922,#65923,#65924,#65925,
#65926,#65927,#65928,#65929,#65930,#65931,#65932,#65933,#65934,#65935,#65936,
#65937,#65938,#65939,#65940,#65941,#65942,#65943,#65944,#65945),
 .UNSPECIFIED.,.F.,.F.,(4,3,3,3,3,3,3,3,4),(133.056936661683,133.342190571134,
134.337281545545,135.332372519957,136.327463494368,137.322554468779,138.317645443191,
139.312736417602,139.340121968862),.UNSPECIFIED.);
#3438=B_SPLINE_CURVE_WITH_KNOTS('',3,(#65950,#65951,#65952,#65953,#65954,
#65955,#65956,#65957,#65958,#65959,#65960,#65961,#65962,#65963,#65964,#65965,
#65966,#65967,#65968,#65969,#65970,#65971),.UNSPECIFIED.,.F.,.F.,(4,3,3,
3,3,3,3,4),(-148.606011105325,-147.957276993926,-146.957565662886,-145.957854331846,
-144.958143000806,-143.958431669766,-142.958720338725,-142.322825798145),
 .UNSPECIFIED.);
#3439=B_SPLINE_CURVE_WITH_KNOTS('',3,(#65972,#65973,#65974,#65975,#65976,
#65977,#65978,#65979,#65980,#65981,#65982,#65983,#65984,#65985,#65986,#65987,
#65988,#65989,#65990,#65991,#65992,#65993),.UNSPECIFIED.,.F.,.F.,(4,3,3,
3,3,3,3,4),(139.340121968862,140.307827392014,141.302918366425,142.298009340837,
143.293100315248,144.28819128966,145.283282264071,145.623307276042),
 .UNSPECIFIED.);
#3440=B_SPLINE_CURVE_WITH_KNOTS('',3,(#65998,#65999,#66000,#66001,#66002,
#66003,#66004,#66005,#66006,#66007,#66008,#66009,#66010,#66011,#66012,#66013,
#66014,#66015,#66016,#66017,#66018,#66019),.UNSPECIFIED.,.F.,.F.,(4,3,3,
3,3,3,3,4),(-154.889196412504,-153.955544980166,-152.955833649126,-151.956122318086,
-150.956410987046,-149.956699656006,-148.956988324966,-148.606011105325),
 .UNSPECIFIED.);
#3441=B_SPLINE_CURVE_WITH_KNOTS('',3,(#66020,#66021,#66022,#66023,#66024,
#66025,#66026,#66027,#66028,#66029,#66030,#66031,#66032,#66033,#66034,#66035,
#66036,#66037,#66038,#66039,#66040,#66041),.UNSPECIFIED.,.F.,.F.,(4,3,3,
3,3,3,3,4),(145.623307276042,146.278373238482,147.273464212894,148.268555187305,
149.263646161717,150.258737136128,151.25382811054,151.906492583222),
 .UNSPECIFIED.);
#3442=B_SPLINE_CURVE_WITH_KNOTS('',3,(#66046,#66047,#66048,#66049,#66050,
#66051,#66052,#66053,#66054,#66055,#66056,#66057,#66058,#66059,#66060,#66061,
#66062,#66063,#66064,#66065,#66066,#66067,#66068,#66069,#66070),
 .UNSPECIFIED.,.F.,.F.,(4,3,3,3,3,3,3,3,4),(-161.172381719684,-160.953524297446,
-159.953812966406,-158.954101635366,-157.954390304326,-156.954678973286,
-155.954967642246,-154.955256311206,-154.889196412504),.UNSPECIFIED.);
#3443=B_SPLINE_CURVE_WITH_KNOTS('',3,(#66071,#66072,#66073,#66074,#66075,
#66076,#66077,#66078,#66079,#66080,#66081,#66082,#66083,#66084,#66085,#66086,
#66087,#66088,#66089,#66090,#66091,#66092),.UNSPECIFIED.,.F.,.F.,(4,3,3,
3,3,3,3,4),(151.906492583222,152.248919084951,153.244010059363,154.239101033774,
155.234192008185,156.229282982597,157.224373957008,158.189677890401),
 .UNSPECIFIED.);
#3444=B_SPLINE_CURVE_WITH_KNOTS('',3,(#66097,#66098,#66099,#66100,#66101,
#66102,#66103,#66104,#66105,#66106,#66107,#66108,#66109,#66110,#66111,#66112,
#66113,#66114,#66115,#66116,#66117,#66118),.UNSPECIFIED.,.F.,.F.,(4,3,3,
3,3,3,3,4),(-167.455567026863,-166.951792283686,-165.952080952646,-164.952369621606,
-163.952658290566,-162.952946959526,-161.953235628486,-161.172381719684),
 .UNSPECIFIED.);
#3445=B_SPLINE_CURVE_WITH_KNOTS('',3,(#66119,#66120,#66121,#66122,#66123,
#66124,#66125,#66126,#66127,#66128,#66129,#66130,#66131,#66132,#66133,#66134,
#66135,#66136,#66137,#66138,#66139,#66140,#66141,#66142,#66143),
 .UNSPECIFIED.,.F.,.F.,(4,3,3,3,3,3,3,3,4),(158.189677890401,158.21946493142,
159.214555905831,160.209646880243,161.204737854654,162.199828829066,163.194919803477,
164.190010777888,164.472863197581),.UNSPECIFIED.);
#3446=B_SPLINE_CURVE_WITH_KNOTS('',3,(#66148,#66149,#66150,#66151,#66152,
#66153,#66154,#66155,#66156,#66157,#66158,#66159,#66160,#66161,#66162,#66163,
#66164,#66165,#66166,#66167,#66168,#66169),.UNSPECIFIED.,.F.,.F.,(4,3,3,
3,3,3,3,4),(-173.738752334043,-172.950060269927,-171.950348938887,-170.950637607847,
-169.950926276807,-168.951214945766,-167.951503614726,-167.455567026863),
 .UNSPECIFIED.);
#3447=B_SPLINE_CURVE_WITH_KNOTS('',3,(#66170,#66171,#66172,#66173,#66174,
#66175,#66176,#66177,#66178,#66179,#66180,#66181,#66182,#66183,#66184,#66185,
#66186,#66187,#66188,#66189,#66190,#66191),.UNSPECIFIED.,.F.,.F.,(4,3,3,
3,3,3,3,4),(164.472863197581,165.1851017523,166.180192726711,167.175283701123,
168.170374675534,169.165465649946,170.160556624357,170.75604850476),
 .UNSPECIFIED.);
#3448=B_SPLINE_CURVE_WITH_KNOTS('',3,(#66196,#66197,#66198,#66199,#66200,
#66201,#66202,#66203,#66204,#66205,#66206,#66207,#66208,#66209,#66210,#66211,
#66212,#66213,#66214,#66215,#66216,#66217,#66218,#66219,#66220),
 .UNSPECIFIED.,.F.,.F.,(4,3,3,3,3,3,3,3,4),(-180.021937641223,-179.948039587207,
-178.948328256167,-177.948616925127,-176.948905594087,-175.949194263047,
-174.949482932007,-173.949771600967,-173.738752334043),.UNSPECIFIED.);
#3449=B_SPLINE_CURVE_WITH_KNOTS('',3,(#66221,#66222,#66223,#66224,#66225,
#66226,#66227,#66228,#66229,#66230,#66231,#66232,#66233,#66234,#66235,#66236,
#66237,#66238,#66239,#66240,#66241,#66242),.UNSPECIFIED.,.F.,.F.,(4,3,3,
3,3,3,3,4),(170.75604850476,171.155647598769,172.15073857318,173.145829547591,
174.140920522003,175.136011496414,176.131102470826,177.03923381194),
 .UNSPECIFIED.);
#3450=B_SPLINE_CURVE_WITH_KNOTS('',3,(#66247,#66248,#66249,#66250,#66251,
#66252,#66253,#66254,#66255,#66256,#66257,#66258,#66259,#66260,#66261,#66262,
#66263,#66264,#66265,#66266,#66267,#66268),.UNSPECIFIED.,.F.,.F.,(4,3,3,
3,3,3,3,4),(-186.305122948402,-185.946307573447,-184.946596242407,-183.946884911367,
-182.947173580327,-181.947462249287,-180.947750918247,-180.021937641223),
 .UNSPECIFIED.);
#3451=B_SPLINE_CURVE_WITH_KNOTS('',3,(#66269,#66270,#66271,#66272,#66273,
#66274,#66275,#66276,#66277,#66278,#66279,#66280,#66281,#66282,#66283,#66284,
#66285,#66286,#66287,#66288,#66289,#66290,#66291,#66292,#66293),
 .UNSPECIFIED.,.F.,.F.,(4,3,3,3,3,3,3,3,4),(177.03923381194,177.126193445237,
178.121284419649,179.11637539406,180.111466368472,181.106557342883,182.101648317294,
183.096739291706,183.322419119119),.UNSPECIFIED.);
#3452=B_SPLINE_CURVE_WITH_KNOTS('',3,(#66298,#66299,#66300,#66301,#66302,
#66303,#66304,#66305,#66306,#66307,#66308,#66309,#66310,#66311,#66312,#66313,
#66314,#66315,#66316,#66317,#66318,#66319),.UNSPECIFIED.,.F.,.F.,(4,3,3,
3,3,3,3,4),(-192.588308255582,-191.944575559687,-190.944864228647,-189.945152897607,
-188.945441566567,-187.945730235527,-186.946018904487,-186.305122948402),
 .UNSPECIFIED.);
#3453=B_SPLINE_CURVE_WITH_KNOTS('',3,(#66320,#66321,#66322,#66323,#66324,
#66325,#66326,#66327,#66328,#66329,#66330,#66331,#66332,#66333,#66334,#66335,
#66336,#66337,#66338,#66339,#66340,#66341),.UNSPECIFIED.,.F.,.F.,(4,3,3,
3,3,3,3,4),(183.322419119119,184.091830266117,185.086921240529,186.08201221494,
187.077103189352,188.072194163763,189.067285138175,189.605604426299),
 .UNSPECIFIED.);
#3454=B_SPLINE_CURVE_WITH_KNOTS('',3,(#66348,#66349,#66350,#66351,#66352,
#66353,#66354,#66355,#66356,#66357,#66358,#66359,#66360,#66361,#66362,#66363,
#66364,#66365,#66366,#66367,#66368,#66369),.UNSPECIFIED.,.F.,.F.,(4,3,3,
3,3,3,3,4),(-198.433361913984,-197.942843545928,-196.943132214888,-195.943420883848,
-194.943709552807,-193.943998221767,-192.944286890727,-192.588308255582),
 .UNSPECIFIED.);
#3455=B_SPLINE_CURVE_WITH_KNOTS('',3,(#66370,#66371,#66372,#66373,#66374,
#66375,#66376,#66377,#66378,#66379,#66380,#66381,#66382,#66383,#66384,#66385,
#66386,#66387,#66388,#66389,#66390,#66391),.UNSPECIFIED.,.F.,.F.,(4,3,3,
3,3,3,3,4),(189.605604426299,190.062376112586,191.057467086998,192.052558061409,
193.04764903582,194.042740010232,195.037830984643,195.888789733479),
 .UNSPECIFIED.);
#3456=B_SPLINE_CURVE_WITH_KNOTS('',3,(#66397,#66398,#66399,#66400,#66401),
 .UNSPECIFIED.,.F.,.F.,(4,1,4),(210.486707790516,210.557769104723,211.557480435763),
 .UNSPECIFIED.);
#3457=B_SPLINE_CURVE_WITH_KNOTS('',3,(#66407,#66408,#66409,#66410,#66411,
#66412,#66413,#66414,#66415,#66416),.UNSPECIFIED.,.F.,.F.,(4,1,1,1,1,1,
1,4),(204.203522483337,204.559501118482,205.559212449522,206.558923780562,
207.558635111602,208.558346442642,209.558057773683,210.486707790516),
 .UNSPECIFIED.);
#3458=B_SPLINE_CURVE_WITH_KNOTS('',3,(#66419,#66420,#66421,#66422,#66423,
#66424,#66425,#66426,#66427,#66428),.UNSPECIFIED.,.F.,.F.,(4,1,1,1,1,1,
1,4),(204.203522483337,204.347654708913,205.342745683324,206.337836657736,
207.332927632147,208.328018606559,209.32310958097,210.318200555382),
 .UNSPECIFIED.);
#3459=B_SPLINE_CURVE_WITH_KNOTS('',3,(#66433,#66434,#66435,#66436,#66437,
#66438,#66439,#66440,#66441,#66442),.UNSPECIFIED.,.F.,.F.,(4,1,1,1,1,1,
1,4),(197.920337176157,198.561233132242,199.560944463282,200.560655794322,
201.560367125362,202.560078456402,203.559789787442,204.203522483337),
 .UNSPECIFIED.);
#3460=B_SPLINE_CURVE_WITH_KNOTS('',3,(#66443,#66444,#66445,#66446,#66447,
#66448,#66449,#66450,#66451,#66452),.UNSPECIFIED.,.F.,.F.,(4,1,1,1,1,1,
1,4),(197.920337176157,198.377108862444,199.372199836856,200.367290811267,
201.362381785679,202.35747276009,203.352563734501,204.203522483337),
 .UNSPECIFIED.);
#3461=B_SPLINE_CURVE_WITH_KNOTS('',3,(#66457,#66458,#66459,#66460,#66461,
#66462,#66463,#66464,#66465,#66466),.UNSPECIFIED.,.F.,.F.,(4,1,1,1,1,1,
1,4),(191.637151868977,192.562965146002,193.562676477042,194.562387808082,
195.562099139122,196.561810470162,197.561521801202,197.920337176157),
 .UNSPECIFIED.);
#3462=B_SPLINE_CURVE_WITH_KNOTS('',3,(#66467,#66468,#66469,#66470,#66471,
#66472,#66473,#66474,#66475,#66476),.UNSPECIFIED.,.F.,.F.,(4,1,1,1,1,1,
1,4),(191.637151868977,192.406563015976,193.401653990387,194.396744964798,
195.39183593921,196.386926913621,197.382017888033,197.920337176157),
 .UNSPECIFIED.);
#3463=B_SPLINE_CURVE_WITH_KNOTS('',3,(#66481,#66482,#66483,#66484,#66485,
#66486,#66487,#66488,#66489,#66490,#66491),.UNSPECIFIED.,.F.,.F.,(4,1,1,
1,1,1,1,1,4),(185.353966561798,185.564985828722,186.564697159762,187.564408490802,
188.564119821842,189.563831152882,190.563542483922,191.563253814962,191.637151868977),
 .UNSPECIFIED.);
#3464=B_SPLINE_CURVE_WITH_KNOTS('',3,(#66492,#66493,#66494,#66495,#66496,
#66497,#66498,#66499,#66500,#66501,#66502),.UNSPECIFIED.,.F.,.F.,(4,1,1,
1,1,1,1,1,4),(185.353966561798,185.440926195095,186.436017169507,187.431108143918,
188.42619911833,189.421290092741,190.416381067153,191.411472041564,191.637151868977),
 .UNSPECIFIED.);
#3465=B_SPLINE_CURVE_WITH_KNOTS('',3,(#66507,#66508,#66509,#66510,#66511,
#66512,#66513,#66514,#66515,#66516),.UNSPECIFIED.,.F.,.F.,(4,1,1,1,1,1,
1,4),(179.070781254618,179.566717842481,180.566429173521,181.566140504561,
182.565851835602,183.565563166642,184.565274497682,185.353966561798),
 .UNSPECIFIED.);
#3466=B_SPLINE_CURVE_WITH_KNOTS('',3,(#66517,#66518,#66519,#66520,#66521,
#66522,#66523,#66524,#66525,#66526),.UNSPECIFIED.,.F.,.F.,(4,1,1,1,1,1,
1,4),(179.070781254618,179.470380348627,180.465471323038,181.46056229745,
182.455653271861,183.450744246273,184.445835220684,185.353966561798),
 .UNSPECIFIED.);
#3467=B_SPLINE_CURVE_WITH_KNOTS('',3,(#66531,#66532,#66533,#66534,#66535,
#66536,#66537,#66538,#66539,#66540),.UNSPECIFIED.,.F.,.F.,(4,1,1,1,1,1,
1,4),(172.787595947439,173.568449856241,174.568161187281,175.567872518321,
176.567583849361,177.567295180401,178.567006511441,179.070781254618),
 .UNSPECIFIED.);
#3468=B_SPLINE_CURVE_WITH_KNOTS('',3,(#66541,#66542,#66543,#66544,#66545,
#66546,#66547,#66548,#66549,#66550),.UNSPECIFIED.,.F.,.F.,(4,1,1,1,1,1,
1,4),(172.787595947439,173.499834502158,174.49492547657,175.490016450981,
176.485107425392,177.480198399804,178.475289374215,179.070781254618),
 .UNSPECIFIED.);
#3469=B_SPLINE_CURVE_WITH_KNOTS('',3,(#66555,#66556,#66557,#66558,#66559,
#66560,#66561,#66562,#66563,#66564,#66565),.UNSPECIFIED.,.F.,.F.,(4,1,1,
1,1,1,1,1,4),(166.504410640259,166.570470538961,167.570181870001,168.569893201041,
169.569604532081,170.569315863121,171.569027194161,172.568738525201,172.787595947439),
 .UNSPECIFIED.);
#3470=B_SPLINE_CURVE_WITH_KNOTS('',3,(#66566,#66567,#66568,#66569,#66570,
#66571,#66572,#66573,#66574,#66575,#66576),.UNSPECIFIED.,.F.,.F.,(4,1,1,
1,1,1,1,1,4),(166.504410640259,166.534197681278,167.529288655689,168.524379630101,
169.519470604512,170.514561578924,171.509652553335,172.504743527747,172.787595947439),
 .UNSPECIFIED.);
#3471=B_SPLINE_CURVE_WITH_KNOTS('',3,(#66581,#66582,#66583,#66584,#66585,
#66586,#66587,#66588,#66589,#66590),.UNSPECIFIED.,.F.,.F.,(4,1,1,1,1,1,
1,4),(160.22122533308,160.572202552721,161.571913883761,162.571625214801,
163.571336545841,164.571047876881,165.570759207921,166.504410640259),
 .UNSPECIFIED.);
#3472=B_SPLINE_CURVE_WITH_KNOTS('',3,(#66591,#66592,#66593,#66594,#66595,
#66596,#66597,#66598,#66599,#66600),.UNSPECIFIED.,.F.,.F.,(4,1,1,1,1,1,
1,4),(160.22122533308,160.563651834809,161.558742809221,162.553833783632,
163.548924758044,164.544015732455,165.539106706867,166.504410640259),
 .UNSPECIFIED.);
#3473=B_SPLINE_CURVE_WITH_KNOTS('',3,(#66605,#66606,#66607,#66608,#66609,
#66610,#66611,#66612,#66613,#66614),.UNSPECIFIED.,.F.,.F.,(4,1,1,1,1,1,
1,4),(153.9380400259,154.57393456648,155.57364589752,156.57335722856,157.573068559601,
158.572779890641,159.572491221681,160.22122533308),.UNSPECIFIED.);
#3474=B_SPLINE_CURVE_WITH_KNOTS('',3,(#66615,#66616,#66617,#66618,#66619,
#66620,#66621,#66622,#66623,#66624),.UNSPECIFIED.,.F.,.F.,(4,1,1,1,1,1,
1,4),(153.9380400259,154.593105988341,155.588196962752,156.583287937164,
157.578378911575,158.573469885986,159.568560860398,160.22122533308),
 .UNSPECIFIED.);
#3475=B_SPLINE_CURVE_WITH_KNOTS('',3,(#66629,#66630,#66631,#66632,#66633,
#66634,#66635,#66636,#66637,#66638),.UNSPECIFIED.,.F.,.F.,(4,1,1,1,1,1,
1,4),(147.65485471872,148.57566658024,149.57537791128,150.57508924232,151.57480057336,
152.5745119044,153.57422323544,153.9380400259),.UNSPECIFIED.);
#3476=B_SPLINE_CURVE_WITH_KNOTS('',3,(#66639,#66640,#66641,#66642,#66643,
#66644,#66645,#66646,#66647,#66648),.UNSPECIFIED.,.F.,.F.,(4,1,1,1,1,1,
1,4),(147.65485471872,148.622560141872,149.617651116283,150.612742090695,
151.607833065106,152.602924039518,153.598015013929,153.9380400259),
 .UNSPECIFIED.);
#3477=B_SPLINE_CURVE_WITH_KNOTS('',3,(#66653,#66654,#66655,#66656,#66657,
#66658,#66659,#66660,#66661,#66662,#66663),.UNSPECIFIED.,.F.,.F.,(4,1,1,
1,1,1,1,1,4),(141.371669411541,141.57768726296,142.577398594,143.57710992504,
144.57682125608,145.57653258712,146.57624391816,147.5759552492,147.65485471872),
 .UNSPECIFIED.);
#3478=B_SPLINE_CURVE_WITH_KNOTS('',3,(#66664,#66665,#66666,#66667,#66668,
#66669,#66670,#66671,#66672,#66673,#66674),.UNSPECIFIED.,.F.,.F.,(4,1,1,
1,1,1,1,1,4),(141.371669411541,141.656923320992,142.652014295403,143.647105269815,
144.642196244226,145.637287218638,146.632378193049,147.627469167461,147.65485471872),
 .UNSPECIFIED.);
#3479=B_SPLINE_CURVE_WITH_KNOTS('',3,(#66679,#66680,#66681,#66682,#66683,
#66684,#66685,#66686,#66687,#66688),.UNSPECIFIED.,.F.,.F.,(4,1,1,1,1,1,
1,4),(135.088484104361,135.57941927672,136.57913060776,137.5788419388,138.57855326984,
139.57826460088,140.57797593192,141.371669411541),.UNSPECIFIED.);
#3480=B_SPLINE_CURVE_WITH_KNOTS('',3,(#66689,#66690,#66691,#66692,#66693,
#66694,#66695,#66696,#66697,#66698),.UNSPECIFIED.,.F.,.F.,(4,1,1,1,1,1,
1,4),(135.088484104361,135.686377474523,136.681468448935,137.676559423346,
138.671650397758,139.666741372169,140.66183234658,141.371669411541),
 .UNSPECIFIED.);
#3481=B_SPLINE_CURVE_WITH_KNOTS('',3,(#66703,#66704,#66705,#66706,#66707,
#66708,#66709,#66710,#66711,#66712),.UNSPECIFIED.,.F.,.F.,(4,1,1,1,1,1,
1,4),(128.805298797182,129.581151290479,130.58086262152,131.58057395256,
132.5802852836,133.57999661464,134.57970794568,135.088484104361),
 .UNSPECIFIED.);
#3482=B_SPLINE_CURVE_WITH_KNOTS('',3,(#66713,#66714,#66715,#66716,#66717,
#66718,#66719,#66720,#66721,#66722),.UNSPECIFIED.,.F.,.F.,(4,1,1,1,1,1,
1,4),(128.805298797182,129.715831628055,130.710922602466,131.706013576877,
132.701104551289,133.6961955257,134.691286500112,135.088484104361),
 .UNSPECIFIED.);
#3483=B_SPLINE_CURVE_WITH_KNOTS('',3,(#66727,#66728,#66729,#66730,#66731,
#66732,#66733,#66734,#66735,#66736,#66737),.UNSPECIFIED.,.F.,.F.,(4,1,1,
1,1,1,1,1,4),(122.522113490002,122.583171973199,123.582883304239,124.582594635279,
125.582305966319,126.582017297359,127.581728628399,128.581439959439,128.805298797182),
 .UNSPECIFIED.);
#3484=B_SPLINE_CURVE_WITH_KNOTS('',3,(#66738,#66739,#66740,#66741,#66742,
#66743,#66744,#66745,#66746,#66747,#66748),.UNSPECIFIED.,.F.,.F.,(4,1,1,
1,1,1,1,1,4),(122.522113490002,122.750194807174,123.745285781586,124.740376755997,
125.735467730409,126.73055870482,127.725649679232,128.720740653643,128.805298797182),
 .UNSPECIFIED.);
#3485=B_SPLINE_CURVE_WITH_KNOTS('',3,(#66753,#66754,#66755,#66756,#66757,
#66758,#66759,#66760,#66761,#66762),.UNSPECIFIED.,.F.,.F.,(4,1,1,1,1,1,
1,4),(116.238928182823,116.584903986959,117.584615317999,118.584326649039,
119.584037980079,120.583749311119,121.583460642159,122.522113490002),
 .UNSPECIFIED.);
#3486=B_SPLINE_CURVE_WITH_KNOTS('',3,(#66763,#66764,#66765,#66766,#66767,
#66768,#66769,#66770,#66771,#66772),.UNSPECIFIED.,.F.,.F.,(4,1,1,1,1,1,
1,4),(116.238928182823,116.779648960706,117.774739935117,118.769830909529,
119.76492188394,120.760012858352,121.755103832763,122.522113490002),
 .UNSPECIFIED.);
#3487=B_SPLINE_CURVE_WITH_KNOTS('',3,(#66777,#66778,#66779,#66780,#66781,
#66782,#66783,#66784,#66785,#66786),.UNSPECIFIED.,.F.,.F.,(4,1,1,1,1,1,
1,4),(109.955742875643,110.586636000719,111.586347331759,112.586058662799,
113.585769993839,114.585481324879,115.585192655919,116.238928182823),
 .UNSPECIFIED.);
#3488=B_SPLINE_CURVE_WITH_KNOTS('',3,(#66787,#66788,#66789,#66790,#66791,
#66792,#66793,#66794,#66795,#66796),.UNSPECIFIED.,.F.,.F.,(4,1,1,1,1,1,
1,4),(109.955742875643,110.809103114237,111.804194088649,112.79928506306,
113.794376037471,114.789467011883,115.784557986294,116.238928182823),
 .UNSPECIFIED.);
#3489=B_SPLINE_CURVE_WITH_KNOTS('',3,(#66801,#66802,#66803,#66804,#66805,
#66806,#66807,#66808,#66809,#66810),.UNSPECIFIED.,.F.,.F.,(4,1,1,1,1,1,
1,4),(103.672557568463,104.588368014479,105.588079345519,106.587790676559,
107.587502007599,108.587213338639,109.586924669679,109.955742875643),
 .UNSPECIFIED.);
#3490=B_SPLINE_CURVE_WITH_KNOTS('',3,(#66811,#66812,#66813,#66814,#66815,
#66816,#66817,#66818,#66819,#66820,#66821),.UNSPECIFIED.,.F.,.F.,(4,1,1,
1,1,1,1,1,4),(103.672557568463,103.843466293357,104.838557267768,105.83364824218,
106.828739216591,107.823830191003,108.818921165414,109.814012139826,109.955742875643),
 .UNSPECIFIED.);
#3491=B_SPLINE_CURVE_WITH_KNOTS('',3,(#66826,#66827,#66828,#66829,#66830,
#66831,#66832,#66833,#66834,#66835,#66836),.UNSPECIFIED.,.F.,.F.,(4,1,1,
1,1,1,1,1,4),(97.3893722612838,97.5903886971983,98.5901000282383,99.5898113592783,
100.589522690318,101.589234021358,102.588945352398,103.588656683438,103.672557568463),
 .UNSPECIFIED.);
#3492=B_SPLINE_CURVE_WITH_KNOTS('',3,(#66837,#66838,#66839,#66840,#66841,
#66842,#66843,#66844,#66845,#66846),.UNSPECIFIED.,.F.,.F.,(4,1,1,1,1,1,
1,4),(97.3893722612838,97.8729204468883,98.8680114212997,99.8631023957112,
100.858193370123,101.853284344534,102.848375318946,103.672557568463),
 .UNSPECIFIED.);
#3493=B_SPLINE_CURVE_WITH_KNOTS('',3,(#66851,#66852,#66853,#66854,#66855,
#66856,#66857,#66858,#66859,#66860),.UNSPECIFIED.,.F.,.F.,(4,1,1,1,1,1,
1,4),(91.1061869541042,91.592120710958,92.5918320419981,93.5915433730381,
94.5912547040781,95.5909660351182,96.5906773661582,97.3893722612838),
 .UNSPECIFIED.);
#3494=B_SPLINE_CURVE_WITH_KNOTS('',3,(#66861,#66862,#66863,#66864,#66865,
#66866,#66867,#66868,#66869,#66870),.UNSPECIFIED.,.F.,.F.,(4,1,1,1,1,1,
1,4),(91.1061869541042,91.9023746004196,92.897465574831,93.8925565492425,
94.8876475236539,95.8827384980654,96.8778294724768,97.3893722612838),
 .UNSPECIFIED.);
#3495=B_SPLINE_CURVE_WITH_KNOTS('',3,(#66875,#66876,#66877,#66878,#66879,
#66880,#66881,#66882,#66883,#66884),.UNSPECIFIED.,.F.,.F.,(4,1,1,1,1,1,
1,4),(84.8230016469246,85.5938527247178,86.5935640557578,87.5932753867979,
88.5929867178379,89.5926980488779,90.592409379918,91.1061869541042),
 .UNSPECIFIED.);
#3496=B_SPLINE_CURVE_WITH_KNOTS('',3,(#66885,#66886,#66887,#66888,#66889,
#66890,#66891,#66892,#66893,#66894,#66895),.UNSPECIFIED.,.F.,.F.,(4,1,1,
1,1,1,1,1,4),(84.8230016469246,84.9367377795395,85.9318287539509,86.9269197283624,
87.9220107027738,88.9171016771853,89.9121926515967,90.9072836260082,91.1061869541042),
 .UNSPECIFIED.);
#3497=B_SPLINE_CURVE_WITH_KNOTS('',3,(#66900,#66901,#66902,#66903,#66904,
#66905,#66906,#66907,#66908,#66909,#66910),.UNSPECIFIED.,.F.,.F.,(4,1,1,
1,1,1,1,1,4),(78.539816339745,78.5958734074375,79.5955847384776,80.5952960695176,
81.5950074005576,82.5947187315977,83.5944300626377,84.5941413936777,84.8230016469246),
 .UNSPECIFIED.);
#3498=B_SPLINE_CURVE_WITH_KNOTS('',3,(#66911,#66912,#66913,#66914,#66915,
#66916,#66917,#66918,#66919,#66920),.UNSPECIFIED.,.F.,.F.,(4,1,1,1,1,1,
1,4),(78.539816339745,78.9661919330708,79.9612829074823,80.9563738818937,
81.9514648563052,82.9465558307166,83.941646805128,84.8230016469246),
 .UNSPECIFIED.);
#3499=B_SPLINE_CURVE_WITH_KNOTS('',3,(#66925,#66926,#66927,#66928,#66929,
#66930,#66931,#66932,#66933,#66934),.UNSPECIFIED.,.F.,.F.,(4,1,1,1,1,1,
1,4),(72.2566310325654,72.5976054211973,73.5973167522373,74.5970280832774,
75.5967394143174,76.5964507453574,77.5961620763975,78.539816339745),
 .UNSPECIFIED.);
#3500=B_SPLINE_CURVE_WITH_KNOTS('',3,(#66935,#66936,#66937,#66938,#66939,
#66940,#66941,#66942,#66943,#66944),.UNSPECIFIED.,.F.,.F.,(4,1,1,1,1,1,
1,4),(72.2566310325654,72.9956460866021,73.9907370610136,74.985828035425,
75.9809190098365,76.9760099842479,77.9711009586594,78.539816339745),
 .UNSPECIFIED.);
#3501=B_SPLINE_CURVE_WITH_KNOTS('',3,(#66949,#66950,#66951,#66952,#66953,
#66954,#66955,#66956,#66957,#66958),.UNSPECIFIED.,.F.,.F.,(4,1,1,1,1,1,
1,4),(65.9734457253858,66.5993374349571,67.5990487659971,68.5987600970371,
69.5984714280772,70.5981827591172,71.5978940901573,72.2566310325654),
 .UNSPECIFIED.);
#3502=B_SPLINE_CURVE_WITH_KNOTS('',3,(#66959,#66960,#66961,#66962,#66963,
#66964,#66965,#66966,#66967,#66968,#66969),.UNSPECIFIED.,.F.,.F.,(4,1,1,
1,1,1,1,1,4),(65.9734457253858,66.030009265722,67.0251002401335,68.0201912145449,
69.0152821889564,70.0103731633678,71.0054641377792,72.0005551121907,72.2566310325654),
 .UNSPECIFIED.);
#3503=B_SPLINE_CURVE_WITH_KNOTS('',3,(#66974,#66975,#66976,#66977,#66978,
#66979,#66980,#66981,#66982,#66983),.UNSPECIFIED.,.F.,.F.,(4,1,1,1,1,1,
1,4),(59.6902604182062,60.6010694487168,61.6007807797569,62.6004921107969,
63.6002034418369,64.599914772877,65.599626103917,65.9734457253858),
 .UNSPECIFIED.);
#3504=B_SPLINE_CURVE_WITH_KNOTS('',3,(#66984,#66985,#66986,#66987,#66988,
#66989,#66990,#66991,#66992,#66993),.UNSPECIFIED.,.F.,.F.,(4,1,1,1,1,1,
1,4),(59.6902604182063,60.0594634192534,61.0545543936648,62.0496453680762,
63.0447363424877,64.0398273168991,65.0349182913106,65.9734457253858),
 .UNSPECIFIED.);
#3505=B_SPLINE_CURVE_WITH_KNOTS('',3,(#66998,#66999,#67000,#67001,#67002,
#67003,#67004,#67005,#67006,#67007,#67008),.UNSPECIFIED.,.F.,.F.,(4,1,1,
1,1,1,1,1,4),(53.4070751110266,53.6030901314366,54.6028014624766,55.6025127935166,
56.6022241245567,57.6019354555967,58.6016467866367,59.6013581176768,59.6902604182062),
 .UNSPECIFIED.);
#3506=B_SPLINE_CURVE_WITH_KNOTS('',3,(#67009,#67010,#67011,#67012,#67013,
#67014,#67015,#67016,#67017,#67018),.UNSPECIFIED.,.F.,.F.,(4,1,1,1,1,1,
1,4),(53.4070751110267,54.0889175727847,55.0840085471961,56.0790995216076,
57.074190496019,58.0692814704305,59.0643724448419,59.6902604182063),
 .UNSPECIFIED.);
#3507=B_SPLINE_CURVE_WITH_KNOTS('',3,(#67023,#67024,#67025,#67026,#67027,
#67028,#67029,#67030,#67031,#67032),.UNSPECIFIED.,.F.,.F.,(4,1,1,1,1,1,
1,4),(47.123889803847,47.6048221451963,48.6045334762364,49.6042448072764,
50.6039561383164,51.6036674693565,52.6033788003965,53.4070751110266),
 .UNSPECIFIED.);
#3508=B_SPLINE_CURVE_WITH_KNOTS('',3,(#67033,#67034,#67035,#67036,#67037,
#67038,#67039,#67040,#67041,#67042),.UNSPECIFIED.,.F.,.F.,(4,1,1,1,1,1,
1,4),(47.1238898038471,48.118371726316,49.1134627007275,50.1085536751389,
51.1036446495503,52.0987356239618,53.0938265983732,53.4070751110267),
 .UNSPECIFIED.);
#3509=B_SPLINE_CURVE_WITH_KNOTS('',3,(#67047,#67048,#67049,#67050,#67051,
#67052,#67053,#67054,#67055,#67056),.UNSPECIFIED.,.F.,.F.,(4,1,1,1,1,1,
1,4),(40.8407044966674,41.6065541589561,42.6062654899961,43.6059768210362,
44.6056881520762,45.6053994831162,46.6051108141563,47.123889803847),
 .UNSPECIFIED.);
#3510=B_SPLINE_CURVE_WITH_KNOTS('',3,(#67057,#67058,#67059,#67060,#67061,
#67062,#67063,#67064,#67065,#67066,#67067),.UNSPECIFIED.,.F.,.F.,(4,1,1,
1,1,1,1,1,4),(40.8407044966675,41.1527349054359,42.1478258798473,43.1429168542588,
44.1380078286702,45.1330988030817,46.1281897774931,47.1232807519046,47.1238898038471),
 .UNSPECIFIED.);
#3511=B_SPLINE_CURVE_WITH_KNOTS('',3,(#67072,#67073,#67074,#67075,#67076,
#67077,#67078,#67079,#67080,#67081,#67082),.UNSPECIFIED.,.F.,.F.,(4,1,1,
1,1,1,1,1,4),(34.5575191894878,34.6085748416758,35.6082861727159,36.6079975037559,
37.6077088347959,38.607420165836,39.607131496876,40.6068428279161,40.8407044966674),
 .UNSPECIFIED.);
#3512=B_SPLINE_CURVE_WITH_KNOTS('',3,(#67083,#67084,#67085,#67086,#67087,
#67088,#67089,#67090,#67091,#67092),.UNSPECIFIED.,.F.,.F.,(4,1,1,1,1,1,
1,4),(34.5575191894879,35.1821890589672,36.1772800333787,37.1723710077901,
38.1674619822016,39.162552956613,40.1576439310244,40.8407044966675),
 .UNSPECIFIED.);
#3513=B_SPLINE_CURVE_WITH_KNOTS('',3,(#67097,#67098,#67099,#67100,#67101,
#67102,#67103,#67104,#67105,#67106),.UNSPECIFIED.,.F.,.F.,(4,1,1,1,1,1,
1,4),(28.2743338823082,28.6103068554356,29.6100181864756,30.6097295175157,
31.6094408485557,32.6091521795958,33.6088635106358,34.5575191894878),
 .UNSPECIFIED.);
#3514=B_SPLINE_CURVE_WITH_KNOTS('',3,(#67107,#67108,#67109,#67110,#67111,
#67112,#67113,#67114,#67115,#67116),.UNSPECIFIED.,.F.,.F.,(4,1,1,1,1,1,
1,4),(28.2743338823083,29.2116432124985,30.20673418691,31.2018251613214,
32.1969161357329,33.1920071101443,34.1870980845558,34.5575191894879),
 .UNSPECIFIED.);
#3515=B_SPLINE_CURVE_WITH_KNOTS('',3,(#67121,#67122,#67123,#67124,#67125,
#67126,#67127,#67128,#67129,#67130),.UNSPECIFIED.,.F.,.F.,(4,1,1,1,1,1,
1,4),(21.9911485751287,22.6120388691954,23.6117502002354,24.6114615312754,
25.6111728623155,26.6108841933555,27.6105955243956,28.2743338823082),
 .UNSPECIFIED.);
#3516=B_SPLINE_CURVE_WITH_KNOTS('',3,(#67131,#67132,#67133,#67134,#67135,
#67136,#67137,#67138,#67139,#67140,#67141),.UNSPECIFIED.,.F.,.F.,(4,1,1,
1,1,1,1,1,4),(21.9911485751287,22.2460063916184,23.2410973660299,24.2361883404413,
25.2312793148528,26.2263702892642,27.2214612636757,28.2165522380871,28.2743338823083),
 .UNSPECIFIED.);
#3517=B_SPLINE_CURVE_WITH_KNOTS('',3,(#67146,#67147,#67148,#67149,#67150,
#67151,#67152,#67153,#67154,#67155),.UNSPECIFIED.,.F.,.F.,(4,1,1,1,1,1,
1,4),(15.7079632679491,16.6137708829551,17.6134822139952,18.6131935450352,
19.6129048760753,20.6126162071153,21.6123275381553,21.9911485751287),
 .UNSPECIFIED.);
#3518=B_SPLINE_CURVE_WITH_KNOTS('',3,(#67156,#67157,#67158,#67159,#67160,
#67161,#67162,#67163,#67164,#67165),.UNSPECIFIED.,.F.,.F.,(4,1,1,1,1,1,
1,4),(15.7079632679491,16.2754605451498,17.2705515195612,18.2656424939726,
19.2607334683841,20.2558244427955,21.250915417207,21.9911485751287),
 .UNSPECIFIED.);
#3519=B_SPLINE_CURVE_WITH_KNOTS('',3,(#67171,#67172,#67173,#67174,#67175,
#67176,#67177,#67178,#67179,#67180,#67181,#67182,#67183,#67184,#67185,#67186,
#67187,#67188,#67189,#67190,#67191,#67192,#67193,#67194,#67195,#67196,#67197,
#67198,#67199,#67200,#67201,#67202,#67203,#67204,#67205,#67206,#67207,#67208,
#67209,#67210,#67211,#67212,#67213,#67214,#67215,#67216,#67217,#67218,#67219,
#67220,#67221,#67222,#67223,#67224,#67225,#67226,#67227,#67228,#67229,#67230,
#67231,#67232,#67233,#67234,#67235,#67236,#67237,#67238,#67239,#67240,#67241,
#67242,#67243,#67244,#67245,#67246,#67247,#67248,#67249,#67250,#67251,#67252,
#67253,#67254,#67255,#67256,#67257,#67258,#67259,#67260,#67261,#67262,#67263,
#67264,#67265,#67266,#67267,#67268,#67269,#67270,#67271,#67272,#67273,#67274,
#67275,#67276,#67277,#67278,#67279,#67280,#67281,#67282,#67283,#67284,#67285,
#67286,#67287,#67288,#67289,#67290,#67291,#67292,#67293,#67294,#67295,#67296,
#67297,#67298,#67299,#67300,#67301,#67302,#67303,#67304,#67305,#67306,#67307,
#67308,#67309,#67310,#67311,#67312,#67313,#67314,#67315,#67316,#67317,#67318,
#67319,#67320,#67321,#67322,#67323,#67324,#67325,#67326,#67327,#67328,#67329,
#67330,#67331,#67332,#67333,#67334,#67335,#67336,#67337,#67338,#67339,#67340,
#67341,#67342,#67343,#67344,#67345,#67346,#67347,#67348,#67349,#67350,#67351,
#67352,#67353,#67354,#67355,#67356,#67357,#67358,#67359,#67360,#67361,#67362,
#67363,#67364,#67365,#67366,#67367,#67368,#67369,#67370,#67371,#67372,#67373,
#67374,#67375,#67376,#67377,#67378,#67379,#67380,#67381,#67382,#67383,#67384,
#67385,#67386,#67387,#67388,#67389,#67390,#67391,#67392,#67393,#67394,#67395,
#67396,#67397,#67398,#67399,#67400,#67401,#67402,#67403,#67404,#67405,#67406,
#67407,#67408,#67409,#67410,#67411,#67412,#67413,#67414,#67415,#67416,#67417,
#67418,#67419,#67420,#67421,#67422,#67423,#67424,#67425,#67426,#67427,#67428,
#67429),.UNSPECIFIED.,.F.,.F.,(4,3,3,3,3,3,3,3,3,3,3,3,3,3,3,3,3,3,3,3,
3,3,3,3,3,3,3,3,3,3,3,3,3,3,3,3,3,3,3,3,3,3,3,3,3,3,3,3,3,3,3,3,3,3,3,3,
3,3,3,3,3,3,3,3,3,3,3,3,3,3,3,3,3,3,3,3,3,3,3,3,3,3,3,3,3,3,4),(-2.02747957522477,
-1.99629697890573,-1.96434882803362,-1.94770684698045,-1.93465745109861,
-1.92899323505435,-1.89637939967214,-1.86351156618679,-1.84191868086962,
-1.83643395258831,-1.80184474723693,-1.76878588804004,-1.7361915602774,
-1.71713434573009,-1.71111396618423,-1.70636535171271,-1.69807713118279,
-1.66615334411595,-1.63338107755074,-1.59870970356575,-1.58354097744731,
-1.57777243171763,-1.57288272657502,-1.53932550715147,-1.50538593530636,
-1.47155442193573,-1.45678251339105,-1.44498318417569,-1.44016588491778,
-1.40590427589964,-1.372125965904,-1.35601008567079,-1.32227811773956,-1.3110762482785,
-1.30413477324209,-1.27089096674751,-1.23651000513344,-1.20188424717791,
-1.17687285717032,-1.17117345644662,-1.16636983006357,-1.13156642853056,
-1.09668061447692,-1.06224151139586,-1.03201731925653,-1.02689100048705,
-1.00179312711721,-0.967864540839157,-0.93313532953401,-0.897918428976919,
-0.890942884625253,-0.885051901025072,-0.849845686106437,-0.814185285823995,
-0.778541242116049,-0.760617194519175,-0.745868237951496,-0.740902737283996,
-0.704880648128088,-0.669414287483829,-0.635148861341054,-0.611477896978161,
-0.602075382147568,-0.596900307049893,-0.562097694744849,-0.526417664836126,
-0.490045423902471,-0.460841424856508,-0.453624100180632,-0.448600894627828,
-0.412078836391778,-0.375321168507609,-0.339131447204507,-0.318451943287073,
-0.304419386760625,-0.299402690224966,-0.262514781947601,-0.25641343153477,
-0.220343758631792,-0.183630684098196,-0.160676848585921,-0.153063253496153,
-0.14786021524992,-0.11089516143744,-0.073565266371696,-0.0362697295661738,
0.),.UNSPECIFIED.);
#3520=B_SPLINE_CURVE_WITH_KNOTS('',3,(#67433,#67434,#67435,#67436,#67437,
#67438,#67439,#67440,#67441,#67442,#67443,#67444,#67445,#67446,#67447,#67448,
#67449,#67450,#67451,#67452,#67453,#67454,#67455,#67456,#67457,#67458,#67459,
#67460,#67461,#67462,#67463,#67464,#67465,#67466,#67467,#67468,#67469,#67470,
#67471,#67472,#67473,#67474,#67475,#67476,#67477,#67478,#67479,#67480,#67481),
 .UNSPECIFIED.,.F.,.F.,(4,3,3,3,3,3,3,3,3,3,3,3,3,3,3,3,4),(-0.379502319520043,
-0.35268354233973,-0.317392763997328,-0.282090054200831,-0.271802233255953,
-0.267093649425612,-0.233020332933001,-0.198977913737098,-0.165391137616394,
-0.144717245414345,-0.134595686290805,-0.130270172117405,-0.097702629088054,
-0.0656991121917264,-0.0328495560958632,-0.00219762996067144,0.),
 .UNSPECIFIED.);
#3521=B_SPLINE_CURVE_WITH_KNOTS('',3,(#67483,#67484,#67485,#67486,#67487,
#67488,#67489,#67490,#67491,#67492,#67493,#67494,#67495,#67496,#67497,#67498,
#67499,#67500,#67501,#67502,#67503,#67504,#67505,#67506,#67507),
 .UNSPECIFIED.,.F.,.F.,(4,3,3,3,3,3,3,3,4),(-0.549622632142038,-0.513019755170316,
-0.477082564278427,-0.4417887745146,-0.426217160765961,-0.417941853469451,
-0.412784386135711,-0.408981449436597,-0.379502319520043),.UNSPECIFIED.);
#3522=B_SPLINE_CURVE_WITH_KNOTS('',3,(#68321,#68322,#68323,#68324,#68325,
#68326,#68327,#68328),.UNSPECIFIED.,.F.,.F.,(4,1,1,1,1,4),(11.6152142277549,
12.614925558795,13.614636889835,14.6143482208751,15.6140595519151,15.7079632679491),
 .UNSPECIFIED.);
#3523=B_SPLINE_CURVE_WITH_KNOTS('',3,(#68329,#68330,#68331,#68332,#68333,
#68334,#68335,#68336,#68337,#68338,#68339,#68340,#68341,#68342,#68343,#68344,
#68345,#68346,#68347,#68348,#68349,#68350,#68351,#68352,#68353,#68354,#68355,
#68356,#68357,#68358,#68359,#68360,#68361,#68362,#68363,#68364,#68365,#68366,
#68367,#68368,#68369,#68370,#68371,#68372,#68373,#68374,#68375,#68376,#68377,
#68378,#68379,#68380,#68381,#68382,#68383,#68384,#68385,#68386,#68387,#68388,
#68389,#68390,#68391,#68392,#68393,#68394,#68395,#68396,#68397,#68398,#68399,
#68400,#68401,#68402,#68403,#68404,#68405,#68406,#68407,#68408,#68409,#68410,
#68411,#68412,#68413,#68414,#68415,#68416,#68417,#68418,#68419,#68420,#68421,
#68422,#68423,#68424,#68425),.UNSPECIFIED.,.F.,.F.,(4,3,3,3,3,3,3,3,3,3,
3,3,3,3,3,3,3,3,3,3,3,3,3,3,3,3,3,3,3,3,3,3,4),(-0.741270768406377,-0.717014623295539,
-0.680491508968579,-0.659046519725601,-0.642659659722095,-0.636144348715375,
-0.599359723630772,-0.567173176681745,-0.553071549886647,-0.544359430417001,
-0.537677536280526,-0.502275731429912,-0.467137784296744,-0.43303904778729,
-0.410246122850107,-0.399258187406409,-0.39485296865865,-0.361233284053521,
-0.341867348038558,-0.307605174602581,-0.273187750648466,-0.26292576164664,
-0.257107052763031,-0.223674627080457,-0.190212894077251,-0.15716430044683,
-0.137518762890977,-0.127951707437281,-0.12318250736928,-0.0909836130414784,
-0.0592393070967323,-0.028471589982648,0.),.UNSPECIFIED.);
#3524=B_SPLINE_CURVE_WITH_KNOTS('',3,(#68428,#68429,#68430,#68431,#68432,
#68433,#68434,#68435,#68436),.UNSPECIFIED.,.F.,.F.,(4,1,1,1,1,1,4),(10.375934347374,
11.3000056730925,12.295096647504,13.2901876219154,14.2852785963269,15.2803695707383,
15.7079632679491),.UNSPECIFIED.);
#3525=B_SPLINE_CURVE_WITH_KNOTS('',3,(#69262,#69263,#69264,#69265,#69266,
#69267,#69268),.UNSPECIFIED.,.F.,.F.,(4,3,4),(195.888789733479,196.032921959055,
196.372160316468),.UNSPECIFIED.);
#3526=B_SPLINE_CURVE_WITH_KNOTS('',3,(#69269,#69270,#69271,#69272,#69273,
#69274,#69275,#69276,#69277,#69278,#69279,#69280,#69281,#69282,#69283,#69284,
#69285,#69286,#69287,#69288,#69289,#69290,#69291,#69292,#69293,#69294,#69295,
#69296,#69297,#69298,#69299,#69300,#69301,#69302,#69303,#69304,#69305,#69306,
#69307,#69308,#69309,#69310,#69311,#69312,#69313,#69314,#69315,#69316,#69317,
#69318,#69319,#69320,#69321,#69322,#69323,#69324,#69325,#69326,#69327,#69328,
#69329,#69330,#69331,#69332,#69333,#69334,#69335,#69336,#69337,#69338,#69339,
#69340,#69341,#69342,#69343,#69344,#69345,#69346,#69347,#69348,#69349,#69350,
#69351,#69352,#69353,#69354,#69355,#69356,#69357,#69358,#69359,#69360,#69361,
#69362,#69363,#69364,#69365,#69366,#69367,#69368),.UNSPECIFIED.,.F.,.F.,
(4,3,3,3,3,3,3,3,3,3,3,3,3,3,3,3,3,3,3,3,3,3,3,3,3,3,3,3,3,3,3,3,3,4),(-0.744397949170583,
-0.721187707565161,-0.690060066224835,-0.670522596439773,-0.661245127518269,
-0.655323531675899,-0.623354149124615,-0.592617449192018,-0.579170142971507,
-0.572605591331247,-0.567933946140104,-0.534583176062334,-0.500700944806229,
-0.466885135058086,-0.444528988709526,-0.437828648817827,-0.433043709852644,
-0.398130555533214,-0.377460549663844,-0.343724507848801,-0.309355146205245,
-0.297653275947071,-0.292702465404463,-0.258301310351799,-0.222794013971477,
-0.186953470658781,-0.163584286826433,-0.155883350189299,-0.150570414508087,
-0.145643391754365,-0.108904568168204,-0.0721037270654814,-0.0359977762023965,
0.),.UNSPECIFIED.);
#4290=LINE('',#64833,#5138);
#4291=LINE('',#64857,#5139);
#4292=LINE('',#64905,#5140);
#4293=LINE('',#64953,#5141);
#4294=LINE('',#65004,#5142);
#4295=LINE('',#65055,#5143);
#4296=LINE('',#65103,#5144);
#4297=LINE('',#65151,#5145);
#4298=LINE('',#65202,#5146);
#4299=LINE('',#65250,#5147);
#4300=LINE('',#65298,#5148);
#4301=LINE('',#65349,#5149);
#4302=LINE('',#65400,#5150);
#4303=LINE('',#65448,#5151);
#4304=LINE('',#65499,#5152);
#4305=LINE('',#65550,#5153);
#4306=LINE('',#65598,#5154);
#4307=LINE('',#65649,#5155);
#4308=LINE('',#65697,#5156);
#4309=LINE('',#65748,#5157);
#4310=LINE('',#65799,#5158);
#4311=LINE('',#65847,#5159);
#4312=LINE('',#65898,#5160);
#4313=LINE('',#65949,#5161);
#4314=LINE('',#65997,#5162);
#4315=LINE('',#66045,#5163);
#4316=LINE('',#66096,#5164);
#4317=LINE('',#66147,#5165);
#4318=LINE('',#66195,#5166);
#4319=LINE('',#66246,#5167);
#4320=LINE('',#66297,#5168);
#4321=LINE('',#66345,#5169);
#4322=LINE('',#66395,#5170);
#4323=LINE('',#66406,#5171);
#4324=LINE('',#66432,#5172);
#4325=LINE('',#66456,#5173);
#4326=LINE('',#66480,#5174);
#4327=LINE('',#66506,#5175);
#4328=LINE('',#66530,#5176);
#4329=LINE('',#66554,#5177);
#4330=LINE('',#66580,#5178);
#4331=LINE('',#66604,#5179);
#4332=LINE('',#66628,#5180);
#4333=LINE('',#66652,#5181);
#4334=LINE('',#66678,#5182);
#4335=LINE('',#66702,#5183);
#4336=LINE('',#66726,#5184);
#4337=LINE('',#66752,#5185);
#4338=LINE('',#66776,#5186);
#4339=LINE('',#66800,#5187);
#4340=LINE('',#66825,#5188);
#4341=LINE('',#66850,#5189);
#4342=LINE('',#66874,#5190);
#4343=LINE('',#66899,#5191);
#4344=LINE('',#66924,#5192);
#4345=LINE('',#66948,#5193);
#4346=LINE('',#66973,#5194);
#4347=LINE('',#66997,#5195);
#4348=LINE('',#67022,#5196);
#4349=LINE('',#67046,#5197);
#4350=LINE('',#67071,#5198);
#4351=LINE('',#67096,#5199);
#4352=LINE('',#67120,#5200);
#4353=LINE('',#67145,#5201);
#4354=LINE('',#67168,#5202);
#4355=LINE('',#67431,#5203);
#4356=LINE('',#69373,#5204);
#4357=LINE('',#69375,#5205);
#4358=LINE('',#69377,#5206);
#4359=LINE('',#69378,#5207);
#4360=LINE('',#69381,#5208);
#4361=LINE('',#69383,#5209);
#4362=LINE('',#69384,#5210);
#4363=LINE('',#69387,#5211);
#4364=LINE('',#69389,#5212);
#4365=LINE('',#69390,#5213);
#4366=LINE('',#69393,#5214);
#4367=LINE('',#69395,#5215);
#4368=LINE('',#69396,#5216);
#4369=LINE('',#69399,#5217);
#4370=LINE('',#69401,#5218);
#4371=LINE('',#69402,#5219);
#4372=LINE('',#69404,#5220);
#4373=LINE('',#69405,#5221);
#4374=LINE('',#69412,#5222);
#5138=VECTOR('',#18350,4.);
#5139=VECTOR('',#18355,4.);
#5140=VECTOR('',#18358,4.);
#5141=VECTOR('',#18361,4.);
#5142=VECTOR('',#18364,4.);
#5143=VECTOR('',#18367,4.);
#5144=VECTOR('',#18370,4.);
#5145=VECTOR('',#18373,4.);
#5146=VECTOR('',#18376,4.);
#5147=VECTOR('',#18379,4.);
#5148=VECTOR('',#18382,4.);
#5149=VECTOR('',#18385,4.);
#5150=VECTOR('',#18388,4.);
#5151=VECTOR('',#18391,4.);
#5152=VECTOR('',#18394,4.);
#5153=VECTOR('',#18397,4.);
#5154=VECTOR('',#18400,4.);
#5155=VECTOR('',#18403,4.);
#5156=VECTOR('',#18406,4.);
#5157=VECTOR('',#18409,4.);
#5158=VECTOR('',#18412,4.);
#5159=VECTOR('',#18415,4.);
#5160=VECTOR('',#18418,4.);
#5161=VECTOR('',#18421,4.);
#5162=VECTOR('',#18424,4.);
#5163=VECTOR('',#18427,4.);
#5164=VECTOR('',#18430,4.);
#5165=VECTOR('',#18433,4.);
#5166=VECTOR('',#18436,4.);
#5167=VECTOR('',#18439,4.);
#5168=VECTOR('',#18442,4.);
#5169=VECTOR('',#18445,4.);
#5170=VECTOR('',#18450,3.22275);
#5171=VECTOR('',#18455,3.22275);
#5172=VECTOR('',#18460,3.22275);
#5173=VECTOR('',#18463,3.22275);
#5174=VECTOR('',#18466,3.22275);
#5175=VECTOR('',#18469,3.22275);
#5176=VECTOR('',#18472,3.22275);
#5177=VECTOR('',#18475,3.22275);
#5178=VECTOR('',#18478,3.22275);
#5179=VECTOR('',#18481,3.22275);
#5180=VECTOR('',#18484,3.22275);
#5181=VECTOR('',#18487,3.22275);
#5182=VECTOR('',#18490,3.22275);
#5183=VECTOR('',#18493,3.22275);
#5184=VECTOR('',#18496,3.22275);
#5185=VECTOR('',#18499,3.22275);
#5186=VECTOR('',#18502,3.22275);
#5187=VECTOR('',#18505,3.22275);
#5188=VECTOR('',#18508,3.22275);
#5189=VECTOR('',#18511,3.22275);
#5190=VECTOR('',#18514,3.22275);
#5191=VECTOR('',#18517,3.22275);
#5192=VECTOR('',#18520,3.22275);
#5193=VECTOR('',#18523,3.22275);
#5194=VECTOR('',#18526,3.22275);
#5195=VECTOR('',#18529,3.22275);
#5196=VECTOR('',#18532,3.22275);
#5197=VECTOR('',#18535,3.22275);
#5198=VECTOR('',#18538,3.22275);
#5199=VECTOR('',#18541,3.22275);
#5200=VECTOR('',#18544,3.22275);
#5201=VECTOR('',#18547,3.22275);
#5202=VECTOR('',#18550,3.5);
#5203=VECTOR('',#18553,3.5);
#5204=VECTOR('',#18566,10.);
#5205=VECTOR('',#18567,10.);
#5206=VECTOR('',#18568,10.);
#5207=VECTOR('',#18569,10.);
#5208=VECTOR('',#18572,10.);
#5209=VECTOR('',#18573,10.);
#5210=VECTOR('',#18574,10.);
#5211=VECTOR('',#18577,10.);
#5212=VECTOR('',#18578,10.);
#5213=VECTOR('',#18579,10.);
#5214=VECTOR('',#18582,10.);
#5215=VECTOR('',#18583,10.);
#5216=VECTOR('',#18584,10.);
#5217=VECTOR('',#18587,10.);
#5218=VECTOR('',#18588,10.);
#5219=VECTOR('',#18589,10.);
#5220=VECTOR('',#18592,10.);
#5221=VECTOR('',#18593,10.);
#5222=VECTOR('',#18602,6.5);
#6545=VERTEX_POINT('',#64831);
#6546=VERTEX_POINT('',#64832);
#6547=VERTEX_POINT('',#64834);
#6548=VERTEX_POINT('',#64845);
#6549=VERTEX_POINT('',#64855);
#6550=VERTEX_POINT('',#64856);
#6551=VERTEX_POINT('',#64903);
#6552=VERTEX_POINT('',#64904);
#6553=VERTEX_POINT('',#64951);
#6554=VERTEX_POINT('',#64952);
#6555=VERTEX_POINT('',#65002);
#6556=VERTEX_POINT('',#65003);
#6557=VERTEX_POINT('',#65053);
#6558=VERTEX_POINT('',#65054);
#6559=VERTEX_POINT('',#65101);
#6560=VERTEX_POINT('',#65102);
#6561=VERTEX_POINT('',#65149);
#6562=VERTEX_POINT('',#65150);
#6563=VERTEX_POINT('',#65200);
#6564=VERTEX_POINT('',#65201);
#6565=VERTEX_POINT('',#65248);
#6566=VERTEX_POINT('',#65249);
#6567=VERTEX_POINT('',#65296);
#6568=VERTEX_POINT('',#65297);
#6569=VERTEX_POINT('',#65347);
#6570=VERTEX_POINT('',#65348);
#6571=VERTEX_POINT('',#65398);
#6572=VERTEX_POINT('',#65399);
#6573=VERTEX_POINT('',#65446);
#6574=VERTEX_POINT('',#65447);
#6575=VERTEX_POINT('',#65497);
#6576=VERTEX_POINT('',#65498);
#6577=VERTEX_POINT('',#65548);
#6578=VERTEX_POINT('',#65549);
#6579=VERTEX_POINT('',#65596);
#6580=VERTEX_POINT('',#65597);
#6581=VERTEX_POINT('',#65647);
#6582=VERTEX_POINT('',#65648);
#6583=VERTEX_POINT('',#65695);
#6584=VERTEX_POINT('',#65696);
#6585=VERTEX_POINT('',#65746);
#6586=VERTEX_POINT('',#65747);
#6587=VERTEX_POINT('',#65797);
#6588=VERTEX_POINT('',#65798);
#6589=VERTEX_POINT('',#65845);
#6590=VERTEX_POINT('',#65846);
#6591=VERTEX_POINT('',#65896);
#6592=VERTEX_POINT('',#65897);
#6593=VERTEX_POINT('',#65947);
#6594=VERTEX_POINT('',#65948);
#6595=VERTEX_POINT('',#65995);
#6596=VERTEX_POINT('',#65996);
#6597=VERTEX_POINT('',#66043);
#6598=VERTEX_POINT('',#66044);
#6599=VERTEX_POINT('',#66094);
#6600=VERTEX_POINT('',#66095);
#6601=VERTEX_POINT('',#66145);
#6602=VERTEX_POINT('',#66146);
#6603=VERTEX_POINT('',#66193);
#6604=VERTEX_POINT('',#66194);
#6605=VERTEX_POINT('',#66244);
#6606=VERTEX_POINT('',#66245);
#6607=VERTEX_POINT('',#66295);
#6608=VERTEX_POINT('',#66296);
#6609=VERTEX_POINT('',#66343);
#6610=VERTEX_POINT('',#66344);
#6611=VERTEX_POINT('',#66346);
#6612=VERTEX_POINT('',#66393);
#6613=VERTEX_POINT('',#66394);
#6614=VERTEX_POINT('',#66396);
#6615=VERTEX_POINT('',#66404);
#6616=VERTEX_POINT('',#66405);
#6617=VERTEX_POINT('',#66417);
#6618=VERTEX_POINT('',#66430);
#6619=VERTEX_POINT('',#66431);
#6620=VERTEX_POINT('',#66454);
#6621=VERTEX_POINT('',#66455);
#6622=VERTEX_POINT('',#66478);
#6623=VERTEX_POINT('',#66479);
#6624=VERTEX_POINT('',#66504);
#6625=VERTEX_POINT('',#66505);
#6626=VERTEX_POINT('',#66528);
#6627=VERTEX_POINT('',#66529);
#6628=VERTEX_POINT('',#66552);
#6629=VERTEX_POINT('',#66553);
#6630=VERTEX_POINT('',#66578);
#6631=VERTEX_POINT('',#66579);
#6632=VERTEX_POINT('',#66602);
#6633=VERTEX_POINT('',#66603);
#6634=VERTEX_POINT('',#66626);
#6635=VERTEX_POINT('',#66627);
#6636=VERTEX_POINT('',#66650);
#6637=VERTEX_POINT('',#66651);
#6638=VERTEX_POINT('',#66676);
#6639=VERTEX_POINT('',#66677);
#6640=VERTEX_POINT('',#66700);
#6641=VERTEX_POINT('',#66701);
#6642=VERTEX_POINT('',#66724);
#6643=VERTEX_POINT('',#66725);
#6644=VERTEX_POINT('',#66750);
#6645=VERTEX_POINT('',#66751);
#6646=VERTEX_POINT('',#66774);
#6647=VERTEX_POINT('',#66775);
#6648=VERTEX_POINT('',#66798);
#6649=VERTEX_POINT('',#66799);
#6650=VERTEX_POINT('',#66823);
#6651=VERTEX_POINT('',#66824);
#6652=VERTEX_POINT('',#66848);
#6653=VERTEX_POINT('',#66849);
#6654=VERTEX_POINT('',#66872);
#6655=VERTEX_POINT('',#66873);
#6656=VERTEX_POINT('',#66897);
#6657=VERTEX_POINT('',#66898);
#6658=VERTEX_POINT('',#66922);
#6659=VERTEX_POINT('',#66923);
#6660=VERTEX_POINT('',#66946);
#6661=VERTEX_POINT('',#66947);
#6662=VERTEX_POINT('',#66971);
#6663=VERTEX_POINT('',#66972);
#6664=VERTEX_POINT('',#66995);
#6665=VERTEX_POINT('',#66996);
#6666=VERTEX_POINT('',#67020);
#6667=VERTEX_POINT('',#67021);
#6668=VERTEX_POINT('',#67044);
#6669=VERTEX_POINT('',#67045);
#6670=VERTEX_POINT('',#67069);
#6671=VERTEX_POINT('',#67070);
#6672=VERTEX_POINT('',#67094);
#6673=VERTEX_POINT('',#67095);
#6674=VERTEX_POINT('',#67118);
#6675=VERTEX_POINT('',#67119);
#6676=VERTEX_POINT('',#67143);
#6677=VERTEX_POINT('',#67144);
#6678=VERTEX_POINT('',#67167);
#6679=VERTEX_POINT('',#67169);
#6680=VERTEX_POINT('',#67430);
#6681=VERTEX_POINT('',#68320);
#6682=VERTEX_POINT('',#68427);
#6683=VERTEX_POINT('',#69371);
#6684=VERTEX_POINT('',#69372);
#6685=VERTEX_POINT('',#69374);
#6686=VERTEX_POINT('',#69376);
#6687=VERTEX_POINT('',#69380);
#6688=VERTEX_POINT('',#69382);
#6689=VERTEX_POINT('',#69386);
#6690=VERTEX_POINT('',#69388);
#6691=VERTEX_POINT('',#69392);
#6692=VERTEX_POINT('',#69394);
#6693=VERTEX_POINT('',#69398);
#6694=VERTEX_POINT('',#69400);
#6695=VERTEX_POINT('',#69408);
#6696=VERTEX_POINT('',#69411);
#8692=EDGE_CURVE('',#6545,#6546,#4290,.T.);
#8693=EDGE_CURVE('',#6545,#6547,#3392,.T.);
#8694=EDGE_CURVE('',#6547,#6548,#2338,.F.);
#8695=EDGE_CURVE('',#6548,#6546,#3393,.T.);
#8696=EDGE_CURVE('',#6549,#6550,#4291,.T.);
#8697=EDGE_CURVE('',#6549,#6545,#3394,.T.);
#8698=EDGE_CURVE('',#6546,#6550,#3395,.T.);
#8699=EDGE_CURVE('',#6551,#6552,#4292,.T.);
#8700=EDGE_CURVE('',#6551,#6549,#3396,.T.);
#8701=EDGE_CURVE('',#6550,#6552,#3397,.T.);
#8702=EDGE_CURVE('',#6553,#6554,#4293,.T.);
#8703=EDGE_CURVE('',#6553,#6551,#3398,.T.);
#8704=EDGE_CURVE('',#6552,#6554,#3399,.T.);
#8705=EDGE_CURVE('',#6555,#6556,#4294,.T.);
#8706=EDGE_CURVE('',#6555,#6553,#3400,.T.);
#8707=EDGE_CURVE('',#6554,#6556,#3401,.T.);
#8708=EDGE_CURVE('',#6557,#6558,#4295,.T.);
#8709=EDGE_CURVE('',#6557,#6555,#3402,.T.);
#8710=EDGE_CURVE('',#6556,#6558,#3403,.T.);
#8711=EDGE_CURVE('',#6559,#6560,#4296,.T.);
#8712=EDGE_CURVE('',#6559,#6557,#3404,.T.);
#8713=EDGE_CURVE('',#6558,#6560,#3405,.T.);
#8714=EDGE_CURVE('',#6561,#6562,#4297,.T.);
#8715=EDGE_CURVE('',#6561,#6559,#3406,.T.);
#8716=EDGE_CURVE('',#6560,#6562,#3407,.T.);
#8717=EDGE_CURVE('',#6563,#6564,#4298,.T.);
#8718=EDGE_CURVE('',#6563,#6561,#3408,.T.);
#8719=EDGE_CURVE('',#6562,#6564,#3409,.T.);
#8720=EDGE_CURVE('',#6565,#6566,#4299,.T.);
#8721=EDGE_CURVE('',#6565,#6563,#3410,.T.);
#8722=EDGE_CURVE('',#6564,#6566,#3411,.T.);
#8723=EDGE_CURVE('',#6567,#6568,#4300,.T.);
#8724=EDGE_CURVE('',#6567,#6565,#3412,.T.);
#8725=EDGE_CURVE('',#6566,#6568,#3413,.T.);
#8726=EDGE_CURVE('',#6569,#6570,#4301,.T.);
#8727=EDGE_CURVE('',#6569,#6567,#3414,.T.);
#8728=EDGE_CURVE('',#6568,#6570,#3415,.T.);
#8729=EDGE_CURVE('',#6571,#6572,#4302,.T.);
#8730=EDGE_CURVE('',#6571,#6569,#3416,.T.);
#8731=EDGE_CURVE('',#6570,#6572,#3417,.T.);
#8732=EDGE_CURVE('',#6573,#6574,#4303,.T.);
#8733=EDGE_CURVE('',#6573,#6571,#3418,.T.);
#8734=EDGE_CURVE('',#6572,#6574,#3419,.T.);
#8735=EDGE_CURVE('',#6575,#6576,#4304,.T.);
#8736=EDGE_CURVE('',#6575,#6573,#3420,.T.);
#8737=EDGE_CURVE('',#6574,#6576,#3421,.T.);
#8738=EDGE_CURVE('',#6577,#6578,#4305,.T.);
#8739=EDGE_CURVE('',#6577,#6575,#3422,.T.);
#8740=EDGE_CURVE('',#6576,#6578,#3423,.T.);
#8741=EDGE_CURVE('',#6579,#6580,#4306,.T.);
#8742=EDGE_CURVE('',#6579,#6577,#3424,.T.);
#8743=EDGE_CURVE('',#6578,#6580,#3425,.T.);
#8744=EDGE_CURVE('',#6581,#6582,#4307,.T.);
#8745=EDGE_CURVE('',#6581,#6579,#3426,.T.);
#8746=EDGE_CURVE('',#6580,#6582,#3427,.T.);
#8747=EDGE_CURVE('',#6583,#6584,#4308,.T.);
#8748=EDGE_CURVE('',#6583,#6581,#3428,.T.);
#8749=EDGE_CURVE('',#6582,#6584,#3429,.T.);
#8750=EDGE_CURVE('',#6585,#6586,#4309,.T.);
#8751=EDGE_CURVE('',#6585,#6583,#3430,.T.);
#8752=EDGE_CURVE('',#6584,#6586,#3431,.T.);
#8753=EDGE_CURVE('',#6587,#6588,#4310,.T.);
#8754=EDGE_CURVE('',#6587,#6585,#3432,.T.);
#8755=EDGE_CURVE('',#6586,#6588,#3433,.T.);
#8756=EDGE_CURVE('',#6589,#6590,#4311,.T.);
#8757=EDGE_CURVE('',#6589,#6587,#3434,.T.);
#8758=EDGE_CURVE('',#6588,#6590,#3435,.T.);
#8759=EDGE_CURVE('',#6591,#6592,#4312,.T.);
#8760=EDGE_CURVE('',#6591,#6589,#3436,.T.);
#8761=EDGE_CURVE('',#6590,#6592,#3437,.T.);
#8762=EDGE_CURVE('',#6593,#6594,#4313,.T.);
#8763=EDGE_CURVE('',#6593,#6591,#3438,.T.);
#8764=EDGE_CURVE('',#6592,#6594,#3439,.T.);
#8765=EDGE_CURVE('',#6595,#6596,#4314,.T.);
#8766=EDGE_CURVE('',#6595,#6593,#3440,.T.);
#8767=EDGE_CURVE('',#6594,#6596,#3441,.T.);
#8768=EDGE_CURVE('',#6597,#6598,#4315,.T.);
#8769=EDGE_CURVE('',#6597,#6595,#3442,.T.);
#8770=EDGE_CURVE('',#6596,#6598,#3443,.T.);
#8771=EDGE_CURVE('',#6599,#6600,#4316,.T.);
#8772=EDGE_CURVE('',#6599,#6597,#3444,.T.);
#8773=EDGE_CURVE('',#6598,#6600,#3445,.T.);
#8774=EDGE_CURVE('',#6601,#6602,#4317,.T.);
#8775=EDGE_CURVE('',#6601,#6599,#3446,.T.);
#8776=EDGE_CURVE('',#6600,#6602,#3447,.T.);
#8777=EDGE_CURVE('',#6603,#6604,#4318,.T.);
#8778=EDGE_CURVE('',#6603,#6601,#3448,.T.);
#8779=EDGE_CURVE('',#6602,#6604,#3449,.T.);
#8780=EDGE_CURVE('',#6605,#6606,#4319,.T.);
#8781=EDGE_CURVE('',#6605,#6603,#3450,.T.);
#8782=EDGE_CURVE('',#6604,#6606,#3451,.T.);
#8783=EDGE_CURVE('',#6607,#6608,#4320,.T.);
#8784=EDGE_CURVE('',#6607,#6605,#3452,.T.);
#8785=EDGE_CURVE('',#6606,#6608,#3453,.T.);
#8786=EDGE_CURVE('',#6609,#6610,#4321,.T.);
#8787=EDGE_CURVE('',#6609,#6611,#2339,.T.);
#8788=EDGE_CURVE('',#6611,#6607,#3454,.T.);
#8789=EDGE_CURVE('',#6608,#6610,#3455,.T.);
#8790=EDGE_CURVE('',#6612,#6613,#4322,.T.);
#8791=EDGE_CURVE('',#6612,#6614,#3456,.T.);
#8792=EDGE_CURVE('',#6614,#6613,#2340,.T.);
#8793=EDGE_CURVE('',#6615,#6616,#4323,.T.);
#8794=EDGE_CURVE('',#6615,#6612,#3457,.T.);
#8795=EDGE_CURVE('',#6613,#6617,#2341,.T.);
#8796=EDGE_CURVE('',#6616,#6617,#3458,.T.);
#8797=EDGE_CURVE('',#6618,#6619,#4324,.T.);
#8798=EDGE_CURVE('',#6618,#6615,#3459,.T.);
#8799=EDGE_CURVE('',#6619,#6616,#3460,.T.);
#8800=EDGE_CURVE('',#6620,#6621,#4325,.T.);
#8801=EDGE_CURVE('',#6620,#6618,#3461,.T.);
#8802=EDGE_CURVE('',#6621,#6619,#3462,.T.);
#8803=EDGE_CURVE('',#6622,#6623,#4326,.T.);
#8804=EDGE_CURVE('',#6622,#6620,#3463,.T.);
#8805=EDGE_CURVE('',#6623,#6621,#3464,.T.);
#8806=EDGE_CURVE('',#6624,#6625,#4327,.T.);
#8807=EDGE_CURVE('',#6624,#6622,#3465,.T.);
#8808=EDGE_CURVE('',#6625,#6623,#3466,.T.);
#8809=EDGE_CURVE('',#6626,#6627,#4328,.T.);
#8810=EDGE_CURVE('',#6626,#6624,#3467,.T.);
#8811=EDGE_CURVE('',#6627,#6625,#3468,.T.);
#8812=EDGE_CURVE('',#6628,#6629,#4329,.T.);
#8813=EDGE_CURVE('',#6628,#6626,#3469,.T.);
#8814=EDGE_CURVE('',#6629,#6627,#3470,.T.);
#8815=EDGE_CURVE('',#6630,#6631,#4330,.T.);
#8816=EDGE_CURVE('',#6630,#6628,#3471,.T.);
#8817=EDGE_CURVE('',#6631,#6629,#3472,.T.);
#8818=EDGE_CURVE('',#6632,#6633,#4331,.T.);
#8819=EDGE_CURVE('',#6632,#6630,#3473,.T.);
#8820=EDGE_CURVE('',#6633,#6631,#3474,.T.);
#8821=EDGE_CURVE('',#6634,#6635,#4332,.T.);
#8822=EDGE_CURVE('',#6634,#6632,#3475,.T.);
#8823=EDGE_CURVE('',#6635,#6633,#3476,.T.);
#8824=EDGE_CURVE('',#6636,#6637,#4333,.T.);
#8825=EDGE_CURVE('',#6636,#6634,#3477,.T.);
#8826=EDGE_CURVE('',#6637,#6635,#3478,.T.);
#8827=EDGE_CURVE('',#6638,#6639,#4334,.T.);
#8828=EDGE_CURVE('',#6638,#6636,#3479,.T.);
#8829=EDGE_CURVE('',#6639,#6637,#3480,.T.);
#8830=EDGE_CURVE('',#6640,#6641,#4335,.T.);
#8831=EDGE_CURVE('',#6640,#6638,#3481,.T.);
#8832=EDGE_CURVE('',#6641,#6639,#3482,.T.);
#8833=EDGE_CURVE('',#6642,#6643,#4336,.T.);
#8834=EDGE_CURVE('',#6642,#6640,#3483,.T.);
#8835=EDGE_CURVE('',#6643,#6641,#3484,.T.);
#8836=EDGE_CURVE('',#6644,#6645,#4337,.T.);
#8837=EDGE_CURVE('',#6644,#6642,#3485,.T.);
#8838=EDGE_CURVE('',#6645,#6643,#3486,.T.);
#8839=EDGE_CURVE('',#6646,#6647,#4338,.T.);
#8840=EDGE_CURVE('',#6646,#6644,#3487,.T.);
#8841=EDGE_CURVE('',#6647,#6645,#3488,.T.);
#8842=EDGE_CURVE('',#6648,#6649,#4339,.T.);
#8843=EDGE_CURVE('',#6648,#6646,#3489,.T.);
#8844=EDGE_CURVE('',#6649,#6647,#3490,.T.);
#8845=EDGE_CURVE('',#6650,#6651,#4340,.T.);
#8846=EDGE_CURVE('',#6650,#6648,#3491,.T.);
#8847=EDGE_CURVE('',#6651,#6649,#3492,.T.);
#8848=EDGE_CURVE('',#6652,#6653,#4341,.T.);
#8849=EDGE_CURVE('',#6652,#6650,#3493,.T.);
#8850=EDGE_CURVE('',#6653,#6651,#3494,.T.);
#8851=EDGE_CURVE('',#6654,#6655,#4342,.T.);
#8852=EDGE_CURVE('',#6654,#6652,#3495,.T.);
#8853=EDGE_CURVE('',#6655,#6653,#3496,.T.);
#8854=EDGE_CURVE('',#6656,#6657,#4343,.T.);
#8855=EDGE_CURVE('',#6656,#6654,#3497,.T.);
#8856=EDGE_CURVE('',#6657,#6655,#3498,.T.);
#8857=EDGE_CURVE('',#6658,#6659,#4344,.T.);
#8858=EDGE_CURVE('',#6658,#6656,#3499,.T.);
#8859=EDGE_CURVE('',#6659,#6657,#3500,.T.);
#8860=EDGE_CURVE('',#6660,#6661,#4345,.T.);
#8861=EDGE_CURVE('',#6660,#6658,#3501,.T.);
#8862=EDGE_CURVE('',#6661,#6659,#3502,.T.);
#8863=EDGE_CURVE('',#6662,#6663,#4346,.T.);
#8864=EDGE_CURVE('',#6662,#6660,#3503,.T.);
#8865=EDGE_CURVE('',#6663,#6661,#3504,.T.);
#8866=EDGE_CURVE('',#6664,#6665,#4347,.T.);
#8867=EDGE_CURVE('',#6664,#6662,#3505,.T.);
#8868=EDGE_CURVE('',#6665,#6663,#3506,.T.);
#8869=EDGE_CURVE('',#6666,#6667,#4348,.T.);
#8870=EDGE_CURVE('',#6666,#6664,#3507,.T.);
#8871=EDGE_CURVE('',#6667,#6665,#3508,.T.);
#8872=EDGE_CURVE('',#6668,#6669,#4349,.T.);
#8873=EDGE_CURVE('',#6668,#6666,#3509,.T.);
#8874=EDGE_CURVE('',#6669,#6667,#3510,.T.);
#8875=EDGE_CURVE('',#6670,#6671,#4350,.T.);
#8876=EDGE_CURVE('',#6670,#6668,#3511,.T.);
#8877=EDGE_CURVE('',#6671,#6669,#3512,.T.);
#8878=EDGE_CURVE('',#6672,#6673,#4351,.T.);
#8879=EDGE_CURVE('',#6672,#6670,#3513,.T.);
#8880=EDGE_CURVE('',#6673,#6671,#3514,.T.);
#8881=EDGE_CURVE('',#6674,#6675,#4352,.T.);
#8882=EDGE_CURVE('',#6674,#6672,#3515,.T.);
#8883=EDGE_CURVE('',#6675,#6673,#3516,.T.);
#8884=EDGE_CURVE('',#6676,#6677,#4353,.T.);
#8885=EDGE_CURVE('',#6676,#6674,#3517,.T.);
#8886=EDGE_CURVE('',#6677,#6675,#3518,.T.);
#8887=EDGE_CURVE('',#6609,#6678,#4354,.T.);
#8888=EDGE_CURVE('',#6679,#6609,#2342,.T.);
#8889=EDGE_CURVE('',#6617,#6679,#3519,.T.);
#8890=EDGE_CURVE('',#6613,#6680,#4355,.T.);
#8891=EDGE_CURVE('',#6680,#6680,#2343,.T.);
#8892=EDGE_CURVE('',#6678,#6614,#3520,.T.);
#8893=EDGE_CURVE('',#6611,#6678,#3521,.T.);
#8894=EDGE_CURVE('',#6681,#6676,#3522,.T.);
#8895=EDGE_CURVE('',#6547,#6681,#3523,.T.);
#8896=EDGE_CURVE('',#6682,#6677,#3524,.T.);
#8897=EDGE_CURVE('',#6681,#6682,#2344,.T.);
#8898=EDGE_CURVE('',#6610,#6679,#3525,.T.);
#8899=EDGE_CURVE('',#6682,#6548,#3526,.T.);
#8900=EDGE_CURVE('',#6683,#6684,#4356,.T.);
#8901=EDGE_CURVE('',#6683,#6685,#4357,.T.);
#8902=EDGE_CURVE('',#6685,#6686,#4358,.T.);
#8903=EDGE_CURVE('',#6684,#6686,#4359,.T.);
#8904=EDGE_CURVE('',#6687,#6683,#4360,.T.);
#8905=EDGE_CURVE('',#6687,#6688,#4361,.T.);
#8906=EDGE_CURVE('',#6688,#6685,#4362,.T.);
#8907=EDGE_CURVE('',#6689,#6687,#4363,.T.);
#8908=EDGE_CURVE('',#6689,#6690,#4364,.T.);
#8909=EDGE_CURVE('',#6690,#6688,#4365,.T.);
#8910=EDGE_CURVE('',#6691,#6689,#4366,.T.);
#8911=EDGE_CURVE('',#6691,#6692,#4367,.T.);
#8912=EDGE_CURVE('',#6692,#6690,#4368,.T.);
#8913=EDGE_CURVE('',#6693,#6691,#4369,.T.);
#8914=EDGE_CURVE('',#6693,#6694,#4370,.T.);
#8915=EDGE_CURVE('',#6694,#6692,#4371,.T.);
#8916=EDGE_CURVE('',#6684,#6693,#4372,.T.);
#8917=EDGE_CURVE('',#6686,#6694,#4373,.T.);
#8918=EDGE_CURVE('',#6695,#6695,#2345,.T.);
#8919=EDGE_CURVE('',#6695,#6696,#4374,.T.);
#8920=EDGE_CURVE('',#6696,#6696,#2346,.T.);
#12911=ORIENTED_EDGE('',*,*,#8692,.F.);
#12912=ORIENTED_EDGE('',*,*,#8693,.T.);
#12913=ORIENTED_EDGE('',*,*,#8694,.T.);
#12914=ORIENTED_EDGE('',*,*,#8695,.T.);
#12915=ORIENTED_EDGE('',*,*,#8696,.F.);
#12916=ORIENTED_EDGE('',*,*,#8697,.T.);
#12917=ORIENTED_EDGE('',*,*,#8692,.T.);
#12918=ORIENTED_EDGE('',*,*,#8698,.T.);
#12919=ORIENTED_EDGE('',*,*,#8699,.F.);
#12920=ORIENTED_EDGE('',*,*,#8700,.T.);
#12921=ORIENTED_EDGE('',*,*,#8696,.T.);
#12922=ORIENTED_EDGE('',*,*,#8701,.T.);
#12923=ORIENTED_EDGE('',*,*,#8702,.F.);
#12924=ORIENTED_EDGE('',*,*,#8703,.T.);
#12925=ORIENTED_EDGE('',*,*,#8699,.T.);
#12926=ORIENTED_EDGE('',*,*,#8704,.T.);
#12927=ORIENTED_EDGE('',*,*,#8705,.F.);
#12928=ORIENTED_EDGE('',*,*,#8706,.T.);
#12929=ORIENTED_EDGE('',*,*,#8702,.T.);
#12930=ORIENTED_EDGE('',*,*,#8707,.T.);
#12931=ORIENTED_EDGE('',*,*,#8708,.F.);
#12932=ORIENTED_EDGE('',*,*,#8709,.T.);
#12933=ORIENTED_EDGE('',*,*,#8705,.T.);
#12934=ORIENTED_EDGE('',*,*,#8710,.T.);
#12935=ORIENTED_EDGE('',*,*,#8711,.F.);
#12936=ORIENTED_EDGE('',*,*,#8712,.T.);
#12937=ORIENTED_EDGE('',*,*,#8708,.T.);
#12938=ORIENTED_EDGE('',*,*,#8713,.T.);
#12939=ORIENTED_EDGE('',*,*,#8714,.F.);
#12940=ORIENTED_EDGE('',*,*,#8715,.T.);
#12941=ORIENTED_EDGE('',*,*,#8711,.T.);
#12942=ORIENTED_EDGE('',*,*,#8716,.T.);
#12943=ORIENTED_EDGE('',*,*,#8717,.F.);
#12944=ORIENTED_EDGE('',*,*,#8718,.T.);
#12945=ORIENTED_EDGE('',*,*,#8714,.T.);
#12946=ORIENTED_EDGE('',*,*,#8719,.T.);
#12947=ORIENTED_EDGE('',*,*,#8720,.F.);
#12948=ORIENTED_EDGE('',*,*,#8721,.T.);
#12949=ORIENTED_EDGE('',*,*,#8717,.T.);
#12950=ORIENTED_EDGE('',*,*,#8722,.T.);
#12951=ORIENTED_EDGE('',*,*,#8723,.F.);
#12952=ORIENTED_EDGE('',*,*,#8724,.T.);
#12953=ORIENTED_EDGE('',*,*,#8720,.T.);
#12954=ORIENTED_EDGE('',*,*,#8725,.T.);
#12955=ORIENTED_EDGE('',*,*,#8726,.F.);
#12956=ORIENTED_EDGE('',*,*,#8727,.T.);
#12957=ORIENTED_EDGE('',*,*,#8723,.T.);
#12958=ORIENTED_EDGE('',*,*,#8728,.T.);
#12959=ORIENTED_EDGE('',*,*,#8729,.F.);
#12960=ORIENTED_EDGE('',*,*,#8730,.T.);
#12961=ORIENTED_EDGE('',*,*,#8726,.T.);
#12962=ORIENTED_EDGE('',*,*,#8731,.T.);
#12963=ORIENTED_EDGE('',*,*,#8732,.F.);
#12964=ORIENTED_EDGE('',*,*,#8733,.T.);
#12965=ORIENTED_EDGE('',*,*,#8729,.T.);
#12966=ORIENTED_EDGE('',*,*,#8734,.T.);
#12967=ORIENTED_EDGE('',*,*,#8735,.F.);
#12968=ORIENTED_EDGE('',*,*,#8736,.T.);
#12969=ORIENTED_EDGE('',*,*,#8732,.T.);
#12970=ORIENTED_EDGE('',*,*,#8737,.T.);
#12971=ORIENTED_EDGE('',*,*,#8738,.F.);
#12972=ORIENTED_EDGE('',*,*,#8739,.T.);
#12973=ORIENTED_EDGE('',*,*,#8735,.T.);
#12974=ORIENTED_EDGE('',*,*,#8740,.T.);
#12975=ORIENTED_EDGE('',*,*,#8741,.F.);
#12976=ORIENTED_EDGE('',*,*,#8742,.T.);
#12977=ORIENTED_EDGE('',*,*,#8738,.T.);
#12978=ORIENTED_EDGE('',*,*,#8743,.T.);
#12979=ORIENTED_EDGE('',*,*,#8744,.F.);
#12980=ORIENTED_EDGE('',*,*,#8745,.T.);
#12981=ORIENTED_EDGE('',*,*,#8741,.T.);
#12982=ORIENTED_EDGE('',*,*,#8746,.T.);
#12983=ORIENTED_EDGE('',*,*,#8747,.F.);
#12984=ORIENTED_EDGE('',*,*,#8748,.T.);
#12985=ORIENTED_EDGE('',*,*,#8744,.T.);
#12986=ORIENTED_EDGE('',*,*,#8749,.T.);
#12987=ORIENTED_EDGE('',*,*,#8750,.F.);
#12988=ORIENTED_EDGE('',*,*,#8751,.T.);
#12989=ORIENTED_EDGE('',*,*,#8747,.T.);
#12990=ORIENTED_EDGE('',*,*,#8752,.T.);
#12991=ORIENTED_EDGE('',*,*,#8753,.F.);
#12992=ORIENTED_EDGE('',*,*,#8754,.T.);
#12993=ORIENTED_EDGE('',*,*,#8750,.T.);
#12994=ORIENTED_EDGE('',*,*,#8755,.T.);
#12995=ORIENTED_EDGE('',*,*,#8756,.F.);
#12996=ORIENTED_EDGE('',*,*,#8757,.T.);
#12997=ORIENTED_EDGE('',*,*,#8753,.T.);
#12998=ORIENTED_EDGE('',*,*,#8758,.T.);
#12999=ORIENTED_EDGE('',*,*,#8759,.F.);
#13000=ORIENTED_EDGE('',*,*,#8760,.T.);
#13001=ORIENTED_EDGE('',*,*,#8756,.T.);
#13002=ORIENTED_EDGE('',*,*,#8761,.T.);
#13003=ORIENTED_EDGE('',*,*,#8762,.F.);
#13004=ORIENTED_EDGE('',*,*,#8763,.T.);
#13005=ORIENTED_EDGE('',*,*,#8759,.T.);
#13006=ORIENTED_EDGE('',*,*,#8764,.T.);
#13007=ORIENTED_EDGE('',*,*,#8765,.F.);
#13008=ORIENTED_EDGE('',*,*,#8766,.T.);
#13009=ORIENTED_EDGE('',*,*,#8762,.T.);
#13010=ORIENTED_EDGE('',*,*,#8767,.T.);
#13011=ORIENTED_EDGE('',*,*,#8768,.F.);
#13012=ORIENTED_EDGE('',*,*,#8769,.T.);
#13013=ORIENTED_EDGE('',*,*,#8765,.T.);
#13014=ORIENTED_EDGE('',*,*,#8770,.T.);
#13015=ORIENTED_EDGE('',*,*,#8771,.F.);
#13016=ORIENTED_EDGE('',*,*,#8772,.T.);
#13017=ORIENTED_EDGE('',*,*,#8768,.T.);
#13018=ORIENTED_EDGE('',*,*,#8773,.T.);
#13019=ORIENTED_EDGE('',*,*,#8774,.F.);
#13020=ORIENTED_EDGE('',*,*,#8775,.T.);
#13021=ORIENTED_EDGE('',*,*,#8771,.T.);
#13022=ORIENTED_EDGE('',*,*,#8776,.T.);
#13023=ORIENTED_EDGE('',*,*,#8777,.F.);
#13024=ORIENTED_EDGE('',*,*,#8778,.T.);
#13025=ORIENTED_EDGE('',*,*,#8774,.T.);
#13026=ORIENTED_EDGE('',*,*,#8779,.T.);
#13027=ORIENTED_EDGE('',*,*,#8780,.F.);
#13028=ORIENTED_EDGE('',*,*,#8781,.T.);
#13029=ORIENTED_EDGE('',*,*,#8777,.T.);
#13030=ORIENTED_EDGE('',*,*,#8782,.T.);
#13031=ORIENTED_EDGE('',*,*,#8783,.F.);
#13032=ORIENTED_EDGE('',*,*,#8784,.T.);
#13033=ORIENTED_EDGE('',*,*,#8780,.T.);
#13034=ORIENTED_EDGE('',*,*,#8785,.T.);
#13035=ORIENTED_EDGE('',*,*,#8786,.F.);
#13036=ORIENTED_EDGE('',*,*,#8787,.T.);
#13037=ORIENTED_EDGE('',*,*,#8788,.T.);
#13038=ORIENTED_EDGE('',*,*,#8783,.T.);
#13039=ORIENTED_EDGE('',*,*,#8789,.T.);
#13040=ORIENTED_EDGE('',*,*,#8790,.F.);
#13041=ORIENTED_EDGE('',*,*,#8791,.T.);
#13042=ORIENTED_EDGE('',*,*,#8792,.T.);
#13043=ORIENTED_EDGE('',*,*,#8793,.F.);
#13044=ORIENTED_EDGE('',*,*,#8794,.T.);
#13045=ORIENTED_EDGE('',*,*,#8790,.T.);
#13046=ORIENTED_EDGE('',*,*,#8795,.T.);
#13047=ORIENTED_EDGE('',*,*,#8796,.F.);
#13048=ORIENTED_EDGE('',*,*,#8797,.F.);
#13049=ORIENTED_EDGE('',*,*,#8798,.T.);
#13050=ORIENTED_EDGE('',*,*,#8793,.T.);
#13051=ORIENTED_EDGE('',*,*,#8799,.F.);
#13052=ORIENTED_EDGE('',*,*,#8800,.F.);
#13053=ORIENTED_EDGE('',*,*,#8801,.T.);
#13054=ORIENTED_EDGE('',*,*,#8797,.T.);
#13055=ORIENTED_EDGE('',*,*,#8802,.F.);
#13056=ORIENTED_EDGE('',*,*,#8803,.F.);
#13057=ORIENTED_EDGE('',*,*,#8804,.T.);
#13058=ORIENTED_EDGE('',*,*,#8800,.T.);
#13059=ORIENTED_EDGE('',*,*,#8805,.F.);
#13060=ORIENTED_EDGE('',*,*,#8806,.F.);
#13061=ORIENTED_EDGE('',*,*,#8807,.T.);
#13062=ORIENTED_EDGE('',*,*,#8803,.T.);
#13063=ORIENTED_EDGE('',*,*,#8808,.F.);
#13064=ORIENTED_EDGE('',*,*,#8809,.F.);
#13065=ORIENTED_EDGE('',*,*,#8810,.T.);
#13066=ORIENTED_EDGE('',*,*,#8806,.T.);
#13067=ORIENTED_EDGE('',*,*,#8811,.F.);
#13068=ORIENTED_EDGE('',*,*,#8812,.F.);
#13069=ORIENTED_EDGE('',*,*,#8813,.T.);
#13070=ORIENTED_EDGE('',*,*,#8809,.T.);
#13071=ORIENTED_EDGE('',*,*,#8814,.F.);
#13072=ORIENTED_EDGE('',*,*,#8815,.F.);
#13073=ORIENTED_EDGE('',*,*,#8816,.T.);
#13074=ORIENTED_EDGE('',*,*,#8812,.T.);
#13075=ORIENTED_EDGE('',*,*,#8817,.F.);
#13076=ORIENTED_EDGE('',*,*,#8818,.F.);
#13077=ORIENTED_EDGE('',*,*,#8819,.T.);
#13078=ORIENTED_EDGE('',*,*,#8815,.T.);
#13079=ORIENTED_EDGE('',*,*,#8820,.F.);
#13080=ORIENTED_EDGE('',*,*,#8821,.F.);
#13081=ORIENTED_EDGE('',*,*,#8822,.T.);
#13082=ORIENTED_EDGE('',*,*,#8818,.T.);
#13083=ORIENTED_EDGE('',*,*,#8823,.F.);
#13084=ORIENTED_EDGE('',*,*,#8824,.F.);
#13085=ORIENTED_EDGE('',*,*,#8825,.T.);
#13086=ORIENTED_EDGE('',*,*,#8821,.T.);
#13087=ORIENTED_EDGE('',*,*,#8826,.F.);
#13088=ORIENTED_EDGE('',*,*,#8827,.F.);
#13089=ORIENTED_EDGE('',*,*,#8828,.T.);
#13090=ORIENTED_EDGE('',*,*,#8824,.T.);
#13091=ORIENTED_EDGE('',*,*,#8829,.F.);
#13092=ORIENTED_EDGE('',*,*,#8830,.F.);
#13093=ORIENTED_EDGE('',*,*,#8831,.T.);
#13094=ORIENTED_EDGE('',*,*,#8827,.T.);
#13095=ORIENTED_EDGE('',*,*,#8832,.F.);
#13096=ORIENTED_EDGE('',*,*,#8833,.F.);
#13097=ORIENTED_EDGE('',*,*,#8834,.T.);
#13098=ORIENTED_EDGE('',*,*,#8830,.T.);
#13099=ORIENTED_EDGE('',*,*,#8835,.F.);
#13100=ORIENTED_EDGE('',*,*,#8836,.F.);
#13101=ORIENTED_EDGE('',*,*,#8837,.T.);
#13102=ORIENTED_EDGE('',*,*,#8833,.T.);
#13103=ORIENTED_EDGE('',*,*,#8838,.F.);
#13104=ORIENTED_EDGE('',*,*,#8839,.F.);
#13105=ORIENTED_EDGE('',*,*,#8840,.T.);
#13106=ORIENTED_EDGE('',*,*,#8836,.T.);
#13107=ORIENTED_EDGE('',*,*,#8841,.F.);
#13108=ORIENTED_EDGE('',*,*,#8842,.F.);
#13109=ORIENTED_EDGE('',*,*,#8843,.T.);
#13110=ORIENTED_EDGE('',*,*,#8839,.T.);
#13111=ORIENTED_EDGE('',*,*,#8844,.F.);
#13112=ORIENTED_EDGE('',*,*,#8845,.F.);
#13113=ORIENTED_EDGE('',*,*,#8846,.T.);
#13114=ORIENTED_EDGE('',*,*,#8842,.T.);
#13115=ORIENTED_EDGE('',*,*,#8847,.F.);
#13116=ORIENTED_EDGE('',*,*,#8848,.F.);
#13117=ORIENTED_EDGE('',*,*,#8849,.T.);
#13118=ORIENTED_EDGE('',*,*,#8845,.T.);
#13119=ORIENTED_EDGE('',*,*,#8850,.F.);
#13120=ORIENTED_EDGE('',*,*,#8851,.F.);
#13121=ORIENTED_EDGE('',*,*,#8852,.T.);
#13122=ORIENTED_EDGE('',*,*,#8848,.T.);
#13123=ORIENTED_EDGE('',*,*,#8853,.F.);
#13124=ORIENTED_EDGE('',*,*,#8854,.F.);
#13125=ORIENTED_EDGE('',*,*,#8855,.T.);
#13126=ORIENTED_EDGE('',*,*,#8851,.T.);
#13127=ORIENTED_EDGE('',*,*,#8856,.F.);
#13128=ORIENTED_EDGE('',*,*,#8857,.F.);
#13129=ORIENTED_EDGE('',*,*,#8858,.T.);
#13130=ORIENTED_EDGE('',*,*,#8854,.T.);
#13131=ORIENTED_EDGE('',*,*,#8859,.F.);
#13132=ORIENTED_EDGE('',*,*,#8860,.F.);
#13133=ORIENTED_EDGE('',*,*,#8861,.T.);
#13134=ORIENTED_EDGE('',*,*,#8857,.T.);
#13135=ORIENTED_EDGE('',*,*,#8862,.F.);
#13136=ORIENTED_EDGE('',*,*,#8863,.F.);
#13137=ORIENTED_EDGE('',*,*,#8864,.T.);
#13138=ORIENTED_EDGE('',*,*,#8860,.T.);
#13139=ORIENTED_EDGE('',*,*,#8865,.F.);
#13140=ORIENTED_EDGE('',*,*,#8866,.F.);
#13141=ORIENTED_EDGE('',*,*,#8867,.T.);
#13142=ORIENTED_EDGE('',*,*,#8863,.T.);
#13143=ORIENTED_EDGE('',*,*,#8868,.F.);
#13144=ORIENTED_EDGE('',*,*,#8869,.F.);
#13145=ORIENTED_EDGE('',*,*,#8870,.T.);
#13146=ORIENTED_EDGE('',*,*,#8866,.T.);
#13147=ORIENTED_EDGE('',*,*,#8871,.F.);
#13148=ORIENTED_EDGE('',*,*,#8872,.F.);
#13149=ORIENTED_EDGE('',*,*,#8873,.T.);
#13150=ORIENTED_EDGE('',*,*,#8869,.T.);
#13151=ORIENTED_EDGE('',*,*,#8874,.F.);
#13152=ORIENTED_EDGE('',*,*,#8875,.F.);
#13153=ORIENTED_EDGE('',*,*,#8876,.T.);
#13154=ORIENTED_EDGE('',*,*,#8872,.T.);
#13155=ORIENTED_EDGE('',*,*,#8877,.F.);
#13156=ORIENTED_EDGE('',*,*,#8878,.F.);
#13157=ORIENTED_EDGE('',*,*,#8879,.T.);
#13158=ORIENTED_EDGE('',*,*,#8875,.T.);
#13159=ORIENTED_EDGE('',*,*,#8880,.F.);
#13160=ORIENTED_EDGE('',*,*,#8881,.F.);
#13161=ORIENTED_EDGE('',*,*,#8882,.T.);
#13162=ORIENTED_EDGE('',*,*,#8878,.T.);
#13163=ORIENTED_EDGE('',*,*,#8883,.F.);
#13164=ORIENTED_EDGE('',*,*,#8884,.F.);
#13165=ORIENTED_EDGE('',*,*,#8885,.T.);
#13166=ORIENTED_EDGE('',*,*,#8881,.T.);
#13167=ORIENTED_EDGE('',*,*,#8886,.F.);
#13168=ORIENTED_EDGE('',*,*,#8887,.F.);
#13169=ORIENTED_EDGE('',*,*,#8888,.F.);
#13170=ORIENTED_EDGE('',*,*,#8889,.F.);
#13171=ORIENTED_EDGE('',*,*,#8795,.F.);
#13172=ORIENTED_EDGE('',*,*,#8890,.T.);
#13173=ORIENTED_EDGE('',*,*,#8891,.F.);
#13174=ORIENTED_EDGE('',*,*,#8890,.F.);
#13175=ORIENTED_EDGE('',*,*,#8792,.F.);
#13176=ORIENTED_EDGE('',*,*,#8892,.F.);
#13177=ORIENTED_EDGE('',*,*,#8887,.T.);
#13178=ORIENTED_EDGE('',*,*,#8893,.F.);
#13179=ORIENTED_EDGE('',*,*,#8787,.F.);
#13180=ORIENTED_EDGE('',*,*,#8893,.T.);
#13181=ORIENTED_EDGE('',*,*,#8892,.T.);
#13182=ORIENTED_EDGE('',*,*,#8791,.F.);
#13183=ORIENTED_EDGE('',*,*,#8794,.F.);
#13184=ORIENTED_EDGE('',*,*,#8798,.F.);
#13185=ORIENTED_EDGE('',*,*,#8801,.F.);
#13186=ORIENTED_EDGE('',*,*,#8804,.F.);
#13187=ORIENTED_EDGE('',*,*,#8807,.F.);
#13188=ORIENTED_EDGE('',*,*,#8810,.F.);
#13189=ORIENTED_EDGE('',*,*,#8813,.F.);
#13190=ORIENTED_EDGE('',*,*,#8816,.F.);
#13191=ORIENTED_EDGE('',*,*,#8819,.F.);
#13192=ORIENTED_EDGE('',*,*,#8822,.F.);
#13193=ORIENTED_EDGE('',*,*,#8825,.F.);
#13194=ORIENTED_EDGE('',*,*,#8828,.F.);
#13195=ORIENTED_EDGE('',*,*,#8831,.F.);
#13196=ORIENTED_EDGE('',*,*,#8834,.F.);
#13197=ORIENTED_EDGE('',*,*,#8837,.F.);
#13198=ORIENTED_EDGE('',*,*,#8840,.F.);
#13199=ORIENTED_EDGE('',*,*,#8843,.F.);
#13200=ORIENTED_EDGE('',*,*,#8846,.F.);
#13201=ORIENTED_EDGE('',*,*,#8849,.F.);
#13202=ORIENTED_EDGE('',*,*,#8852,.F.);
#13203=ORIENTED_EDGE('',*,*,#8855,.F.);
#13204=ORIENTED_EDGE('',*,*,#8858,.F.);
#13205=ORIENTED_EDGE('',*,*,#8861,.F.);
#13206=ORIENTED_EDGE('',*,*,#8864,.F.);
#13207=ORIENTED_EDGE('',*,*,#8867,.F.);
#13208=ORIENTED_EDGE('',*,*,#8870,.F.);
#13209=ORIENTED_EDGE('',*,*,#8873,.F.);
#13210=ORIENTED_EDGE('',*,*,#8876,.F.);
#13211=ORIENTED_EDGE('',*,*,#8879,.F.);
#13212=ORIENTED_EDGE('',*,*,#8882,.F.);
#13213=ORIENTED_EDGE('',*,*,#8885,.F.);
#13214=ORIENTED_EDGE('',*,*,#8894,.F.);
#13215=ORIENTED_EDGE('',*,*,#8895,.F.);
#13216=ORIENTED_EDGE('',*,*,#8693,.F.);
#13217=ORIENTED_EDGE('',*,*,#8697,.F.);
#13218=ORIENTED_EDGE('',*,*,#8700,.F.);
#13219=ORIENTED_EDGE('',*,*,#8703,.F.);
#13220=ORIENTED_EDGE('',*,*,#8706,.F.);
#13221=ORIENTED_EDGE('',*,*,#8709,.F.);
#13222=ORIENTED_EDGE('',*,*,#8712,.F.);
#13223=ORIENTED_EDGE('',*,*,#8715,.F.);
#13224=ORIENTED_EDGE('',*,*,#8718,.F.);
#13225=ORIENTED_EDGE('',*,*,#8721,.F.);
#13226=ORIENTED_EDGE('',*,*,#8724,.F.);
#13227=ORIENTED_EDGE('',*,*,#8727,.F.);
#13228=ORIENTED_EDGE('',*,*,#8730,.F.);
#13229=ORIENTED_EDGE('',*,*,#8733,.F.);
#13230=ORIENTED_EDGE('',*,*,#8736,.F.);
#13231=ORIENTED_EDGE('',*,*,#8739,.F.);
#13232=ORIENTED_EDGE('',*,*,#8742,.F.);
#13233=ORIENTED_EDGE('',*,*,#8745,.F.);
#13234=ORIENTED_EDGE('',*,*,#8748,.F.);
#13235=ORIENTED_EDGE('',*,*,#8751,.F.);
#13236=ORIENTED_EDGE('',*,*,#8754,.F.);
#13237=ORIENTED_EDGE('',*,*,#8757,.F.);
#13238=ORIENTED_EDGE('',*,*,#8760,.F.);
#13239=ORIENTED_EDGE('',*,*,#8763,.F.);
#13240=ORIENTED_EDGE('',*,*,#8766,.F.);
#13241=ORIENTED_EDGE('',*,*,#8769,.F.);
#13242=ORIENTED_EDGE('',*,*,#8772,.F.);
#13243=ORIENTED_EDGE('',*,*,#8775,.F.);
#13244=ORIENTED_EDGE('',*,*,#8778,.F.);
#13245=ORIENTED_EDGE('',*,*,#8781,.F.);
#13246=ORIENTED_EDGE('',*,*,#8784,.F.);
#13247=ORIENTED_EDGE('',*,*,#8788,.F.);
#13248=ORIENTED_EDGE('',*,*,#8884,.T.);
#13249=ORIENTED_EDGE('',*,*,#8896,.F.);
#13250=ORIENTED_EDGE('',*,*,#8897,.F.);
#13251=ORIENTED_EDGE('',*,*,#8894,.T.);
#13252=ORIENTED_EDGE('',*,*,#8889,.T.);
#13253=ORIENTED_EDGE('',*,*,#8898,.F.);
#13254=ORIENTED_EDGE('',*,*,#8789,.F.);
#13255=ORIENTED_EDGE('',*,*,#8785,.F.);
#13256=ORIENTED_EDGE('',*,*,#8782,.F.);
#13257=ORIENTED_EDGE('',*,*,#8779,.F.);
#13258=ORIENTED_EDGE('',*,*,#8776,.F.);
#13259=ORIENTED_EDGE('',*,*,#8773,.F.);
#13260=ORIENTED_EDGE('',*,*,#8770,.F.);
#13261=ORIENTED_EDGE('',*,*,#8767,.F.);
#13262=ORIENTED_EDGE('',*,*,#8764,.F.);
#13263=ORIENTED_EDGE('',*,*,#8761,.F.);
#13264=ORIENTED_EDGE('',*,*,#8758,.F.);
#13265=ORIENTED_EDGE('',*,*,#8755,.F.);
#13266=ORIENTED_EDGE('',*,*,#8752,.F.);
#13267=ORIENTED_EDGE('',*,*,#8749,.F.);
#13268=ORIENTED_EDGE('',*,*,#8746,.F.);
#13269=ORIENTED_EDGE('',*,*,#8743,.F.);
#13270=ORIENTED_EDGE('',*,*,#8740,.F.);
#13271=ORIENTED_EDGE('',*,*,#8737,.F.);
#13272=ORIENTED_EDGE('',*,*,#8734,.F.);
#13273=ORIENTED_EDGE('',*,*,#8731,.F.);
#13274=ORIENTED_EDGE('',*,*,#8728,.F.);
#13275=ORIENTED_EDGE('',*,*,#8725,.F.);
#13276=ORIENTED_EDGE('',*,*,#8722,.F.);
#13277=ORIENTED_EDGE('',*,*,#8719,.F.);
#13278=ORIENTED_EDGE('',*,*,#8716,.F.);
#13279=ORIENTED_EDGE('',*,*,#8713,.F.);
#13280=ORIENTED_EDGE('',*,*,#8710,.F.);
#13281=ORIENTED_EDGE('',*,*,#8707,.F.);
#13282=ORIENTED_EDGE('',*,*,#8704,.F.);
#13283=ORIENTED_EDGE('',*,*,#8701,.F.);
#13284=ORIENTED_EDGE('',*,*,#8698,.F.);
#13285=ORIENTED_EDGE('',*,*,#8695,.F.);
#13286=ORIENTED_EDGE('',*,*,#8899,.F.);
#13287=ORIENTED_EDGE('',*,*,#8896,.T.);
#13288=ORIENTED_EDGE('',*,*,#8886,.T.);
#13289=ORIENTED_EDGE('',*,*,#8883,.T.);
#13290=ORIENTED_EDGE('',*,*,#8880,.T.);
#13291=ORIENTED_EDGE('',*,*,#8877,.T.);
#13292=ORIENTED_EDGE('',*,*,#8874,.T.);
#13293=ORIENTED_EDGE('',*,*,#8871,.T.);
#13294=ORIENTED_EDGE('',*,*,#8868,.T.);
#13295=ORIENTED_EDGE('',*,*,#8865,.T.);
#13296=ORIENTED_EDGE('',*,*,#8862,.T.);
#13297=ORIENTED_EDGE('',*,*,#8859,.T.);
#13298=ORIENTED_EDGE('',*,*,#8856,.T.);
#13299=ORIENTED_EDGE('',*,*,#8853,.T.);
#13300=ORIENTED_EDGE('',*,*,#8850,.T.);
#13301=ORIENTED_EDGE('',*,*,#8847,.T.);
#13302=ORIENTED_EDGE('',*,*,#8844,.T.);
#13303=ORIENTED_EDGE('',*,*,#8841,.T.);
#13304=ORIENTED_EDGE('',*,*,#8838,.T.);
#13305=ORIENTED_EDGE('',*,*,#8835,.T.);
#13306=ORIENTED_EDGE('',*,*,#8832,.T.);
#13307=ORIENTED_EDGE('',*,*,#8829,.T.);
#13308=ORIENTED_EDGE('',*,*,#8826,.T.);
#13309=ORIENTED_EDGE('',*,*,#8823,.T.);
#13310=ORIENTED_EDGE('',*,*,#8820,.T.);
#13311=ORIENTED_EDGE('',*,*,#8817,.T.);
#13312=ORIENTED_EDGE('',*,*,#8814,.T.);
#13313=ORIENTED_EDGE('',*,*,#8811,.T.);
#13314=ORIENTED_EDGE('',*,*,#8808,.T.);
#13315=ORIENTED_EDGE('',*,*,#8805,.T.);
#13316=ORIENTED_EDGE('',*,*,#8802,.T.);
#13317=ORIENTED_EDGE('',*,*,#8799,.T.);
#13318=ORIENTED_EDGE('',*,*,#8796,.T.);
#13319=ORIENTED_EDGE('',*,*,#8786,.T.);
#13320=ORIENTED_EDGE('',*,*,#8898,.T.);
#13321=ORIENTED_EDGE('',*,*,#8888,.T.);
#13322=ORIENTED_EDGE('',*,*,#8900,.F.);
#13323=ORIENTED_EDGE('',*,*,#8901,.T.);
#13324=ORIENTED_EDGE('',*,*,#8902,.T.);
#13325=ORIENTED_EDGE('',*,*,#8903,.F.);
#13326=ORIENTED_EDGE('',*,*,#8904,.F.);
#13327=ORIENTED_EDGE('',*,*,#8905,.T.);
#13328=ORIENTED_EDGE('',*,*,#8906,.T.);
#13329=ORIENTED_EDGE('',*,*,#8901,.F.);
#13330=ORIENTED_EDGE('',*,*,#8907,.F.);
#13331=ORIENTED_EDGE('',*,*,#8908,.T.);
#13332=ORIENTED_EDGE('',*,*,#8909,.T.);
#13333=ORIENTED_EDGE('',*,*,#8905,.F.);
#13334=ORIENTED_EDGE('',*,*,#8910,.F.);
#13335=ORIENTED_EDGE('',*,*,#8911,.T.);
#13336=ORIENTED_EDGE('',*,*,#8912,.T.);
#13337=ORIENTED_EDGE('',*,*,#8908,.F.);
#13338=ORIENTED_EDGE('',*,*,#8913,.F.);
#13339=ORIENTED_EDGE('',*,*,#8914,.T.);
#13340=ORIENTED_EDGE('',*,*,#8915,.T.);
#13341=ORIENTED_EDGE('',*,*,#8911,.F.);
#13342=ORIENTED_EDGE('',*,*,#8916,.F.);
#13343=ORIENTED_EDGE('',*,*,#8903,.T.);
#13344=ORIENTED_EDGE('',*,*,#8917,.T.);
#13345=ORIENTED_EDGE('',*,*,#8914,.F.);
#13346=ORIENTED_EDGE('',*,*,#8917,.F.);
#13347=ORIENTED_EDGE('',*,*,#8902,.F.);
#13348=ORIENTED_EDGE('',*,*,#8906,.F.);
#13349=ORIENTED_EDGE('',*,*,#8909,.F.);
#13350=ORIENTED_EDGE('',*,*,#8912,.F.);
#13351=ORIENTED_EDGE('',*,*,#8915,.F.);
#13352=ORIENTED_EDGE('',*,*,#8918,.T.);
#13353=ORIENTED_EDGE('',*,*,#8895,.T.);
#13354=ORIENTED_EDGE('',*,*,#8897,.T.);
#13355=ORIENTED_EDGE('',*,*,#8899,.T.);
#13356=ORIENTED_EDGE('',*,*,#8694,.F.);
#13357=ORIENTED_EDGE('',*,*,#8918,.F.);
#13358=ORIENTED_EDGE('',*,*,#8919,.T.);
#13359=ORIENTED_EDGE('',*,*,#8920,.T.);
#13360=ORIENTED_EDGE('',*,*,#8919,.F.);
#13361=ORIENTED_EDGE('',*,*,#8920,.F.);
#13362=ORIENTED_EDGE('',*,*,#8900,.T.);
#13363=ORIENTED_EDGE('',*,*,#8916,.T.);
#13364=ORIENTED_EDGE('',*,*,#8913,.T.);
#13365=ORIENTED_EDGE('',*,*,#8910,.T.);
#13366=ORIENTED_EDGE('',*,*,#8907,.T.);
#13367=ORIENTED_EDGE('',*,*,#8904,.T.);
#13368=ORIENTED_EDGE('',*,*,#8891,.T.);
#13883=CYLINDRICAL_SURFACE('',#15725,3.933);
#13884=CYLINDRICAL_SURFACE('',#15727,3.933);
#13885=CYLINDRICAL_SURFACE('',#15728,3.933);
#13886=CYLINDRICAL_SURFACE('',#15729,3.933);
#13887=CYLINDRICAL_SURFACE('',#15730,3.933);
#13888=CYLINDRICAL_SURFACE('',#15731,3.933);
#13889=CYLINDRICAL_SURFACE('',#15732,3.933);
#13890=CYLINDRICAL_SURFACE('',#15733,3.933);
#13891=CYLINDRICAL_SURFACE('',#15734,3.933);
#13892=CYLINDRICAL_SURFACE('',#15735,3.933);
#13893=CYLINDRICAL_SURFACE('',#15736,3.933);
#13894=CYLINDRICAL_SURFACE('',#15737,3.933);
#13895=CYLINDRICAL_SURFACE('',#15738,3.933);
#13896=CYLINDRICAL_SURFACE('',#15739,3.933);
#13897=CYLINDRICAL_SURFACE('',#15740,3.933);
#13898=CYLINDRICAL_SURFACE('',#15741,3.933);
#13899=CYLINDRICAL_SURFACE('',#15742,3.933);
#13900=CYLINDRICAL_SURFACE('',#15743,3.933);
#13901=CYLINDRICAL_SURFACE('',#15744,3.933);
#13902=CYLINDRICAL_SURFACE('',#15745,3.933);
#13903=CYLINDRICAL_SURFACE('',#15746,3.933);
#13904=CYLINDRICAL_SURFACE('',#15747,3.933);
#13905=CYLINDRICAL_SURFACE('',#15748,3.933);
#13906=CYLINDRICAL_SURFACE('',#15749,3.933);
#13907=CYLINDRICAL_SURFACE('',#15750,3.933);
#13908=CYLINDRICAL_SURFACE('',#15751,3.933);
#13909=CYLINDRICAL_SURFACE('',#15752,3.933);
#13910=CYLINDRICAL_SURFACE('',#15753,3.933);
#13911=CYLINDRICAL_SURFACE('',#15754,3.933);
#13912=CYLINDRICAL_SURFACE('',#15755,3.933);
#13913=CYLINDRICAL_SURFACE('',#15756,3.933);
#13914=CYLINDRICAL_SURFACE('',#15757,3.933);
#13915=CYLINDRICAL_SURFACE('',#15759,3.22275);
#13916=CYLINDRICAL_SURFACE('',#15761,3.22275);
#13917=CYLINDRICAL_SURFACE('',#15763,3.22275);
#13918=CYLINDRICAL_SURFACE('',#15764,3.22275);
#13919=CYLINDRICAL_SURFACE('',#15765,3.22275);
#13920=CYLINDRICAL_SURFACE('',#15766,3.22275);
#13921=CYLINDRICAL_SURFACE('',#15767,3.22275);
#13922=CYLINDRICAL_SURFACE('',#15768,3.22275);
#13923=CYLINDRICAL_SURFACE('',#15769,3.22275);
#13924=CYLINDRICAL_SURFACE('',#15770,3.22275);
#13925=CYLINDRICAL_SURFACE('',#15771,3.22275);
#13926=CYLINDRICAL_SURFACE('',#15772,3.22275);
#13927=CYLINDRICAL_SURFACE('',#15773,3.22275);
#13928=CYLINDRICAL_SURFACE('',#15774,3.22275);
#13929=CYLINDRICAL_SURFACE('',#15775,3.22275);
#13930=CYLINDRICAL_SURFACE('',#15776,3.22275);
#13931=CYLINDRICAL_SURFACE('',#15777,3.22275);
#13932=CYLINDRICAL_SURFACE('',#15778,3.22275);
#13933=CYLINDRICAL_SURFACE('',#15779,3.22275);
#13934=CYLINDRICAL_SURFACE('',#15780,3.22275);
#13935=CYLINDRICAL_SURFACE('',#15781,3.22275);
#13936=CYLINDRICAL_SURFACE('',#15782,3.22275);
#13937=CYLINDRICAL_SURFACE('',#15783,3.22275);
#13938=CYLINDRICAL_SURFACE('',#15784,3.22275);
#13939=CYLINDRICAL_SURFACE('',#15785,3.22275);
#13940=CYLINDRICAL_SURFACE('',#15786,3.22275);
#13941=CYLINDRICAL_SURFACE('',#15787,3.22275);
#13942=CYLINDRICAL_SURFACE('',#15788,3.22275);
#13943=CYLINDRICAL_SURFACE('',#15789,3.22275);
#13944=CYLINDRICAL_SURFACE('',#15790,3.22275);
#13945=CYLINDRICAL_SURFACE('',#15791,3.22275);
#13946=CYLINDRICAL_SURFACE('',#15792,3.22275);
#13947=CYLINDRICAL_SURFACE('',#15797,3.22275);
#13948=CYLINDRICAL_SURFACE('',#15799,3.933);
#13949=CYLINDRICAL_SURFACE('',#15809,6.5);
#14650=ADVANCED_FACE('',(#1222),#13883,.T.);
#14651=ADVANCED_FACE('',(#1223),#13884,.T.);
#14652=ADVANCED_FACE('',(#1224),#13885,.T.);
#14653=ADVANCED_FACE('',(#1225),#13886,.T.);
#14654=ADVANCED_FACE('',(#1226),#13887,.T.);
#14655=ADVANCED_FACE('',(#1227),#13888,.T.);
#14656=ADVANCED_FACE('',(#1228),#13889,.T.);
#14657=ADVANCED_FACE('',(#1229),#13890,.T.);
#14658=ADVANCED_FACE('',(#1230),#13891,.T.);
#14659=ADVANCED_FACE('',(#1231),#13892,.T.);
#14660=ADVANCED_FACE('',(#1232),#13893,.T.);
#14661=ADVANCED_FACE('',(#1233),#13894,.T.);
#14662=ADVANCED_FACE('',(#1234),#13895,.T.);
#14663=ADVANCED_FACE('',(#1235),#13896,.T.);
#14664=ADVANCED_FACE('',(#1236),#13897,.T.);
#14665=ADVANCED_FACE('',(#1237),#13898,.T.);
#14666=ADVANCED_FACE('',(#1238),#13899,.T.);
#14667=ADVANCED_FACE('',(#1239),#13900,.T.);
#14668=ADVANCED_FACE('',(#1240),#13901,.T.);
#14669=ADVANCED_FACE('',(#1241),#13902,.T.);
#14670=ADVANCED_FACE('',(#1242),#13903,.T.);
#14671=ADVANCED_FACE('',(#1243),#13904,.T.);
#14672=ADVANCED_FACE('',(#1244),#13905,.T.);
#14673=ADVANCED_FACE('',(#1245),#13906,.T.);
#14674=ADVANCED_FACE('',(#1246),#13907,.T.);
#14675=ADVANCED_FACE('',(#1247),#13908,.T.);
#14676=ADVANCED_FACE('',(#1248),#13909,.T.);
#14677=ADVANCED_FACE('',(#1249),#13910,.T.);
#14678=ADVANCED_FACE('',(#1250),#13911,.T.);
#14679=ADVANCED_FACE('',(#1251),#13912,.T.);
#14680=ADVANCED_FACE('',(#1252),#13913,.T.);
#14681=ADVANCED_FACE('',(#1253),#13914,.T.);
#14682=ADVANCED_FACE('',(#1254),#13915,.T.);
#14683=ADVANCED_FACE('',(#1255),#13916,.T.);
#14684=ADVANCED_FACE('',(#1256),#13917,.T.);
#14685=ADVANCED_FACE('',(#1257),#13918,.T.);
#14686=ADVANCED_FACE('',(#1258),#13919,.T.);
#14687=ADVANCED_FACE('',(#1259),#13920,.T.);
#14688=ADVANCED_FACE('',(#1260),#13921,.T.);
#14689=ADVANCED_FACE('',(#1261),#13922,.T.);
#14690=ADVANCED_FACE('',(#1262),#13923,.T.);
#14691=ADVANCED_FACE('',(#1263),#13924,.T.);
#14692=ADVANCED_FACE('',(#1264),#13925,.T.);
#14693=ADVANCED_FACE('',(#1265),#13926,.T.);
#14694=ADVANCED_FACE('',(#1266),#13927,.T.);
#14695=ADVANCED_FACE('',(#1267),#13928,.T.);
#14696=ADVANCED_FACE('',(#1268),#13929,.T.);
#14697=ADVANCED_FACE('',(#1269),#13930,.T.);
#14698=ADVANCED_FACE('',(#1270),#13931,.T.);
#14699=ADVANCED_FACE('',(#1271),#13932,.T.);
#14700=ADVANCED_FACE('',(#1272),#13933,.T.);
#14701=ADVANCED_FACE('',(#1273),#13934,.T.);
#14702=ADVANCED_FACE('',(#1274),#13935,.T.);
#14703=ADVANCED_FACE('',(#1275),#13936,.T.);
#14704=ADVANCED_FACE('',(#1276),#13937,.T.);
#14705=ADVANCED_FACE('',(#1277),#13938,.T.);
#14706=ADVANCED_FACE('',(#1278),#13939,.T.);
#14707=ADVANCED_FACE('',(#1279),#13940,.T.);
#14708=ADVANCED_FACE('',(#1280),#13941,.T.);
#14709=ADVANCED_FACE('',(#1281),#13942,.T.);
#14710=ADVANCED_FACE('',(#1282),#13943,.T.);
#14711=ADVANCED_FACE('',(#1283),#13944,.T.);
#14712=ADVANCED_FACE('',(#1284),#13945,.T.);
#14713=ADVANCED_FACE('',(#1285),#13946,.T.);
#14714=ADVANCED_FACE('',(#1286),#212,.T.);
#14715=ADVANCED_FACE('',(#1287),#213,.T.);
#14716=ADVANCED_FACE('',(#1288),#296,.F.);
#14717=ADVANCED_FACE('',(#1289),#13947,.T.);
#14718=ADVANCED_FACE('',(#1290),#297,.F.);
#14719=ADVANCED_FACE('',(#1291),#13948,.T.);
#14720=ADVANCED_FACE('',(#1292),#512,.F.);
#14721=ADVANCED_FACE('',(#1293),#513,.F.);
#14722=ADVANCED_FACE('',(#1294),#514,.F.);
#14723=ADVANCED_FACE('',(#1295),#515,.F.);
#14724=ADVANCED_FACE('',(#1296),#516,.F.);
#14725=ADVANCED_FACE('',(#1297),#517,.F.);
#14726=ADVANCED_FACE('',(#1298),#518,.F.);
#14727=ADVANCED_FACE('',(#1299,#363),#519,.T.);
#14728=ADVANCED_FACE('',(#1300),#13949,.T.);
#14729=ADVANCED_FACE('',(#1301,#364),#520,.F.);
#14730=ADVANCED_FACE('',(#1302),#521,.T.);
#14741=CLOSED_SHELL('',(#14650,#14651,#14652,#14653,#14654,#14655,#14656,
#14657,#14658,#14659,#14660,#14661,#14662,#14663,#14664,#14665,#14666,#14667,
#14668,#14669,#14670,#14671,#14672,#14673,#14674,#14675,#14676,#14677,#14678,
#14679,#14680,#14681,#14682,#14683,#14684,#14685,#14686,#14687,#14688,#14689,
#14690,#14691,#14692,#14693,#14694,#14695,#14696,#14697,#14698,#14699,#14700,
#14701,#14702,#14703,#14704,#14705,#14706,#14707,#14708,#14709,#14710,#14711,
#14712,#14713,#14714,#14715,#14716,#14717,#14718,#14719,#14720,#14721,#14722,
#14723,#14724,#14725,#14726,#14727,#14728,#14729,#14730));
#15724=AXIS2_PLACEMENT_3D('',#64829,#18346,#18347);
#15725=AXIS2_PLACEMENT_3D('',#64830,#18348,#18349);
#15726=AXIS2_PLACEMENT_3D('',#64846,#18351,#18352);
#15727=AXIS2_PLACEMENT_3D('',#64854,#18353,#18354);
#15728=AXIS2_PLACEMENT_3D('',#64902,#18356,#18357);
#15729=AXIS2_PLACEMENT_3D('',#64950,#18359,#18360);
#15730=AXIS2_PLACEMENT_3D('',#65001,#18362,#18363);
#15731=AXIS2_PLACEMENT_3D('',#65052,#18365,#18366);
#15732=AXIS2_PLACEMENT_3D('',#65100,#18368,#18369);
#15733=AXIS2_PLACEMENT_3D('',#65148,#18371,#18372);
#15734=AXIS2_PLACEMENT_3D('',#65199,#18374,#18375);
#15735=AXIS2_PLACEMENT_3D('',#65247,#18377,#18378);
#15736=AXIS2_PLACEMENT_3D('',#65295,#18380,#18381);
#15737=AXIS2_PLACEMENT_3D('',#65346,#18383,#18384);
#15738=AXIS2_PLACEMENT_3D('',#65397,#18386,#18387);
#15739=AXIS2_PLACEMENT_3D('',#65445,#18389,#18390);
#15740=AXIS2_PLACEMENT_3D('',#65496,#18392,#18393);
#15741=AXIS2_PLACEMENT_3D('',#65547,#18395,#18396);
#15742=AXIS2_PLACEMENT_3D('',#65595,#18398,#18399);
#15743=AXIS2_PLACEMENT_3D('',#65646,#18401,#18402);
#15744=AXIS2_PLACEMENT_3D('',#65694,#18404,#18405);
#15745=AXIS2_PLACEMENT_3D('',#65745,#18407,#18408);
#15746=AXIS2_PLACEMENT_3D('',#65796,#18410,#18411);
#15747=AXIS2_PLACEMENT_3D('',#65844,#18413,#18414);
#15748=AXIS2_PLACEMENT_3D('',#65895,#18416,#18417);
#15749=AXIS2_PLACEMENT_3D('',#65946,#18419,#18420);
#15750=AXIS2_PLACEMENT_3D('',#65994,#18422,#18423);
#15751=AXIS2_PLACEMENT_3D('',#66042,#18425,#18426);
#15752=AXIS2_PLACEMENT_3D('',#66093,#18428,#18429);
#15753=AXIS2_PLACEMENT_3D('',#66144,#18431,#18432);
#15754=AXIS2_PLACEMENT_3D('',#66192,#18434,#18435);
#15755=AXIS2_PLACEMENT_3D('',#66243,#18437,#18438);
#15756=AXIS2_PLACEMENT_3D('',#66294,#18440,#18441);
#15757=AXIS2_PLACEMENT_3D('',#66342,#18443,#18444);
#15758=AXIS2_PLACEMENT_3D('',#66347,#18446,#18447);
#15759=AXIS2_PLACEMENT_3D('',#66392,#18448,#18449);
#15760=AXIS2_PLACEMENT_3D('',#66402,#18451,#18452);
#15761=AXIS2_PLACEMENT_3D('',#66403,#18453,#18454);
#15762=AXIS2_PLACEMENT_3D('',#66418,#18456,#18457);
#15763=AXIS2_PLACEMENT_3D('',#66429,#18458,#18459);
#15764=AXIS2_PLACEMENT_3D('',#66453,#18461,#18462);
#15765=AXIS2_PLACEMENT_3D('',#66477,#18464,#18465);
#15766=AXIS2_PLACEMENT_3D('',#66503,#18467,#18468);
#15767=AXIS2_PLACEMENT_3D('',#66527,#18470,#18471);
#15768=AXIS2_PLACEMENT_3D('',#66551,#18473,#18474);
#15769=AXIS2_PLACEMENT_3D('',#66577,#18476,#18477);
#15770=AXIS2_PLACEMENT_3D('',#66601,#18479,#18480);
#15771=AXIS2_PLACEMENT_3D('',#66625,#18482,#18483);
#15772=AXIS2_PLACEMENT_3D('',#66649,#18485,#18486);
#15773=AXIS2_PLACEMENT_3D('',#66675,#18488,#18489);
#15774=AXIS2_PLACEMENT_3D('',#66699,#18491,#18492);
#15775=AXIS2_PLACEMENT_3D('',#66723,#18494,#18495);
#15776=AXIS2_PLACEMENT_3D('',#66749,#18497,#18498);
#15777=AXIS2_PLACEMENT_3D('',#66773,#18500,#18501);
#15778=AXIS2_PLACEMENT_3D('',#66797,#18503,#18504);
#15779=AXIS2_PLACEMENT_3D('',#66822,#18506,#18507);
#15780=AXIS2_PLACEMENT_3D('',#66847,#18509,#18510);
#15781=AXIS2_PLACEMENT_3D('',#66871,#18512,#18513);
#15782=AXIS2_PLACEMENT_3D('',#66896,#18515,#18516);
#15783=AXIS2_PLACEMENT_3D('',#66921,#18518,#18519);
#15784=AXIS2_PLACEMENT_3D('',#66945,#18521,#18522);
#15785=AXIS2_PLACEMENT_3D('',#66970,#18524,#18525);
#15786=AXIS2_PLACEMENT_3D('',#66994,#18527,#18528);
#15787=AXIS2_PLACEMENT_3D('',#67019,#18530,#18531);
#15788=AXIS2_PLACEMENT_3D('',#67043,#18533,#18534);
#15789=AXIS2_PLACEMENT_3D('',#67068,#18536,#18537);
#15790=AXIS2_PLACEMENT_3D('',#67093,#18539,#18540);
#15791=AXIS2_PLACEMENT_3D('',#67117,#18542,#18543);
#15792=AXIS2_PLACEMENT_3D('',#67142,#18545,#18546);
#15793=AXIS2_PLACEMENT_3D('',#67166,#18548,#18549);
#15794=AXIS2_PLACEMENT_3D('',#67170,#18551,#18552);
#15795=AXIS2_PLACEMENT_3D('',#67432,#18554,#18555);
#15796=AXIS2_PLACEMENT_3D('',#67482,#18556,#18557);
#15797=AXIS2_PLACEMENT_3D('',#68426,#18558,#18559);
#15798=AXIS2_PLACEMENT_3D('',#68437,#18560,#18561);
#15799=AXIS2_PLACEMENT_3D('',#69369,#18562,#18563);
#15800=AXIS2_PLACEMENT_3D('',#69370,#18564,#18565);
#15801=AXIS2_PLACEMENT_3D('',#69379,#18570,#18571);
#15802=AXIS2_PLACEMENT_3D('',#69385,#18575,#18576);
#15803=AXIS2_PLACEMENT_3D('',#69391,#18580,#18581);
#15804=AXIS2_PLACEMENT_3D('',#69397,#18585,#18586);
#15805=AXIS2_PLACEMENT_3D('',#69403,#18590,#18591);
#15806=AXIS2_PLACEMENT_3D('',#69406,#18594,#18595);
#15807=AXIS2_PLACEMENT_3D('',#69407,#18596,#18597);
#15808=AXIS2_PLACEMENT_3D('',#69409,#18598,#18599);
#15809=AXIS2_PLACEMENT_3D('',#69410,#18600,#18601);
#15810=AXIS2_PLACEMENT_3D('',#69413,#18603,#18604);
#15811=AXIS2_PLACEMENT_3D('',#69414,#18605,#18606);
#15812=AXIS2_PLACEMENT_3D('',#69415,#18607,#18608);
#18346=DIRECTION('axis',(0.,0.,1.));
#18347=DIRECTION('refdir',(1.,0.,0.));
#18348=DIRECTION('center_axis',(0.,0.,1.));
#18349=DIRECTION('ref_axis',(1.,0.,0.));
#18350=DIRECTION('',(0.,0.,-1.));
#18351=DIRECTION('center_axis',(0.,0.,-1.));
#18352=DIRECTION('ref_axis',(1.,0.,0.));
#18353=DIRECTION('center_axis',(0.,0.,1.));
#18354=DIRECTION('ref_axis',(1.,0.,0.));
#18355=DIRECTION('',(0.,0.,-1.));
#18356=DIRECTION('center_axis',(0.,0.,1.));
#18357=DIRECTION('ref_axis',(1.,0.,0.));
#18358=DIRECTION('',(0.,0.,-1.));
#18359=DIRECTION('center_axis',(0.,0.,1.));
#18360=DIRECTION('ref_axis',(1.,0.,0.));
#18361=DIRECTION('',(0.,0.,-1.));
#18362=DIRECTION('center_axis',(0.,0.,1.));
#18363=DIRECTION('ref_axis',(1.,0.,0.));
#18364=DIRECTION('',(0.,0.,-1.));
#18365=DIRECTION('center_axis',(0.,0.,1.));
#18366=DIRECTION('ref_axis',(1.,0.,0.));
#18367=DIRECTION('',(0.,0.,-1.));
#18368=DIRECTION('center_axis',(0.,0.,1.));
#18369=DIRECTION('ref_axis',(1.,0.,0.));
#18370=DIRECTION('',(0.,0.,-1.));
#18371=DIRECTION('center_axis',(0.,0.,1.));
#18372=DIRECTION('ref_axis',(1.,0.,0.));
#18373=DIRECTION('',(0.,0.,-1.));
#18374=DIRECTION('center_axis',(0.,0.,1.));
#18375=DIRECTION('ref_axis',(1.,0.,0.));
#18376=DIRECTION('',(0.,0.,-1.));
#18377=DIRECTION('center_axis',(0.,0.,1.));
#18378=DIRECTION('ref_axis',(1.,0.,0.));
#18379=DIRECTION('',(0.,0.,-1.));
#18380=DIRECTION('center_axis',(0.,0.,1.));
#18381=DIRECTION('ref_axis',(1.,0.,0.));
#18382=DIRECTION('',(0.,0.,-1.));
#18383=DIRECTION('center_axis',(0.,0.,1.));
#18384=DIRECTION('ref_axis',(1.,0.,0.));
#18385=DIRECTION('',(0.,0.,-1.));
#18386=DIRECTION('center_axis',(0.,0.,1.));
#18387=DIRECTION('ref_axis',(1.,0.,0.));
#18388=DIRECTION('',(0.,0.,-1.));
#18389=DIRECTION('center_axis',(0.,0.,1.));
#18390=DIRECTION('ref_axis',(1.,0.,0.));
#18391=DIRECTION('',(0.,0.,-1.));
#18392=DIRECTION('center_axis',(0.,0.,1.));
#18393=DIRECTION('ref_axis',(1.,0.,0.));
#18394=DIRECTION('',(0.,0.,-1.));
#18395=DIRECTION('center_axis',(0.,0.,1.));
#18396=DIRECTION('ref_axis',(1.,0.,0.));
#18397=DIRECTION('',(0.,0.,-1.));
#18398=DIRECTION('center_axis',(0.,0.,1.));
#18399=DIRECTION('ref_axis',(1.,0.,0.));
#18400=DIRECTION('',(0.,0.,-1.));
#18401=DIRECTION('center_axis',(0.,0.,1.));
#18402=DIRECTION('ref_axis',(1.,0.,0.));
#18403=DIRECTION('',(0.,0.,-1.));
#18404=DIRECTION('center_axis',(0.,0.,1.));
#18405=DIRECTION('ref_axis',(1.,0.,0.));
#18406=DIRECTION('',(0.,0.,-1.));
#18407=DIRECTION('center_axis',(0.,0.,1.));
#18408=DIRECTION('ref_axis',(1.,0.,0.));
#18409=DIRECTION('',(0.,0.,-1.));
#18410=DIRECTION('center_axis',(0.,0.,1.));
#18411=DIRECTION('ref_axis',(1.,0.,0.));
#18412=DIRECTION('',(0.,0.,-1.));
#18413=DIRECTION('center_axis',(0.,0.,1.));
#18414=DIRECTION('ref_axis',(1.,0.,0.));
#18415=DIRECTION('',(0.,0.,-1.));
#18416=DIRECTION('center_axis',(0.,0.,1.));
#18417=DIRECTION('ref_axis',(1.,0.,0.));
#18418=DIRECTION('',(0.,0.,-1.));
#18419=DIRECTION('center_axis',(0.,0.,1.));
#18420=DIRECTION('ref_axis',(1.,0.,0.));
#18421=DIRECTION('',(0.,0.,-1.));
#18422=DIRECTION('center_axis',(0.,0.,1.));
#18423=DIRECTION('ref_axis',(1.,0.,0.));
#18424=DIRECTION('',(0.,0.,-1.));
#18425=DIRECTION('center_axis',(0.,0.,1.));
#18426=DIRECTION('ref_axis',(1.,0.,0.));
#18427=DIRECTION('',(0.,0.,-1.));
#18428=DIRECTION('center_axis',(0.,0.,1.));
#18429=DIRECTION('ref_axis',(1.,0.,0.));
#18430=DIRECTION('',(0.,0.,-1.));
#18431=DIRECTION('center_axis',(0.,0.,1.));
#18432=DIRECTION('ref_axis',(1.,0.,0.));
#18433=DIRECTION('',(0.,0.,-1.));
#18434=DIRECTION('center_axis',(0.,0.,1.));
#18435=DIRECTION('ref_axis',(1.,0.,0.));
#18436=DIRECTION('',(0.,0.,-1.));
#18437=DIRECTION('center_axis',(0.,0.,1.));
#18438=DIRECTION('ref_axis',(1.,0.,0.));
#18439=DIRECTION('',(0.,0.,-1.));
#18440=DIRECTION('center_axis',(0.,0.,1.));
#18441=DIRECTION('ref_axis',(1.,0.,0.));
#18442=DIRECTION('',(0.,0.,-1.));
#18443=DIRECTION('center_axis',(0.,0.,1.));
#18444=DIRECTION('ref_axis',(1.,0.,0.));
#18445=DIRECTION('',(0.,0.,-1.));
#18446=DIRECTION('center_axis',(0.,0.,-1.));
#18447=DIRECTION('ref_axis',(1.,0.,0.));
#18448=DIRECTION('center_axis',(0.,0.,1.));
#18449=DIRECTION('ref_axis',(1.,-2.38163665272677E-13,0.));
#18450=DIRECTION('',(0.,0.,1.));
#18451=DIRECTION('center_axis',(0.,0.,-1.));
#18452=DIRECTION('ref_axis',(1.,-2.38163665272677E-13,0.));
#18453=DIRECTION('center_axis',(0.,0.,1.));
#18454=DIRECTION('ref_axis',(1.,-2.38163665272677E-13,0.));
#18455=DIRECTION('',(0.,0.,1.));
#18456=DIRECTION('center_axis',(0.,0.,-1.));
#18457=DIRECTION('ref_axis',(1.,-2.38163665272677E-13,0.));
#18458=DIRECTION('center_axis',(0.,0.,1.));
#18459=DIRECTION('ref_axis',(1.,-2.38163665272677E-13,0.));
#18460=DIRECTION('',(0.,0.,1.));
#18461=DIRECTION('center_axis',(0.,0.,1.));
#18462=DIRECTION('ref_axis',(1.,-2.38163665272677E-13,0.));
#18463=DIRECTION('',(0.,0.,1.));
#18464=DIRECTION('center_axis',(0.,0.,1.));
#18465=DIRECTION('ref_axis',(1.,-2.38163665272677E-13,0.));
#18466=DIRECTION('',(0.,0.,1.));
#18467=DIRECTION('center_axis',(0.,0.,1.));
#18468=DIRECTION('ref_axis',(1.,-2.38163665272677E-13,0.));
#18469=DIRECTION('',(0.,0.,1.));
#18470=DIRECTION('center_axis',(0.,0.,1.));
#18471=DIRECTION('ref_axis',(1.,-2.38163665272677E-13,0.));
#18472=DIRECTION('',(0.,0.,1.));
#18473=DIRECTION('center_axis',(0.,0.,1.));
#18474=DIRECTION('ref_axis',(1.,-2.38163665272677E-13,0.));
#18475=DIRECTION('',(0.,0.,1.));
#18476=DIRECTION('center_axis',(0.,0.,1.));
#18477=DIRECTION('ref_axis',(1.,-2.38163665272677E-13,0.));
#18478=DIRECTION('',(0.,0.,1.));
#18479=DIRECTION('center_axis',(0.,0.,1.));
#18480=DIRECTION('ref_axis',(1.,-2.38163665272677E-13,0.));
#18481=DIRECTION('',(0.,0.,1.));
#18482=DIRECTION('center_axis',(0.,0.,1.));
#18483=DIRECTION('ref_axis',(1.,-2.38163665272677E-13,0.));
#18484=DIRECTION('',(0.,0.,1.));
#18485=DIRECTION('center_axis',(0.,0.,1.));
#18486=DIRECTION('ref_axis',(1.,-2.38163665272677E-13,0.));
#18487=DIRECTION('',(0.,0.,1.));
#18488=DIRECTION('center_axis',(0.,0.,1.));
#18489=DIRECTION('ref_axis',(1.,-2.38163665272677E-13,0.));
#18490=DIRECTION('',(0.,0.,1.));
#18491=DIRECTION('center_axis',(0.,0.,1.));
#18492=DIRECTION('ref_axis',(1.,-2.38163665272677E-13,0.));
#18493=DIRECTION('',(0.,0.,1.));
#18494=DIRECTION('center_axis',(0.,0.,1.));
#18495=DIRECTION('ref_axis',(1.,-2.38163665272677E-13,0.));
#18496=DIRECTION('',(0.,0.,1.));
#18497=DIRECTION('center_axis',(0.,0.,1.));
#18498=DIRECTION('ref_axis',(1.,-2.38163665272677E-13,0.));
#18499=DIRECTION('',(0.,0.,1.));
#18500=DIRECTION('center_axis',(0.,0.,1.));
#18501=DIRECTION('ref_axis',(1.,-2.38163665272677E-13,0.));
#18502=DIRECTION('',(0.,0.,1.));
#18503=DIRECTION('center_axis',(0.,0.,1.));
#18504=DIRECTION('ref_axis',(1.,-2.38163665272677E-13,0.));
#18505=DIRECTION('',(0.,0.,1.));
#18506=DIRECTION('center_axis',(0.,0.,1.));
#18507=DIRECTION('ref_axis',(1.,-2.38163665272677E-13,0.));
#18508=DIRECTION('',(0.,0.,1.));
#18509=DIRECTION('center_axis',(0.,0.,1.));
#18510=DIRECTION('ref_axis',(1.,-2.38163665272677E-13,0.));
#18511=DIRECTION('',(0.,0.,1.));
#18512=DIRECTION('center_axis',(0.,0.,1.));
#18513=DIRECTION('ref_axis',(1.,-2.38163665272677E-13,0.));
#18514=DIRECTION('',(0.,0.,1.));
#18515=DIRECTION('center_axis',(0.,0.,1.));
#18516=DIRECTION('ref_axis',(1.,-2.38163665272677E-13,0.));
#18517=DIRECTION('',(0.,0.,1.));
#18518=DIRECTION('center_axis',(0.,0.,1.));
#18519=DIRECTION('ref_axis',(1.,-2.38163665272677E-13,0.));
#18520=DIRECTION('',(0.,0.,1.));
#18521=DIRECTION('center_axis',(0.,0.,1.));
#18522=DIRECTION('ref_axis',(1.,-2.38163665272677E-13,0.));
#18523=DIRECTION('',(0.,0.,1.));
#18524=DIRECTION('center_axis',(0.,0.,1.));
#18525=DIRECTION('ref_axis',(1.,-2.38163665272677E-13,0.));
#18526=DIRECTION('',(0.,0.,1.));
#18527=DIRECTION('center_axis',(0.,0.,1.));
#18528=DIRECTION('ref_axis',(1.,-2.38163665272677E-13,0.));
#18529=DIRECTION('',(0.,0.,1.));
#18530=DIRECTION('center_axis',(0.,0.,1.));
#18531=DIRECTION('ref_axis',(1.,-2.38163665272677E-13,0.));
#18532=DIRECTION('',(0.,0.,1.));
#18533=DIRECTION('center_axis',(0.,0.,1.));
#18534=DIRECTION('ref_axis',(1.,-2.38163665272677E-13,0.));
#18535=DIRECTION('',(0.,0.,1.));
#18536=DIRECTION('center_axis',(0.,0.,1.));
#18537=DIRECTION('ref_axis',(1.,-2.38163665272677E-13,0.));
#18538=DIRECTION('',(0.,0.,1.));
#18539=DIRECTION('center_axis',(0.,0.,1.));
#18540=DIRECTION('ref_axis',(1.,-2.38163665272677E-13,0.));
#18541=DIRECTION('',(0.,0.,1.));
#18542=DIRECTION('center_axis',(0.,0.,1.));
#18543=DIRECTION('ref_axis',(1.,-2.38163665272677E-13,0.));
#18544=DIRECTION('',(0.,0.,1.));
#18545=DIRECTION('center_axis',(0.,0.,1.));
#18546=DIRECTION('ref_axis',(1.,-2.38163665272677E-13,0.));
#18547=DIRECTION('',(0.,0.,1.));
#18548=DIRECTION('center_axis',(0.,0.,-1.));
#18549=DIRECTION('ref_axis',(1.,0.,0.));
#18550=DIRECTION('',(0.707106781186547,8.65956056235493E-17,0.707106781186548));
#18551=DIRECTION('center_axis',(0.,0.,-1.));
#18552=DIRECTION('ref_axis',(1.,0.,0.));
#18553=DIRECTION('',(0.707106781186547,8.65956056235493E-17,0.707106781186548));
#18554=DIRECTION('center_axis',(0.,0.,1.));
#18555=DIRECTION('ref_axis',(1.,0.,0.));
#18556=DIRECTION('center_axis',(0.,0.,-1.));
#18557=DIRECTION('ref_axis',(-0.976187422880467,0.216928825677901,0.));
#18558=DIRECTION('center_axis',(0.,0.,1.));
#18559=DIRECTION('ref_axis',(1.,-2.38163665272677E-13,0.));
#18560=DIRECTION('center_axis',(0.,0.,-1.));
#18561=DIRECTION('ref_axis',(1.,-2.38163665272677E-13,0.));
#18562=DIRECTION('center_axis',(0.,0.,1.));
#18563=DIRECTION('ref_axis',(1.,0.,0.));
#18564=DIRECTION('center_axis',(-1.60246890531964E-16,-1.,0.));
#18565=DIRECTION('ref_axis',(1.,-1.60246890531964E-16,0.));
#18566=DIRECTION('',(1.,-1.60246890531964E-16,0.));
#18567=DIRECTION('',(0.,0.,1.));
#18568=DIRECTION('',(1.,-1.60246890531964E-16,0.));
#18569=DIRECTION('',(0.,0.,1.));
#18570=DIRECTION('center_axis',(-0.866025403784439,-0.5,0.));
#18571=DIRECTION('ref_axis',(0.5,-0.866025403784439,0.));
#18572=DIRECTION('',(0.5,-0.866025403784439,0.));
#18573=DIRECTION('',(0.,0.,1.));
#18574=DIRECTION('',(0.5,-0.866025403784439,0.));
#18575=DIRECTION('center_axis',(-0.866025403784439,0.5,0.));
#18576=DIRECTION('ref_axis',(-0.5,-0.866025403784439,0.));
#18577=DIRECTION('',(-0.5,-0.866025403784439,0.));
#18578=DIRECTION('',(0.,0.,1.));
#18579=DIRECTION('',(-0.5,-0.866025403784439,0.));
#18580=DIRECTION('center_axis',(1.60246890531964E-16,1.,0.));
#18581=DIRECTION('ref_axis',(-1.,1.60246890531964E-16,0.));
#18582=DIRECTION('',(-1.,1.60246890531964E-16,0.));
#18583=DIRECTION('',(0.,0.,1.));
#18584=DIRECTION('',(-1.,1.60246890531964E-16,0.));
#18585=DIRECTION('center_axis',(0.866025403784439,0.5,0.));
#18586=DIRECTION('ref_axis',(-0.5,0.866025403784439,0.));
#18587=DIRECTION('',(-0.5,0.866025403784439,0.));
#18588=DIRECTION('',(0.,0.,1.));
#18589=DIRECTION('',(-0.5,0.866025403784439,0.));
#18590=DIRECTION('center_axis',(0.866025403784439,-0.5,0.));
#18591=DIRECTION('ref_axis',(0.5,0.866025403784439,0.));
#18592=DIRECTION('',(0.5,0.866025403784439,0.));
#18593=DIRECTION('',(0.5,0.866025403784439,0.));
#18594=DIRECTION('center_axis',(0.,0.,1.));
#18595=DIRECTION('ref_axis',(1.,0.,0.));
#18596=DIRECTION('center_axis',(0.,0.,1.));
#18597=DIRECTION('ref_axis',(1.,0.,0.));
#18598=DIRECTION('center_axis',(0.,0.,1.));
#18599=DIRECTION('ref_axis',(1.,0.,0.));
#18600=DIRECTION('center_axis',(0.,0.,1.));
#18601=DIRECTION('ref_axis',(1.,0.,0.));
#18602=DIRECTION('',(0.,0.,-1.));
#18603=DIRECTION('center_axis',(0.,0.,1.));
#18604=DIRECTION('ref_axis',(1.,0.,0.));
#18605=DIRECTION('center_axis',(0.,0.,1.));
#18606=DIRECTION('ref_axis',(1.,0.,0.));
#18607=DIRECTION('center_axis',(0.,0.,1.));
#18608=DIRECTION('ref_axis',(1.,0.,0.));
#64829=CARTESIAN_POINT('',(0.,0.,0.));
#64830=CARTESIAN_POINT('Origin',(0.,0.,0.));
#64831=CARTESIAN_POINT('',(-3.93802926031087,0.00240391602587063,0.404163522034967));
#64832=CARTESIAN_POINT('',(-3.93675118057464,0.0040445736593347,0.220836477965066));
#64833=CARTESIAN_POINT('',(-3.933,-4.81653586104654E-16,0.));
#64834=CARTESIAN_POINT('',(1.74869447533108,3.5228619944509,0.));
#64835=CARTESIAN_POINT('Ctrl Pts',(-3.93802926031087,0.00240391602587063,
0.404163522034967));
#64836=CARTESIAN_POINT('Ctrl Pts',(-3.93883377792363,0.125055838975485,
0.397936338459335));
#64837=CARTESIAN_POINT('Ctrl Pts',(-3.93360440738597,0.247633516884382,
0.391709154883702));
#64838=CARTESIAN_POINT('Ctrl Pts',(-3.92211779044761,0.369616139861192,
0.385481971308069));
#64839=CARTESIAN_POINT('Ctrl Pts',(-3.79982975336477,1.66825921310945,0.319186554641402));
#64840=CARTESIAN_POINT('Ctrl Pts',(-2.96834465298263,2.89945868843819,0.252891137974736));
#64841=CARTESIAN_POINT('Ctrl Pts',(-1.80941221321754,3.49902123369862,0.186595721308069));
#64842=CARTESIAN_POINT('Ctrl Pts',(-0.722098059799251,4.06153274770308,
0.124397147538713));
#64843=CARTESIAN_POINT('Ctrl Pts',(0.653443523808812,4.06806145998554,0.0621985737693561));
#64844=CARTESIAN_POINT('Ctrl Pts',(1.75279216821279,3.52834843496255,-3.8597597340484E-16));
#64845=CARTESIAN_POINT('',(-1.74869447533093,3.52286199445097,0.));
#64846=CARTESIAN_POINT('Origin',(0.,0.,0.));
#64847=CARTESIAN_POINT('Ctrl Pts',(-1.74869447533093,3.52286199445097,-8.32667268468867E-15));
#64848=CARTESIAN_POINT('Ctrl Pts',(-2.91721720025602,2.94282529798265,0.0659890197515385));
#64849=CARTESIAN_POINT('Ctrl Pts',(-3.7645849420613,1.74090009686325,0.131978039503085));
#64850=CARTESIAN_POINT('Ctrl Pts',(-3.91293878839921,0.452893260042974,
0.197967059254632));
#64851=CARTESIAN_POINT('Ctrl Pts',(-3.9300768225852,0.304100992460439,0.205590198824777));
#64852=CARTESIAN_POINT('Ctrl Pts',(-3.93788639153707,0.15415995008081,0.213213338394921));
#64853=CARTESIAN_POINT('Ctrl Pts',(-3.93675118057464,0.0040445736593347,
0.220836477965066));
#64854=CARTESIAN_POINT('Origin',(0.,0.,0.));
#64855=CARTESIAN_POINT('',(-3.92802248803715,0.00242352018653469,1.65416352203497));
#64856=CARTESIAN_POINT('',(-3.92713181934273,0.00148022330437236,1.47083647796506));
#64857=CARTESIAN_POINT('',(-3.933,-4.81653586104654E-16,0.));
#64858=CARTESIAN_POINT('Ctrl Pts',(-3.92802248803715,0.00242352018653469,
1.65416352203497));
#64859=CARTESIAN_POINT('Ctrl Pts',(-3.93080769929044,0.500504119499087,
1.62904217179267));
#64860=CARTESIAN_POINT('Ctrl Pts',(-3.84303217595021,0.997638580245937,
1.60392082155037));
#64861=CARTESIAN_POINT('Ctrl Pts',(-3.66020947060703,1.45693784959832,1.57879947130807));
#64862=CARTESIAN_POINT('Ctrl Pts',(-3.17773908943919,2.66903179131414,1.5125040546414));
#64863=CARTESIAN_POINT('Ctrl Pts',(-2.03332616040844,3.61762793685371,1.44620863797474));
#64864=CARTESIAN_POINT('Ctrl Pts',(-0.752770987957444,3.86691928292382,
1.37991322130807));
#64865=CARTESIAN_POINT('Ctrl Pts',(0.52778418449355,4.11621062899393,1.31361780464141));
#64866=CARTESIAN_POINT('Ctrl Pts',(1.9444816003648,3.66619717559459,1.24732238797474));
#64867=CARTESIAN_POINT('Ctrl Pts',(2.84640187373471,2.72358226420012,1.18102697130807));
#64868=CARTESIAN_POINT('Ctrl Pts',(3.74832214710463,1.78096735280565,1.1147315546414));
#64869=CARTESIAN_POINT('Ctrl Pts',(4.13546527797321,0.345750983416053,1.04843613797474));
#64870=CARTESIAN_POINT('Ctrl Pts',(3.82997742875317,-0.922539768331961,
0.98214072130807));
#64871=CARTESIAN_POINT('Ctrl Pts',(3.52448957953313,-2.19083052007998,0.915845304641404));
#64872=CARTESIAN_POINT('Ctrl Pts',(2.52637075022448,-3.29219565418641,0.849549887974737));
#64873=CARTESIAN_POINT('Ctrl Pts',(1.29417138623458,-3.72081813581125,0.78325447130807));
#64874=CARTESIAN_POINT('Ctrl Pts',(0.0619720222446886,-4.14944061743609,
0.716959054641403));
#64875=CARTESIAN_POINT('Ctrl Pts',(-1.40430787642644,-3.90532044657934,
0.650663637974736));
#64876=CARTESIAN_POINT('Ctrl Pts',(-2.43090233887023,-3.10021702556709,
0.58436822130807));
#64877=CARTESIAN_POINT('Ctrl Pts',(-3.36106793040868,-2.37073763789067,
0.524299988217036));
#64878=CARTESIAN_POINT('Ctrl Pts',(-3.93026877743734,-1.18071268995158,
0.464231755126001));
#64879=CARTESIAN_POINT('Ctrl Pts',(-3.93802926031087,0.00240391602587063,
0.404163522034967));
#64880=CARTESIAN_POINT('Ctrl Pts',(-3.93675118057464,0.0040445736593347,
0.220836477965066));
#64881=CARTESIAN_POINT('Ctrl Pts',(-3.92805954028601,-1.14530025900202,
0.279202358146468));
#64882=CARTESIAN_POINT('Ctrl Pts',(-3.39501944186553,-2.30486465960329,
0.33756823832787));
#64883=CARTESIAN_POINT('Ctrl Pts',(-2.50983784011762,-3.03729680249085,
0.395934118509273));
#64884=CARTESIAN_POINT('Ctrl Pts',(-1.50904309462757,-3.86539155568325,
0.46192313826082));
#64885=CARTESIAN_POINT('Ctrl Pts',(-0.0581136527769394,-4.14749258954689,
0.527912158012366));
#64886=CARTESIAN_POINT('Ctrl Pts',(1.18097747525515,-3.75784467875485,0.593901177763913));
#64887=CARTESIAN_POINT('Ctrl Pts',(2.42006860328725,-3.3681967679628,0.65989019751546));
#64888=CARTESIAN_POINT('Ctrl Pts',(3.4473214175008,-2.30679991251506,0.725879217267006));
#64889=CARTESIAN_POINT('Ctrl Pts',(3.7952461569347,-1.05580326723859,0.791868237018553));
#64890=CARTESIAN_POINT('Ctrl Pts',(4.14317089636859,0.195193378037875,0.857857256770099));
#64891=CARTESIAN_POINT('Ctrl Pts',(3.81176756102284,1.63578981314307,0.923846276521646));
#64892=CARTESIAN_POINT('Ctrl Pts',(2.95175447945861,2.60896495945216,0.989835296273193));
#64893=CARTESIAN_POINT('Ctrl Pts',(2.09174139789438,3.58214010576126,1.05582431602474));
#64894=CARTESIAN_POINT('Ctrl Pts',(0.703118570111659,4.08789396327424,1.12181333577629));
#64895=CARTESIAN_POINT('Ctrl Pts',(-0.581358437963121,3.89619610319946,
1.18780235552783));
#64896=CARTESIAN_POINT('Ctrl Pts',(-1.8658354460379,3.70449824312467,1.25379137527938));
#64897=CARTESIAN_POINT('Ctrl Pts',(-3.04616663440473,2.81534866546211,1.31978039503093));
#64898=CARTESIAN_POINT('Ctrl Pts',(-3.58469551400156,1.63362301388125,1.38576941478248));
#64899=CARTESIAN_POINT('Ctrl Pts',(-3.81610305421957,1.12583181343609,1.41412510251));
#64900=CARTESIAN_POINT('Ctrl Pts',(-3.92900515343478,0.564017970515558,
1.44248079023753));
#64901=CARTESIAN_POINT('Ctrl Pts',(-3.92713181934273,0.00148022330437236,
1.47083647796506));
#64902=CARTESIAN_POINT('Origin',(0.,0.,0.));
#64903=CARTESIAN_POINT('',(-3.92922266509235,-0.00303564498597975,2.90416352203497));
#64904=CARTESIAN_POINT('',(-3.93210165425081,-0.00353477514852048,2.72083647796507));
#64905=CARTESIAN_POINT('',(-3.933,-4.81653586104654E-16,0.));
#64906=CARTESIAN_POINT('Ctrl Pts',(-3.92922266509235,-0.00303564498597975,
2.90416352203497));
#64907=CARTESIAN_POINT('Ctrl Pts',(-3.92297871157792,0.868988737466586,
2.860148005126));
#64908=CARTESIAN_POINT('Ctrl Pts',(-3.63674668852252,1.74473416863609,2.81613248821704));
#64909=CARTESIAN_POINT('Ctrl Pts',(-3.1031365207039,2.42700192932171,2.77211697130807));
#64910=CARTESIAN_POINT('Ctrl Pts',(-2.29942203778026,3.45462192902401,2.70582155464141));
#64911=CARTESIAN_POINT('Ctrl Pts',(-0.934508767172172,4.04332104416919,
2.63952613797474));
#64912=CARTESIAN_POINT('Ctrl Pts',(0.364487440276112,3.9226192477873,2.57323072130807));
#64913=CARTESIAN_POINT('Ctrl Pts',(1.66348364772439,3.80191745140542,2.5069353046414));
#64914=CARTESIAN_POINT('Ctrl Pts',(2.89656279201286,2.97181474349649,2.44063988797474));
#64915=CARTESIAN_POINT('Ctrl Pts',(3.49718050582551,1.81370463302472,2.37434447130807));
#64916=CARTESIAN_POINT('Ctrl Pts',(4.09779821963816,0.655594522552941,2.30804905464141));
#64917=CARTESIAN_POINT('Ctrl Pts',(4.06595450297497,-0.830522990481683,
2.24175363797474));
#64918=CARTESIAN_POINT('Ctrl Pts',(3.41628053171535,-1.96184182221916,2.17545822130807));
#64919=CARTESIAN_POINT('Ctrl Pts',(2.76660656045572,-3.09316065395665,2.1091628046414));
#64920=CARTESIAN_POINT('Ctrl Pts',(1.49910233459966,-3.86968080439699,2.04286738797474));
#64921=CARTESIAN_POINT('Ctrl Pts',(0.19612795048357,-3.93463064846122,1.97657197130807));
#64922=CARTESIAN_POINT('Ctrl Pts',(-1.10684643363252,-3.99958049252545,
1.91027655464141));
#64923=CARTESIAN_POINT('Ctrl Pts',(-2.44529097600864,-3.35296003021357,
1.84398113797474));
#64924=CARTESIAN_POINT('Ctrl Pts',(-3.20424933054423,-2.29185393011158,
1.77768572130807));
#64925=CARTESIAN_POINT('Ctrl Pts',(-3.67561527519315,-1.6328332127583,1.7365116548837));
#64926=CARTESIAN_POINT('Ctrl Pts',(-3.92345750757062,-0.813934019634444,
1.69533758845933));
#64927=CARTESIAN_POINT('Ctrl Pts',(-3.92802248803715,0.00242352018653469,
1.65416352203497));
#64928=CARTESIAN_POINT('Ctrl Pts',(-3.92713181934273,0.00148022330437236,
1.47083647796506));
#64929=CARTESIAN_POINT('Ctrl Pts',(-3.92464555258188,-0.745113194575937,
1.50846980998908));
#64930=CARTESIAN_POINT('Ctrl Pts',(-3.71999058729667,-1.49298171797386,
1.5461031420131));
#64931=CARTESIAN_POINT('Ctrl Pts',(-3.32188673684523,-2.11752639505612,
1.58373647403711));
#64932=CARTESIAN_POINT('Ctrl Pts',(-2.62382250926525,-3.21264842691343,
1.64972549378866));
#64933=CARTESIAN_POINT('Ctrl Pts',(-1.33096748327849,-3.92859076512888,
1.71571451354021));
#64934=CARTESIAN_POINT('Ctrl Pts',(-0.0323314417446383,-3.93924298867845,
1.78170353329176));
#64935=CARTESIAN_POINT('Ctrl Pts',(1.26630459978921,-3.94989521222801,1.8476925530433));
#64936=CARTESIAN_POINT('Ctrl Pts',(2.57072165687014,-3.2552573211117,1.91368157279485));
#64937=CARTESIAN_POINT('Ctrl Pts',(3.28667213041528,-2.17175971616106,1.9796705925464));
#64938=CARTESIAN_POINT('Ctrl Pts',(4.00262260396041,-1.08826211121042,2.04565961229794));
#64939=CARTESIAN_POINT('Ctrl Pts',(4.13010649396975,0.384095207574565,2.11164863204949));
#64940=CARTESIAN_POINT('Ctrl Pts',(3.61104023017667,1.57453066739559,2.17763765180103));
#64941=CARTESIAN_POINT('Ctrl Pts',(3.0919739663836,2.76496612721661,2.24362667155258));
#64942=CARTESIAN_POINT('Ctrl Pts',(1.92635754878811,3.67347972807368,2.30961569130413));
#64943=CARTESIAN_POINT('Ctrl Pts',(0.645217602507054,3.8861845142162,2.37560471105568));
#64944=CARTESIAN_POINT('Ctrl Pts',(-0.635922343774005,4.09888930035871,
2.44159373080722));
#64945=CARTESIAN_POINT('Ctrl Pts',(-2.03258581874064,3.61578527178667,2.50758275055877));
#64946=CARTESIAN_POINT('Ctrl Pts',(-2.90849151609697,2.65695776267421,2.57357177031032));
#64947=CARTESIAN_POINT('Ctrl Pts',(-3.56006454516537,1.94370044929889,2.62266000619523));
#64948=CARTESIAN_POINT('Ctrl Pts',(-3.92346857353215,0.967194528045436,
2.67174824208015));
#64949=CARTESIAN_POINT('Ctrl Pts',(-3.93210165425081,-0.00353477514852048,
2.72083647796507));
#64950=CARTESIAN_POINT('Origin',(0.,0.,0.));
#64951=CARTESIAN_POINT('',(-3.93905614328696,-0.0012270906503109,4.15416352203497));
#64952=CARTESIAN_POINT('',(-3.93880751349539,0.00135256466245784,3.97083647796506));
#64953=CARTESIAN_POINT('',(-3.933,-4.81653586104654E-16,0.));
#64954=CARTESIAN_POINT('Ctrl Pts',(-3.93905614328696,-0.0012270906503109,
4.15416352203497));
#64955=CARTESIAN_POINT('Ctrl Pts',(-3.93400271395434,1.23712682041522,4.09125383845934));
#64956=CARTESIAN_POINT('Ctrl Pts',(-3.30186786252818,2.47992387689092,4.0283441548837));
#64957=CARTESIAN_POINT('Ctrl Pts',(-2.29585618320052,3.20138074646178,3.96543447130807));
#64958=CARTESIAN_POINT('Ctrl Pts',(-1.2357020119849,3.96166566694986,3.89913905464141));
#64959=CARTESIAN_POINT('Ctrl Pts',(0.239655229969981,4.14298438694454,3.83284363797474));
#64960=CARTESIAN_POINT('Ctrl Pts',(1.45235556362318,3.66202916089297,3.76654822130808));
#64961=CARTESIAN_POINT('Ctrl Pts',(2.66505589727639,3.1810739348414,3.70025280464141));
#64962=CARTESIAN_POINT('Ctrl Pts',(3.61509932262791,2.03784476274358,3.63395738797474));
#64963=CARTESIAN_POINT('Ctrl Pts',(3.86598381354877,0.757603762828532,3.56766197130808));
#64964=CARTESIAN_POINT('Ctrl Pts',(4.11686830446962,-0.522637237086509,
3.50136655464141));
#64965=CARTESIAN_POINT('Ctrl Pts',(3.66859386095981,-1.93989006481879,3.43507113797474));
#64966=CARTESIAN_POINT('Ctrl Pts',(2.727122341044,-2.84299104576975,3.36877572130807));
#64967=CARTESIAN_POINT('Ctrl Pts',(1.78565082112817,-3.74609202672072,3.30248030464141));
#64968=CARTESIAN_POINT('Ctrl Pts',(0.350982224806341,-4.13504116089037,
3.23618488797474));
#64969=CARTESIAN_POINT('Ctrl Pts',(-0.917718077119649,-3.83113398528177,
3.16988947130807));
#64970=CARTESIAN_POINT('Ctrl Pts',(-2.18641837904563,-3.52722680967316,
3.10359405464141));
#64971=CARTESIAN_POINT('Ctrl Pts',(-3.28915038657576,-2.5304633242863,3.03729863797474));
#64972=CARTESIAN_POINT('Ctrl Pts',(-3.71925854272124,-1.29881113946316,
2.97100322130807));
#64973=CARTESIAN_POINT('Ctrl Pts',(-3.86380498477882,-0.884889806828835,
2.94872332155037));
#64974=CARTESIAN_POINT('Ctrl Pts',(-3.93238324727252,-0.44443943146198,
2.92644342179267));
#64975=CARTESIAN_POINT('Ctrl Pts',(-3.92922266509235,-0.00303564498597975,
2.90416352203497));
#64976=CARTESIAN_POINT('Ctrl Pts',(-3.93210165425081,-0.00353477514852048,
2.72083647796507));
#64977=CARTESIAN_POINT('Ctrl Pts',(-3.93507397192935,-0.337751025753829,
2.7377372618317));
#64978=CARTESIAN_POINT('Ctrl Pts',(-3.89599232991999,-0.671282525635842,
2.75463804569833));
#64979=CARTESIAN_POINT('Ctrl Pts',(-3.8121385671165,-0.993149807387589,
2.77153882956496));
#64980=CARTESIAN_POINT('Ctrl Pts',(-3.48473200103367,-2.24987887868406,
2.8375278493165));
#64981=CARTESIAN_POINT('Ctrl Pts',(-2.47477094912201,-3.32878603162411,
2.90351686906805));
#64982=CARTESIAN_POINT('Ctrl Pts',(-1.24236721552543,-3.73835094435147,
2.9695058888196));
#64983=CARTESIAN_POINT('Ctrl Pts',(-0.00996348192884827,-4.14791585707883,
3.03549490857114));
#64984=CARTESIAN_POINT('Ctrl Pts',(1.44488293335264,-3.88813852959348,3.10148392832269));
#64985=CARTESIAN_POINT('Ctrl Pts',(2.45938288232363,-3.07736603319569,3.16747294807423));
#64986=CARTESIAN_POINT('Ctrl Pts',(3.47388283129462,-2.26659353679789,3.23346196782578));
#64987=CARTESIAN_POINT('Ctrl Pts',(4.04803631395511,-0.904825871487629,
3.29945098757733));
#64988=CARTESIAN_POINT('Ctrl Pts',(3.92027415756993,0.387551512556629,3.36544000732888));
#64989=CARTESIAN_POINT('Ctrl Pts',(3.79251200118475,1.67992889660089,3.43142902708043));
#64990=CARTESIAN_POINT('Ctrl Pts',(2.9628342057539,2.90291599937915,3.49741804683197));
#64991=CARTESIAN_POINT('Ctrl Pts',(1.80921997711047,3.4993525625956,3.56340706658351));
#64992=CARTESIAN_POINT('Ctrl Pts',(0.655605748467037,4.09578912581204,3.62939608633506));
#64993=CARTESIAN_POINT('Ctrl Pts',(-0.821944913388967,4.06567514946666,
3.69538510608661));
#64994=CARTESIAN_POINT('Ctrl Pts',(-1.95029923212904,3.42272967879372,3.76137412583816));
#64995=CARTESIAN_POINT('Ctrl Pts',(-3.07865355086909,2.77978420812079,3.82736314558971));
#64996=CARTESIAN_POINT('Ctrl Pts',(-3.85781152649321,1.52400724312031,3.89335216534125));
#64997=CARTESIAN_POINT('Ctrl Pts',(-3.93280948119039,0.227497431243224,
3.9593411850928));
#64998=CARTESIAN_POINT('Ctrl Pts',(-3.93716436455993,0.152213391285224,
3.96317294938355));
#64999=CARTESIAN_POINT('Ctrl Pts',(-3.93914500265902,0.0767920107140475,
3.96700471367431));
#65000=CARTESIAN_POINT('Ctrl Pts',(-3.93880751349539,0.00135256466245784,
3.97083647796506));
#65001=CARTESIAN_POINT('Origin',(0.,0.,0.));
#65002=CARTESIAN_POINT('',(-3.93296230846032,0.00363373906124689,5.40416352203497));
#65003=CARTESIAN_POINT('',(-3.92828912629456,0.00246571223358432,5.22083647796506));
#65004=CARTESIAN_POINT('',(-3.933,-4.81653586104654E-16,0.));
#65005=CARTESIAN_POINT('Ctrl Pts',(-3.93296230846032,0.00363373906124689,
5.40416352203497));
#65006=CARTESIAN_POINT('Ctrl Pts',(-3.9357953201641,0.310142843416023,5.38865508845934));
#65007=CARTESIAN_POINT('Ctrl Pts',(-3.90300011193378,0.616052391820026,
5.37314665488371));
#65008=CARTESIAN_POINT('Ctrl Pts',(-3.83227848816066,0.912927092582172,
5.35763822130808));
#65009=CARTESIAN_POINT('Ctrl Pts',(-3.5299578512944,2.18200638991017,5.29134280464141));
#65010=CARTESIAN_POINT('Ctrl Pts',(-2.53457385463363,3.285983824268,5.22504738797474));
#65011=CARTESIAN_POINT('Ctrl Pts',(-1.30346046335894,3.71763165307261,5.15875197130808));
#65012=CARTESIAN_POINT('Ctrl Pts',(-0.0723470720842406,4.14927948187723,
5.09245655464141));
#65013=CARTESIAN_POINT('Ctrl Pts',(1.39449571380438,3.90859770512862,5.02616113797475));
#65014=CARTESIAN_POINT('Ctrl Pts',(2.42311992072895,3.10616872311079,4.95986572130808));
#65015=CARTESIAN_POINT('Ctrl Pts',(3.45174412765351,2.30373974109297,4.89357030464141));
#65016=CARTESIAN_POINT('Ctrl Pts',(4.04214975561404,0.939563553805948,4.82727488797474));
#65017=CARTESIAN_POINT('Ctrl Pts',(3.92307209884529,-0.359582528175298,
4.76097947130807));
#65018=CARTESIAN_POINT('Ctrl Pts',(3.80399444207653,-1.65872861015655,4.69468405464141));
#65019=CARTESIAN_POINT('Ctrl Pts',(2.97543350057849,-2.89284458683203,4.62838863797474));
#65020=CARTESIAN_POINT('Ctrl Pts',(1.81807558455521,-3.49490993557188,4.56209322130808));
#65021=CARTESIAN_POINT('Ctrl Pts',(0.660717668531931,-4.09697528431174,
4.49579780464141));
#65022=CARTESIAN_POINT('Ctrl Pts',(-0.825437222016575,-4.06699000511596,
4.42950238797474));
#65023=CARTESIAN_POINT('Ctrl Pts',(-1.9575680744248,-3.4187309805296,4.36320697130807));
#65024=CARTESIAN_POINT('Ctrl Pts',(-3.08969892683302,-2.77047195594323,
4.29691155464141));
#65025=CARTESIAN_POINT('Ctrl Pts',(-3.86780574110097,-1.50393918596629,
4.23061613797475));
#65026=CARTESIAN_POINT('Ctrl Pts',(-3.93438359799676,-0.201047240487073,
4.16432072130808));
#65027=CARTESIAN_POINT('Ctrl Pts',(-3.93778375542175,-0.134508034676906,
4.16093498821704));
#65028=CARTESIAN_POINT('Ctrl Pts',(-3.93932811354563,-0.0678739974030474,
4.15754925512601));
#65029=CARTESIAN_POINT('Ctrl Pts',(-3.93905614328696,-0.0012270906503109,
4.15416352203497));
#65030=CARTESIAN_POINT('Ctrl Pts',(-3.93880751349539,0.00135256466245784,
3.97083647796506));
#65031=CARTESIAN_POINT('Ctrl Pts',(-3.93333290739557,-1.22239413900672,
4.03299373342586));
#65032=CARTESIAN_POINT('Ctrl Pts',(-3.31786739155683,-2.45089458463356,
4.09515098888665));
#65033=CARTESIAN_POINT('Ctrl Pts',(-2.33195280377124,-3.17501835816601,
4.15730824434744));
#65034=CARTESIAN_POINT('Ctrl Pts',(-1.28526023788469,-3.94378167694446,
4.22329726409898));
#65035=CARTESIAN_POINT('Ctrl Pts',(0.178962827658628,-4.14406565574766,
4.28928628385053));
#65036=CARTESIAN_POINT('Ctrl Pts',(1.39365528985826,-3.68462622601686,4.35527530360208));
#65037=CARTESIAN_POINT('Ctrl Pts',(2.60834775205789,-3.22518679628606,4.42126432335363));
#65038=CARTESIAN_POINT('Ctrl Pts',(3.57350961091383,-2.10602395802126,4.48725334310517));
#65039=CARTESIAN_POINT('Ctrl Pts',(3.84943877691641,-0.836998557262767,
4.55324236285672));
#65040=CARTESIAN_POINT('Ctrl Pts',(4.12536794291899,0.432026843495729,4.61923138260827));
#65041=CARTESIAN_POINT('Ctrl Pts',(3.71206441606821,1.85091480674793,4.68522040235981));
#65042=CARTESIAN_POINT('Ctrl Pts',(2.79781829806152,2.77325769599943,4.75120942211136));
#65043=CARTESIAN_POINT('Ctrl Pts',(1.88357218005484,3.69560058525093,4.81719844186291));
#65044=CARTESIAN_POINT('Ctrl Pts',(0.468383470892278,4.12139840050174,4.88318746161446));
#65045=CARTESIAN_POINT('Ctrl Pts',(-0.80302547217005,3.85666897385885,4.949176481366));
#65046=CARTESIAN_POINT('Ctrl Pts',(-2.07443441523238,3.59193954721596,5.01516550111755));
#65047=CARTESIAN_POINT('Ctrl Pts',(-3.20206359219447,2.63668287867936,5.08115452086909));
#65048=CARTESIAN_POINT('Ctrl Pts',(-3.67219512395154,1.42608851501744,5.14714354062064));
#65049=CARTESIAN_POINT('Ctrl Pts',(-3.84720087310926,0.97544660051541,5.17170785306878));
#65050=CARTESIAN_POINT('Ctrl Pts',(-3.93109787542163,0.489422814161963,
5.19627216551692));
#65051=CARTESIAN_POINT('Ctrl Pts',(-3.92828912629456,0.00246571223358432,
5.22083647796506));
#65052=CARTESIAN_POINT('Origin',(0.,0.,0.));
#65053=CARTESIAN_POINT('',(-3.92652974478545,-0.000411687324547438,6.65416352203497));
#65054=CARTESIAN_POINT('',(-3.93002130470952,-0.00320230624235995,6.47083647796506));
#65055=CARTESIAN_POINT('',(-3.933,-4.81653586104654E-16,0.));
#65056=CARTESIAN_POINT('Ctrl Pts',(-3.92652974478545,-0.000411687324547438,
6.65416352203497));
#65057=CARTESIAN_POINT('Ctrl Pts',(-3.92589461438976,0.682335166633042,
6.61976092179267));
#65058=CARTESIAN_POINT('Ctrl Pts',(-3.75684139145261,1.36537647043677,6.58535832155038));
#65059=CARTESIAN_POINT('Ctrl Pts',(-3.42117596084786,1.95329192188792,6.55095572130808));
#65060=CARTESIAN_POINT('Ctrl Pts',(-2.77433300636735,3.0862324422038,6.48466030464142));
#65061=CARTESIAN_POINT('Ctrl Pts',(-1.50877413310263,3.8659222616113,6.41836488797474));
#65062=CARTESIAN_POINT('Ctrl Pts',(-0.20596645283144,3.93412914220049,6.35206947130808));
#65063=CARTESIAN_POINT('Ctrl Pts',(1.09684122743973,4.00233602278968,6.28577405464141));
#65064=CARTESIAN_POINT('Ctrl Pts',(2.43689771471741,3.35905996456059,6.21947863797475));
#65065=CARTESIAN_POINT('Ctrl Pts',(3.19850761012674,2.29985724668934,6.15318322130808));
#65066=CARTESIAN_POINT('Ctrl Pts',(3.96011750553607,1.24065452881808,6.08688780464141));
#65067=CARTESIAN_POINT('Ctrl Pts',(4.14328080907704,-0.234474848695338,
6.02059238797475));
#65068=CARTESIAN_POINT('Ctrl Pts',(3.66384225990336,-1.44777559785307,5.95429697130808));
#65069=CARTESIAN_POINT('Ctrl Pts',(3.18440371072968,-2.66107634701081,5.88800155464141));
#65070=CARTESIAN_POINT('Ctrl Pts',(2.04236330884135,-3.61254846781286,5.82170613797475));
#65071=CARTESIAN_POINT('Ctrl Pts',(0.762437010209958,-3.86503351766844,
5.75541072130808));
#65072=CARTESIAN_POINT('Ctrl Pts',(-0.517489288421428,-4.11751856752401,
5.68911530464141));
#65073=CARTESIAN_POINT('Ctrl Pts',(-1.93530148379588,-3.67101654643311,
5.62281988797474));
#65074=CARTESIAN_POINT('Ctrl Pts',(-2.83957894294725,-2.73067495573858,
5.55652447130808));
#65075=CARTESIAN_POINT('Ctrl Pts',(-3.53231950235033,-2.0103067181193,5.50573748821704));
#65076=CARTESIAN_POINT('Ctrl Pts',(-3.92368476815972,-1.00012158053316,
5.45495050512601));
#65077=CARTESIAN_POINT('Ctrl Pts',(-3.93296230846032,0.00363373906124689,
5.40416352203497));
#65078=CARTESIAN_POINT('Ctrl Pts',(-3.92828912629456,0.00246571223358432,
5.22083647796506));
#65079=CARTESIAN_POINT('Ctrl Pts',(-3.92355251456471,-0.818727857066773,
5.26226118526847));
#65080=CARTESIAN_POINT('Ctrl Pts',(-3.6722360563846,-1.64257565411253,5.30368589257188));
#65081=CARTESIAN_POINT('Ctrl Pts',(-3.19545580456006,-2.30386798269549,
5.34511059987528));
#65082=CARTESIAN_POINT('Ctrl Pts',(-2.43595106685949,-3.35729805795928,
5.41109961962683));
#65083=CARTESIAN_POINT('Ctrl Pts',(-1.10430770490628,-3.99822614969962,
5.47708863937837));
#65084=CARTESIAN_POINT('Ctrl Pts',(0.192812962944398,-3.93466245600138,
5.54307765912992));
#65085=CARTESIAN_POINT('Ctrl Pts',(1.48993363079507,-3.87109876230314,5.60906667888147));
#65086=CARTESIAN_POINT('Ctrl Pts',(2.75253160454323,-3.10304328316634,5.67505569863302));
#65087=CARTESIAN_POINT('Ctrl Pts',(3.40540080922965,-1.98040167883568,5.74104471838456));
#65088=CARTESIAN_POINT('Ctrl Pts',(4.05827001391607,-0.85776007450501,5.80703373813611));
#65089=CARTESIAN_POINT('Ctrl Pts',(4.10141044954074,0.619467655019518,5.87302275788765));
#65090=CARTESIAN_POINT('Ctrl Pts',(3.51516848040003,1.77829582336785,5.9390117776392));
#65091=CARTESIAN_POINT('Ctrl Pts',(2.92892651125932,2.93712399171616,6.00500079739075));
#65092=CARTESIAN_POINT('Ctrl Pts',(1.71330213735326,3.77755259888829,6.0709898171423));
#65093=CARTESIAN_POINT('Ctrl Pts',(0.422101510131257,3.91670471139359,6.13697883689384));
#65094=CARTESIAN_POINT('Ctrl Pts',(-0.869099117090753,4.0558568238989,6.20296785664539));
#65095=CARTESIAN_POINT('Ctrl Pts',(-2.23587599762871,3.49373244173736,6.26895687639693));
#65096=CARTESIAN_POINT('Ctrl Pts',(-3.05556191587462,2.48642049125139,6.33494589614848));
#65097=CARTESIAN_POINT('Ctrl Pts',(-3.61821914155989,1.79497107770904,6.38024275675401));
#65098=CARTESIAN_POINT('Ctrl Pts',(-3.92309448347202,0.893755285438259,
6.42553961735953));
#65099=CARTESIAN_POINT('Ctrl Pts',(-3.93002130470952,-0.00320230624235995,
6.47083647796506));
#65100=CARTESIAN_POINT('Origin',(0.,0.,0.));
#65101=CARTESIAN_POINT('',(-3.93447829914432,-0.00349241703522352,7.90416352203497));
#65102=CARTESIAN_POINT('',(-3.93938385220859,1.46978575541911E-5,7.72083647796507));
#65103=CARTESIAN_POINT('',(-3.933,-4.81653586104654E-16,0.));
#65104=CARTESIAN_POINT('Ctrl Pts',(-3.93447829914432,-0.00349241703522352,
7.90416352203497));
#65105=CARTESIAN_POINT('Ctrl Pts',(-3.9247550811977,1.04882587479658,7.85086675512601));
#65106=CARTESIAN_POINT('Ctrl Pts',(-3.48928102444049,2.10824344340663,7.79756998821704));
#65107=CARTESIAN_POINT('Ctrl Pts',(-2.73422329881441,2.83616241414651,7.74427322130808));
#65108=CARTESIAN_POINT('Ctrl Pts',(-1.79501310969974,3.74161492587582,7.67797780464141));
#65109=CARTESIAN_POINT('Ctrl Pts',(-0.361321637001168,4.13415057686167,
7.61168238797475));
#65110=CARTESIAN_POINT('Ctrl Pts',(0.90813467596085,3.83341697412564,7.54538697130808));
#65111=CARTESIAN_POINT('Ctrl Pts',(2.17759098892287,3.5326833713896,7.47909155464142));
#65112=CARTESIAN_POINT('Ctrl Pts',(3.28281214214833,2.53868051493168,7.41279613797475));
#65113=CARTESIAN_POINT('Ctrl Pts',(3.71599896057147,1.30810779839759,7.34650072130808));
#65114=CARTESIAN_POINT('Ctrl Pts',(4.14918577899461,0.0775350818634785,
7.28020530464142));
#65115=CARTESIAN_POINT('Ctrl Pts',(3.91033826261541,-1.3896074947468,7.21390988797475));
#65116=CARTESIAN_POINT('Ctrl Pts',(3.10919605171297,-2.41923421751785,7.14761447130808));
#65117=CARTESIAN_POINT('Ctrl Pts',(2.30805384081054,-3.44886094028888,7.08131905464142));
#65118=CARTESIAN_POINT('Ctrl Pts',(0.944616935384907,-4.04097180922069,
7.01502363797475));
#65119=CARTESIAN_POINT('Ctrl Pts',(-0.354677020107964,-3.92351863747392,
6.94872822130808));
#65120=CARTESIAN_POINT('Ctrl Pts',(-1.65397097560085,-3.80606546572714,
6.88243280464142));
#65121=CARTESIAN_POINT('Ctrl Pts',(-2.88912198116097,-2.97904825330177,
6.81613738797475));
#65122=CARTESIAN_POINT('Ctrl Pts',(-3.49263396609285,-1.82244403647695,
6.74984197130808));
#65123=CARTESIAN_POINT('Ctrl Pts',(-3.78296620794476,-1.26603504445995,
6.71794915488371));
#65124=CARTESIAN_POINT('Ctrl Pts',(-3.92711854031175,-0.633349893280725,
6.68605633845934));
#65125=CARTESIAN_POINT('Ctrl Pts',(-3.92652974478545,-0.000411687324547438,
6.65416352203497));
#65126=CARTESIAN_POINT('Ctrl Pts',(-3.93002130470952,-0.00320230624235995,
6.47083647796506));
#65127=CARTESIAN_POINT('Ctrl Pts',(-3.93318556124973,-0.412943488880185,
6.49152863711108));
#65128=CARTESIAN_POINT('Ctrl Pts',(-3.87417469570846,-0.821796081297978,
6.5122207962571));
#65129=CARTESIAN_POINT('Ctrl Pts',(-3.74915976782805,-1.2093578942389,6.53291295540312));
#65130=CARTESIAN_POINT('Ctrl Pts',(-3.35047674558173,-2.44532481043286,
6.59890197515467));
#65131=CARTESIAN_POINT('Ctrl Pts',(-2.28051574513518,-3.46475912401038,
6.66489099490622));
#65132=CARTESIAN_POINT('Ctrl Pts',(-1.02672255697162,-3.80323365993697,
6.73088001465776));
#65133=CARTESIAN_POINT('Ctrl Pts',(0.227070631191932,-4.14170819586356,
6.79686903440931));
#65134=CARTESIAN_POINT('Ctrl Pts',(1.6646960070725,-3.79922295413924,6.86285805416086));
#65135=CARTESIAN_POINT('Ctrl Pts',(2.63120966385873,-2.93180510707663,6.92884707391241));
#65136=CARTESIAN_POINT('Ctrl Pts',(3.59772332064497,-2.06438726001401,6.99483609366395));
#65137=CARTESIAN_POINT('Ctrl Pts',(4.09312525833685,-0.67203680761309,7.0608251134155));
#65138=CARTESIAN_POINT('Ctrl Pts',(3.89172352271858,0.610928394972594,7.12681413316704));
#65139=CARTESIAN_POINT('Ctrl Pts',(3.69032178710031,1.89389359755828,7.19280315291859));
#65140=CARTESIAN_POINT('Ctrl Pts',(2.79211637817189,3.06747355032872,7.25879217267014));
#65141=CARTESIAN_POINT('Ctrl Pts',(1.6063058044677,3.59701642248127,7.32478119242169));
#65142=CARTESIAN_POINT('Ctrl Pts',(0.420495230763517,4.12655929463381,7.39077021217323));
#65143=CARTESIAN_POINT('Ctrl Pts',(-1.05292050771645,4.01206508616847,7.45675923192478));
#65144=CARTESIAN_POINT('Ctrl Pts',(-2.14269236632785,3.30569431501852,7.52274825167632));
#65145=CARTESIAN_POINT('Ctrl Pts',(-3.23313122693673,2.59889120501564,7.58877766043924));
#65146=CARTESIAN_POINT('Ctrl Pts',(-3.93945619971352,1.29948678660994,7.65480706920215));
#65147=CARTESIAN_POINT('Ctrl Pts',(-3.93938382520912,1.46977953919901E-5,
7.72083647796507));
#65148=CARTESIAN_POINT('Origin',(0.,0.,0.));
#65149=CARTESIAN_POINT('',(-3.93821611579729,0.00204091754689266,9.15416352203497));
#65150=CARTESIAN_POINT('',(-3.92998043343738,0.00319075123336177,8.97083647796505));
#65151=CARTESIAN_POINT('',(-3.933,-4.81653586104654E-16,0.));
#65152=CARTESIAN_POINT('Ctrl Pts',(-3.93821611579729,0.00204091754689266,
9.15416352203497));
#65153=CARTESIAN_POINT('Ctrl Pts',(-3.93894783685051,0.118157629700958,
9.148268005126));
#65154=CARTESIAN_POINT('Ctrl Pts',(-3.93425943595939,0.234214412386688,
9.14237248821704));
#65155=CARTESIAN_POINT('Ctrl Pts',(-3.92395904216079,0.349770957401461,
9.13647697130808));
#65156=CARTESIAN_POINT('Ctrl Pts',(-3.80813053903654,1.64921075523655,9.07018155464141));
#65157=CARTESIAN_POINT('Ctrl Pts',(-2.98265834852961,2.88539485919645,9.00388613797475));
#65158=CARTESIAN_POINT('Ctrl Pts',(-1.82680963916627,3.49035253655646,8.93759072130809));
#65159=CARTESIAN_POINT('Ctrl Pts',(-0.670960929802935,4.09531021391648,
8.87129530464142));
#65160=CARTESIAN_POINT('Ctrl Pts',(0.815264298416776,4.06904146467662,8.80499988797475));
#65161=CARTESIAN_POINT('Ctrl Pts',(1.94901271550604,3.42361559203026,8.73870447130808));
#65162=CARTESIAN_POINT('Ctrl Pts',(3.08276113259532,2.7781897193839,8.67240905464142));
#65163=CARTESIAN_POINT('Ctrl Pts',(3.86403273855411,1.51360672333098,8.60611363797475));
#65164=CARTESIAN_POINT('Ctrl Pts',(3.93386853603566,0.210885344169694,8.53981822130808));
#65165=CARTESIAN_POINT('Ctrl Pts',(4.00370433351722,-1.09183603499157,8.47352280464141));
#65166=CARTESIAN_POINT('Ctrl Pts',(3.36210432252157,-2.43269579726122,8.40722738797475));
#65167=CARTESIAN_POINT('Ctrl Pts',(2.30385471425629,-3.19562947520453,8.34093197130808));
#65168=CARTESIAN_POINT('Ctrl Pts',(1.245605105991,-3.95856315314785,8.27463655464141));
#65169=CARTESIAN_POINT('Ctrl Pts',(-0.229294099543933,-4.14357074676481,
8.20834113797475));
#65170=CARTESIAN_POINT('Ctrl Pts',(-1.44319336796336,-3.66564962726439,
8.14204572130808));
#65171=CARTESIAN_POINT('Ctrl Pts',(-2.65709263638277,-3.18772850776397,
8.07575030464142));
#65172=CARTESIAN_POINT('Ctrl Pts',(-3.60999196768669,-2.04687867514619,
8.00945488797475));
#65173=CARTESIAN_POINT('Ctrl Pts',(-3.86407718057327,-0.767269072600908,
7.94315947130809));
#65174=CARTESIAN_POINT('Ctrl Pts',(-3.91389607993295,-0.516373944605648,
7.93016082155038));
#65175=CARTESIAN_POINT('Ctrl Pts',(-3.9368497132457,-0.260144324880089,
7.91716217179267));
#65176=CARTESIAN_POINT('Ctrl Pts',(-3.93447829914432,-0.00349241703522352,
7.90416352203497));
#65177=CARTESIAN_POINT('Ctrl Pts',(-3.93938382520912,1.46977953919901E-5,
7.72083647796507));
#65178=CARTESIAN_POINT('Ctrl Pts',(-3.93931153924511,-1.29786766323116,
7.78678510870525));
#65179=CARTESIAN_POINT('Ctrl Pts',(-3.23496159726654,-2.5958172902133,7.85273373944543));
#65180=CARTESIAN_POINT('Ctrl Pts',(-2.14671745478129,-3.30308184131171,
7.91868237018561));
#65181=CARTESIAN_POINT('Ctrl Pts',(-1.05780683742692,-4.01077954341983,
7.98467138993715));
#65182=CARTESIAN_POINT('Ctrl Pts',(0.415468342137214,-4.12706843993453,
8.0506604096887));
#65183=CARTESIAN_POINT('Ctrl Pts',(1.60192307417263,-3.59897040075338,8.11664942944025));
#65184=CARTESIAN_POINT('Ctrl Pts',(2.78837780620806,-3.07087236157223,8.18263844919179));
#65185=CARTESIAN_POINT('Ctrl Pts',(3.68801209071479,-1.89838738669521,8.24862746894334));
#65186=CARTESIAN_POINT('Ctrl Pts',(3.89097646142656,-0.61566846410235,8.31461648869489));
#65187=CARTESIAN_POINT('Ctrl Pts',(4.09394083213833,0.667050458490491,8.38060550844643));
#65188=CARTESIAN_POINT('Ctrl Pts',(3.60023528905517,2.06000332879919,8.44659452819797));
#65189=CARTESIAN_POINT('Ctrl Pts',(2.63477895410256,2.92859784608333,8.51258354794952));
#65190=CARTESIAN_POINT('Ctrl Pts',(1.66932261914996,3.79719236336747,8.57857256770107));
#65191=CARTESIAN_POINT('Ctrl Pts',(0.232115492327916,4.14142852762707,8.64456158745263));
#65192=CARTESIAN_POINT('Ctrl Pts',(-1.02208906270644,3.80448149278736,8.71055060720417));
#65193=CARTESIAN_POINT('Ctrl Pts',(-2.2762936177408,3.46753445794766,8.77653962695572));
#65194=CARTESIAN_POINT('Ctrl Pts',(-3.34749560098745,2.44940422400868,8.84252864670726));
#65195=CARTESIAN_POINT('Ctrl Pts',(-3.74768386318513,1.21392386198126,8.9085176664588));
#65196=CARTESIAN_POINT('Ctrl Pts',(-3.8736606644409,0.82500225001839,8.92929060362755));
#65197=CARTESIAN_POINT('Ctrl Pts',(-3.93314325094733,0.414542291462066,
8.9500635407963));
#65198=CARTESIAN_POINT('Ctrl Pts',(-3.92998043343738,0.00319075123336177,
8.97083647796505));
#65199=CARTESIAN_POINT('Origin',(0.,0.,0.));
#65200=CARTESIAN_POINT('',(-3.92814797210457,0.00249985979813405,10.404163522035));
#65201=CARTESIAN_POINT('',(-3.92831996318525,-0.00248455515896013,10.2208364779651));
#65202=CARTESIAN_POINT('',(-3.933,-4.81653586104654E-16,0.));
#65203=CARTESIAN_POINT('Ctrl Pts',(-3.92814797210457,0.00249985979813405,
10.404163522035));
#65204=CARTESIAN_POINT('Ctrl Pts',(-3.93099418832143,0.493964345027469,
10.3793738384593));
#65205=CARTESIAN_POINT('Ctrl Pts',(-3.84559145503871,0.984475393727741,
10.3545841548837));
#65206=CARTESIAN_POINT('Ctrl Pts',(-3.66745126380575,1.43860888180441,10.3297944713081));
#65207=CARTESIAN_POINT('Ctrl Pts',(-3.19104832115264,2.65310477169666,10.2634990546414));
#65208=CARTESIAN_POINT('Ctrl Pts',(-2.05139084139042,3.60742982376513,10.1972036379748));
#65209=CARTESIAN_POINT('Ctrl Pts',(-0.772099935454148,3.86311480244487,
10.1309082213081));
#65210=CARTESIAN_POINT('Ctrl Pts',(0.507190970482145,4.1187997811246,10.0646128046414));
#65211=CARTESIAN_POINT('Ctrl Pts',(1.92611530259251,3.67584468641558,9.99831738797475));
#65212=CARTESIAN_POINT('Ctrl Pts',(2.83274145133105,2.737767367237,9.93202197130808));
#65213=CARTESIAN_POINT('Ctrl Pts',(3.73936760006958,1.79969004805842,9.86572655464141));
#65214=CARTESIAN_POINT('Ctrl Pts',(4.13369556543631,0.366490504410305,9.79943113797476));
#65215=CARTESIAN_POINT('Ctrl Pts',(3.83454946698936,-0.903340839555381,
9.73313572130809));
#65216=CARTESIAN_POINT('Ctrl Pts',(3.5354033685424,-2.17317218352107,9.66684030464142));
#65217=CARTESIAN_POINT('Ctrl Pts',(2.54278320628176,-3.27963532780432,9.60054488797475));
#65218=CARTESIAN_POINT('Ctrl Pts',(1.31275308835322,-3.71436045857372,9.53424947130808));
#65219=CARTESIAN_POINT('Ctrl Pts',(0.0827229704247114,-4.14908558934312,
9.46795405464141));
#65220=CARTESIAN_POINT('Ctrl Pts',(-1.38471710317168,-3.9120727065987,9.40165863797475));
#65221=CARTESIAN_POINT('Ctrl Pts',(-2.41534473209911,-3.11221851937135,
9.33536322130809));
#65222=CARTESIAN_POINT('Ctrl Pts',(-3.35432073684664,-2.3834937423295,9.27496332155038));
#65223=CARTESIAN_POINT('Ctrl Pts',(-3.9307195927702,-1.18758127887811,9.21456342179267));
#65224=CARTESIAN_POINT('Ctrl Pts',(-3.93821611579729,0.00204091754689266,
9.15416352203497));
#65225=CARTESIAN_POINT('Ctrl Pts',(-3.92998043343738,0.00319075123336177,
8.97083647796505));
#65226=CARTESIAN_POINT('Ctrl Pts',(-3.92309598486073,-0.892190824441041,
9.01605256054785));
#65227=CARTESIAN_POINT('Ctrl Pts',(-3.61940103242935,-1.7917966653998,9.06126864313065));
#65228=CARTESIAN_POINT('Ctrl Pts',(-3.05858836669887,-2.48269665568713,
9.10648472571345));
#65229=CARTESIAN_POINT('Ctrl Pts',(-2.24013006686625,-3.49100632121223,
9.17247374546499));
#65230=CARTESIAN_POINT('Ctrl Pts',(-0.874038926052342,-4.05479516214657,
9.23846276521654));
#65231=CARTESIAN_POINT('Ctrl Pts',(0.417330244931444,-3.91721596899267,
9.30445178496809));
#65232=CARTESIAN_POINT('Ctrl Pts',(1.70869941591521,-3.77963677583877,9.37044080471963));
#65233=CARTESIAN_POINT('Ctrl Pts',(2.92534661706887,-2.94068954859666,9.43642982447118));
#65234=CARTESIAN_POINT('Ctrl Pts',(3.51299972402516,-1.78257634340435,9.50241884422273));
#65235=CARTESIAN_POINT('Ctrl Pts',(4.10065283098146,-0.624463138212041,
9.56840786397428));
#65236=CARTESIAN_POINT('Ctrl Pts',(4.0593118437404,0.852816044930448,9.63439688372583));
#65237=CARTESIAN_POINT('Ctrl Pts',(3.40781061717775,1.97625207868741,9.70038590347737));
#65238=CARTESIAN_POINT('Ctrl Pts',(2.75630939061511,3.09968811244436,9.76637492322892));
#65239=CARTESIAN_POINT('Ctrl Pts',(1.49464792473085,3.86928099681577,9.83236394298046));
#65240=CARTESIAN_POINT('Ctrl Pts',(0.197605646350524,3.93442467072329,9.89835296273201));
#65241=CARTESIAN_POINT('Ctrl Pts',(-1.09943663202981,3.99956834463081,9.96434198248356));
#65242=CARTESIAN_POINT('Ctrl Pts',(-2.4318597229062,3.36026280807446,10.0303310022351));
#65243=CARTESIAN_POINT('Ctrl Pts',(-3.19264708406683,2.30775866971944,10.0963200219866));
#65244=CARTESIAN_POINT('Ctrl Pts',(-3.67116379448099,1.6457592153455,10.1378255073128));
#65245=CARTESIAN_POINT('Ctrl Pts',(-3.92353549711722,0.820294119899656,
10.1793309926389));
#65246=CARTESIAN_POINT('Ctrl Pts',(-3.92831996318525,-0.00248455515896013,
10.2208364779651));
#65247=CARTESIAN_POINT('Origin',(0.,0.,0.));
#65248=CARTESIAN_POINT('',(-3.92906811331088,-0.00297329045681721,11.654163522035));
#65249=CARTESIAN_POINT('',(-3.93883030069056,-0.00132569677973748,11.4708364779651));
#65250=CARTESIAN_POINT('',(-3.933,-4.81653586104654E-16,0.));
#65251=CARTESIAN_POINT('Ctrl Pts',(-3.92906811331088,-0.00297329045681721,
11.654163522035));
#65252=CARTESIAN_POINT('Ctrl Pts',(-3.92301413618412,0.862565781599686,
11.6104796717927));
#65253=CARTESIAN_POINT('Ctrl Pts',(-3.64143222706962,1.73168447743578,11.5667958215504));
#65254=CARTESIAN_POINT('Ctrl Pts',(-3.11523612143517,2.41145147056757,11.5231119713081));
#65255=CARTESIAN_POINT('Ctrl Pts',(-2.31667120836259,3.44307839438409,11.4568165546414));
#65256=CARTESIAN_POINT('Ctrl Pts',(-0.954719260784739,4.0385969656079,11.3905211379748));
#65257=CARTESIAN_POINT('Ctrl Pts',(0.344864347868389,3.92439331219059,11.3242257213081));
#65258=CARTESIAN_POINT('Ctrl Pts',(1.64444795652151,3.81018965877329,11.2579303046414));
#65259=CARTESIAN_POINT('Ctrl Pts',(2.88166322624992,2.98626378071489,11.1916348879748));
#65260=CARTESIAN_POINT('Ctrl Pts',(3.48806565025659,1.8311723858493,11.1253394713081));
#65261=CARTESIAN_POINT('Ctrl Pts',(4.09446807426328,0.676080990983685,11.0590440546414));
#65262=CARTESIAN_POINT('Ctrl Pts',(4.07005765254821,-0.810175920689126,
10.9927486379747));
#65263=CARTESIAN_POINT('Ctrl Pts',(3.42604987078477,-1.94473046206733,10.9264532213081));
#65264=CARTESIAN_POINT('Ctrl Pts',(2.78204208902133,-3.07928500344552,10.8601578046414));
#65265=CARTESIAN_POINT('Ctrl Pts',(1.51843694720952,-3.86213717452911,10.7938623879748));
#65266=CARTESIAN_POINT('Ctrl Pts',(0.215803905812841,-3.9336017797221,10.7275669713081));
#65267=CARTESIAN_POINT('Ctrl Pts',(-1.08682913558383,-4.00506638491508,
10.6612715546414));
#65268=CARTESIAN_POINT('Ctrl Pts',(-2.42849007656536,-3.36514342421749,
10.5949761379748));
#65269=CARTESIAN_POINT('Ctrl Pts',(-3.19274634428412,-2.30784858001068,
10.5286807213081));
#65270=CARTESIAN_POINT('Ctrl Pts',(-3.67122612849879,-1.64590542000571,
10.487174988217));
#65271=CARTESIAN_POINT('Ctrl Pts',(-3.92338251028428,-0.820366381532528,
10.445669255126));
#65272=CARTESIAN_POINT('Ctrl Pts',(-3.92814797210457,0.00249985979813405,
10.404163522035));
#65273=CARTESIAN_POINT('Ctrl Pts',(-3.92831996318525,-0.00248455515896013,
10.2208364779651));
#65274=CARTESIAN_POINT('Ctrl Pts',(-3.93114225616083,-0.487830765593514,
10.2453200123905));
#65275=CARTESIAN_POINT('Ctrl Pts',(-3.84781252523088,-0.972242192165111,
10.2698035468159));
#65276=CARTESIAN_POINT('Ctrl Pts',(-3.67392952307573,-1.42161434311076,
10.2942870812413));
#65277=CARTESIAN_POINT('Ctrl Pts',(-3.20527296947916,-2.63278047743221,
10.3602761009928));
#65278=CARTESIAN_POINT('Ctrl Pts',(-2.07880823084118,-3.58941000592143,
10.4262651207444));
#65279=CARTESIAN_POINT('Ctrl Pts',(-0.807722698804678,-3.85568794418083,
10.4922541404959));
#65280=CARTESIAN_POINT('Ctrl Pts',(0.463362833231834,-4.12196588244023,
10.5582431602475));
#65281=CARTESIAN_POINT('Ctrl Pts',(1.87906915866685,-3.69789223046981,10.624232179999));
#65282=CARTESIAN_POINT('Ctrl Pts',(2.79443810742862,-2.77666367153396,10.6902211997506));
#65283=CARTESIAN_POINT('Ctrl Pts',(3.70980705619038,-1.85543511259812,10.7562102195021));
#65284=CARTESIAN_POINT('Ctrl Pts',(4.12483862827887,-0.437051646696854,
10.8221992392537));
#65285=CARTESIAN_POINT('Ctrl Pts',(3.85045547167055,0.832308922064393,10.8881882590052));
#65286=CARTESIAN_POINT('Ctrl Pts',(3.57607231506224,2.10166949082563,10.9541772787568));
#65287=CARTESIAN_POINT('Ctrl Pts',(2.61227442975715,3.22200716244686,11.0201662985083));
#65288=CARTESIAN_POINT('Ctrl Pts',(1.39814251297149,3.68292587415053,11.0861553182599));
#65289=CARTESIAN_POINT('Ctrl Pts',(0.184010596185846,4.1438445858542,11.1521443380114));
#65290=CARTESIAN_POINT('Ctrl Pts',(-1.28045535208038,3.94534433764033,11.2181333577629));
#65291=CARTESIAN_POINT('Ctrl Pts',(-2.32808357370425,3.17785656613293,11.2841223775145));
#65292=CARTESIAN_POINT('Ctrl Pts',(-3.31616190220804,2.45399478123114,11.346360410998));
#65293=CARTESIAN_POINT('Ctrl Pts',(-3.9334439337259,1.22399246925214,11.4085984444815));
#65294=CARTESIAN_POINT('Ctrl Pts',(-3.93883030069056,-0.00132569677973748,
11.4708364779651));
#65295=CARTESIAN_POINT('Origin',(0.,0.,0.));
#65296=CARTESIAN_POINT('',(-3.93896652246607,-0.00134093135676028,12.904163522035));
#65297=CARTESIAN_POINT('',(-3.93205478066481,0.0035322142048073,12.7208364779651));
#65298=CARTESIAN_POINT('',(-3.933,-4.81653586104654E-16,0.));
#65299=CARTESIAN_POINT('Ctrl Pts',(-3.93896652246607,-0.00134093135676028,
12.904163522035));
#65300=CARTESIAN_POINT('Ctrl Pts',(-3.93353066281598,1.23055890227001,12.841585505126));
#65301=CARTESIAN_POINT('Ctrl Pts',(-3.30894493164482,2.46720899017099,12.779007488217));
#65302=CARTESIAN_POINT('Ctrl Pts',(-2.31183883771011,3.18985822187321,12.7164294713081));
#65303=CARTESIAN_POINT('Ctrl Pts',(-1.25550041052026,3.95543588454092,12.6501340546414));
#65304=CARTESIAN_POINT('Ctrl Pts',(0.218931533905592,4.14413118771503,12.5838386379748));
#65305=CARTESIAN_POINT('Ctrl Pts',(1.43402214654648,3.66924716671025,12.5175432213081));
#65306=CARTESIAN_POINT('Ctrl Pts',(2.6491127591874,3.19436314570546,12.4512478046414));
#65307=CARTESIAN_POINT('Ctrl Pts',(3.60486204004333,2.05589980052175,12.3849523879747));
#65308=CARTESIAN_POINT('Ctrl Pts',(3.86214638478224,0.776929591218173,12.3186569713081));
#65309=CARTESIAN_POINT('Ctrl Pts',(4.11943072952114,-0.502040618085386,
12.2523615546414));
#65310=CARTESIAN_POINT('Ctrl Pts',(3.67825013814305,-1.92151769150881,12.1860661379748));
#65311=CARTESIAN_POINT('Ctrl Pts',(2.74130715547621,-2.82931605985119,12.1197707213081));
#65312=CARTESIAN_POINT('Ctrl Pts',(1.80436417280937,-3.73711442819359,12.0534753046414));
#65313=CARTESIAN_POINT('Ctrl Pts',(0.371658798853772,-4.13323409145493,
11.9871798879748));
#65314=CARTESIAN_POINT('Ctrl Pts',(-0.898545590880796,-3.83567596497744,
11.9208844713081));
#65315=CARTESIAN_POINT('Ctrl Pts',(-2.16874998061535,-3.53811783849996,
11.8545890546414));
#65316=CARTESIAN_POINT('Ctrl Pts',(-3.27645338612888,-2.54688192228365,
11.7882936379748));
#65317=CARTESIAN_POINT('Ctrl Pts',(-3.71271614960198,-1.3173963259709,11.7219982213081));
#65318=CARTESIAN_POINT('Ctrl Pts',(-3.86151353184563,-0.898052174796522,
11.6993866548837));
#65319=CARTESIAN_POINT('Ctrl Pts',(-3.93220176350824,-0.450992274867368,
11.6767750884593));
#65320=CARTESIAN_POINT('Ctrl Pts',(-3.92906811331088,-0.00297329045681721,
11.654163522035));
#65321=CARTESIAN_POINT('Ctrl Pts',(-3.93883030069056,-0.00132569677973748,
11.4708364779651));
#65322=CARTESIAN_POINT('Ctrl Pts',(-3.93915492837218,-0.0751736536879503,
11.4745874642331));
#65323=CARTESIAN_POINT('Ctrl Pts',(-3.93725698015438,-0.149004596470233,
11.4783384505011));
#65324=CARTESIAN_POINT('Ctrl Pts',(-3.93308367658131,-0.222706699664195,
11.4820894367691));
#65325=CARTESIAN_POINT('Ctrl Pts',(-3.85966506285299,-1.51930689915301,
11.5480784565207));
#65326=CARTESIAN_POINT('Ctrl Pts',(-3.08203734041481,-2.77603200332971,
11.6140674762722));
#65327=CARTESIAN_POINT('Ctrl Pts',(-1.95446702898915,-3.42035146054613,
11.6800564960238));
#65328=CARTESIAN_POINT('Ctrl Pts',(-0.826896717563501,-4.06467091776254,
11.7460455157753));
#65329=CARTESIAN_POINT('Ctrl Pts',(0.650616182849622,-4.0965847280187,11.8120345355269));
#65330=CARTESIAN_POINT('Ctrl Pts',(1.80495606953855,-3.50155380768333,11.8780235552784));
#65331=CARTESIAN_POINT('Ctrl Pts',(2.9592959562275,-2.90652288734796,11.94401257503));
#65332=CARTESIAN_POINT('Ctrl Pts',(3.79046282919224,-1.68454723642106,12.0100015947815));
#65333=CARTESIAN_POINT('Ctrl Pts',(3.91979915488898,-0.392326479347616,
12.075990614533));
#65334=CARTESIAN_POINT('Ctrl Pts',(4.04913548058573,0.899894277725841,12.1419796342846));
#65335=CARTESIAN_POINT('Ctrl Pts',(3.47664125901443,2.26236014094584,12.2079686540361));
#65336=CARTESIAN_POINT('Ctrl Pts',(2.46312963968748,3.07436787960692,12.2739576737877));
#65337=CARTESIAN_POINT('Ctrl Pts',(1.44961802036054,3.88637561826799,12.3399466935392));
#65338=CARTESIAN_POINT('Ctrl Pts',(-0.00491099672205467,4.14792523237016,
12.4059357132908));
#65339=CARTESIAN_POINT('Ctrl Pts',(-1.23781265514471,3.73986167014628,12.4719247330423));
#65340=CARTESIAN_POINT('Ctrl Pts',(-2.47071431356738,3.33179810792238,12.5379137527939));
#65341=CARTESIAN_POINT('Ctrl Pts',(-3.48198861333012,2.25412136937241,12.6039027725454));
#65342=CARTESIAN_POINT('Ctrl Pts',(-3.81092586479075,0.997792330164229,
12.669891792297));
#65343=CARTESIAN_POINT('Ctrl Pts',(-3.89557431561527,0.674489613847985,
12.6868733541863));
#65344=CARTESIAN_POINT('Ctrl Pts',(-3.93503604178621,0.339355922885629,
12.7038549160757));
#65345=CARTESIAN_POINT('Ctrl Pts',(-3.93205478066481,0.0035322142048073,
12.7208364779651));
#65346=CARTESIAN_POINT('Origin',(0.,0.,0.));
#65347=CARTESIAN_POINT('',(-3.93316249357423,0.00362678856332621,14.154163522035));
#65348=CARTESIAN_POINT('',(-3.92715970428353,-0.00147643720250167,13.9708364779651));
#65349=CARTESIAN_POINT('',(-3.933,-4.81653586104654E-16,0.));
#65350=CARTESIAN_POINT('Ctrl Pts',(-3.93316249357423,0.00362678856332621,
14.154163522035));
#65351=CARTESIAN_POINT('Ctrl Pts',(-3.93594260249156,0.303541798933824,
14.138986755126));
#65352=CARTESIAN_POINT('Ctrl Pts',(-3.90455172321724,0.602880753633413,
14.123809988217));
#65353=CARTESIAN_POINT('Ctrl Pts',(-3.83679646632876,0.89374893743381,14.1086332213081));
#65354=CARTESIAN_POINT('Ctrl Pts',(-3.54082677701855,2.16432438711924,14.0423378046414));
#65355=CARTESIAN_POINT('Ctrl Pts',(-2.55097665652956,3.27326632209662,13.9760423879748));
#65356=CARTESIAN_POINT('Ctrl Pts',(-1.32203750399143,3.71106603622693,13.9097469713081));
#65357=CARTESIAN_POINT('Ctrl Pts',(-0.0930983514533078,4.14886575035724,
13.8434515546414));
#65358=CARTESIAN_POINT('Ctrl Pts',(1.37492983313397,3.91552324364048,13.7771561379748));
#65359=CARTESIAN_POINT('Ctrl Pts',(2.40755443900989,3.11824885318679,13.7108607213081));
#65360=CARTESIAN_POINT('Ctrl Pts',(3.44017904488582,2.32097446273309,13.6445653046414));
#65361=CARTESIAN_POINT('Ctrl Pts',(4.03740007205041,0.959768188542436,13.5782698879748));
#65362=CARTESIAN_POINT('Ctrl Pts',(3.92482144688428,-0.339957199179704,
13.5119744713081));
#65363=CARTESIAN_POINT('Ctrl Pts',(3.81224282171815,-1.63968258690184,13.4456790546414));
#65364=CARTESIAN_POINT('Ctrl Pts',(2.98986454422134,-2.87792708815543,13.3793836379748));
#65365=CARTESIAN_POINT('Ctrl Pts',(1.83553226970559,-3.48577331076856,13.3130882213081));
#65366=CARTESIAN_POINT('Ctrl Pts',(0.681199995189843,-4.09361953338168,
13.2467928046414));
#65367=CARTESIAN_POINT('Ctrl Pts',(-0.805086276344844,-4.0710674773543,
13.1804973879748));
#65368=CARTESIAN_POINT('Ctrl Pts',(-1.94044516826687,-3.42847879330567,
13.1142019713081));
#65369=CARTESIAN_POINT('Ctrl Pts',(-3.07580406018889,-2.78589010925704,
13.0479065546414));
#65370=CARTESIAN_POINT('Ctrl Pts',(-3.86023557249827,-1.52326479718716,
12.9816111379748));
#65371=CARTESIAN_POINT('Ctrl Pts',(-3.93332887367604,-0.220722130071536,
12.9153157213081));
#65372=CARTESIAN_POINT('Ctrl Pts',(-3.93742745294064,-0.147684323861175,
12.9115983215504));
#65373=CARTESIAN_POINT('Ctrl Pts',(-3.93928943559665,-0.0745210091099791,
12.9078809217927));
#65374=CARTESIAN_POINT('Ctrl Pts',(-3.93896652246607,-0.00134093135676028,
12.904163522035));
#65375=CARTESIAN_POINT('Ctrl Pts',(-3.93205478066481,0.0035322142048073,
12.7208364779651));
#65376=CARTESIAN_POINT('Ctrl Pts',(-3.92345109451774,-0.965628712188094,
12.7698439358273));
#65377=CARTESIAN_POINT('Ctrl Pts',(-3.56135912009011,-1.94053648152827,
12.8188513936894));
#65378=CARTESIAN_POINT('Ctrl Pts',(-2.91172602776107,-2.65341233514967,
12.8678588515516));
#65379=CARTESIAN_POINT('Ctrl Pts',(-2.03698873611219,-3.61330662138906,
12.9338478713032));
#65380=CARTESIAN_POINT('Ctrl Pts',(-0.640913949655874,-4.09811385400143,
12.9998368910547));
#65381=CARTESIAN_POINT('Ctrl Pts',(0.640483768856276,-3.8869687447801,13.0658259108062));
#65382=CARTESIAN_POINT('Ctrl Pts',(1.92188148736843,-3.67582363555876,13.1318149305578));
#65383=CARTESIAN_POINT('Ctrl Pts',(3.08860213793641,-2.76872618450373,13.1978039503093));
#65384=CARTESIAN_POINT('Ctrl Pts',(3.60911880551019,-1.57892587817744,13.2637929700609));
#65385=CARTESIAN_POINT('Ctrl Pts',(4.12963547308396,-0.389125571851176,
13.3297819898124));
#65386=CARTESIAN_POINT('Ctrl Pts',(4.00394815766355,1.08337758974633,13.395771009564));
#65387=CARTESIAN_POINT('Ctrl Pts',(3.28931665917947,2.16775030774074,13.4617600293155));
#65388=CARTESIAN_POINT('Ctrl Pts',(2.5746851606954,3.25212302573516,13.5277490490671));
#65389=CARTESIAN_POINT('Ctrl Pts',(1.27110947914766,3.94836530012648,13.5937380688186));
#65390=CARTESIAN_POINT('Ctrl Pts',(-0.0275359561305553,3.93928765796377,
13.6597270885702));
#65391=CARTESIAN_POINT('Ctrl Pts',(-1.32618139140878,3.93021001580106,13.7257161083217));
#65392=CARTESIAN_POINT('Ctrl Pts',(-2.61989658041747,3.21581245708433,13.7917051280733));
#65393=CARTESIAN_POINT('Ctrl Pts',(-3.31929927211619,2.12155551970592,13.8576941478248));
#65394=CARTESIAN_POINT('Ctrl Pts',(-3.71902259246606,1.49616470906661,13.8954082578716));
#65395=CARTESIAN_POINT('Ctrl Pts',(-3.92462191057852,0.746698057506936,
13.9331223679183));
#65396=CARTESIAN_POINT('Ctrl Pts',(-3.92715970428353,-0.00147643720250167,
13.9708364779651));
#65397=CARTESIAN_POINT('Origin',(0.,0.,0.));
#65398=CARTESIAN_POINT('',(-3.92651200951893,-0.000303167493754808,15.404163522035));
#65399=CARTESIAN_POINT('',(-3.937381585586,-0.00245136677763253,15.2208364779651));
#65400=CARTESIAN_POINT('',(-3.933,-4.81653586104654E-16,0.));
#65401=CARTESIAN_POINT('Ctrl Pts',(-3.92651200951893,-0.000303167493754808,
15.404163522035));
#65402=CARTESIAN_POINT('Ctrl Pts',(-3.92604892251585,0.675869111194285,
15.3700925884593));
#65403=CARTESIAN_POINT('Ctrl Pts',(-3.76041551457725,1.3522540035424,15.3360216548837));
#65404=CARTESIAN_POINT('Ctrl Pts',(-3.43090235579558,1.93615684080429,15.3019507213081));
#65405=CARTESIAN_POINT('Ctrl Pts',(-2.78973377407503,3.07231830826751,15.2356553046414));
#65406=CARTESIAN_POINT('Ctrl Pts',(-1.5280902657161,3.85832793543452,15.1693598879748));
#65407=CARTESIAN_POINT('Ctrl Pts',(-0.225640009256706,3.93304981832414,
15.1030644713081));
#65408=CARTESIAN_POINT('Ctrl Pts',(1.07681024720271,4.00777170121378,15.0367690546414));
#65409=CARTESIAN_POINT('Ctrl Pts',(2.42006725176258,3.37120583982601,14.9704736379748));
#65410=CARTESIAN_POINT('Ctrl Pts',(3.18696511248698,2.31582548111636,14.9041782213081));
#65411=CARTESIAN_POINT('Ctrl Pts',(3.95386297321136,1.26044512240672,14.8378828046414));
#65412=CARTESIAN_POINT('Ctrl Pts',(4.14440169010027,-0.213749733624791,
14.7715873879748));
#65413=CARTESIAN_POINT('Ctrl Pts',(3.67103733317019,-1.42943316936038,14.7052919713081));
#65414=CARTESIAN_POINT('Ctrl Pts',(3.1976729762401,-2.64511660509598,14.6389965546414));
#65415=CARTESIAN_POINT('Ctrl Pts',(2.06040554549099,-3.60228862053565,14.5727011379748));
#65416=CARTESIAN_POINT('Ctrl Pts',(0.781758032342482,-3.86117192909937,
14.5064057213081));
#65417=CARTESIAN_POINT('Ctrl Pts',(-0.49688948080601,-4.12005523766308,
14.4401103046414));
#65418=CARTESIAN_POINT('Ctrl Pts',(-1.9169170763539,-3.68064983935086,14.3738148879748));
#65419=CARTESIAN_POINT('Ctrl Pts',(-2.82588624506214,-2.74484265799801,
14.3075194713081));
#65420=CARTESIAN_POINT('Ctrl Pts',(-3.52676843137341,-2.02326638697389,
14.2564008215504));
#65421=CARTESIAN_POINT('Ctrl Pts',(-3.92379848245872,-1.00655215561986,
14.2052821717927));
#65422=CARTESIAN_POINT('Ctrl Pts',(-3.93316249357423,0.00362678856332621,
14.154163522035));
#65423=CARTESIAN_POINT('Ctrl Pts',(-3.92715970428353,-0.00147643720250167,
13.9708364779651));
#65424=CARTESIAN_POINT('Ctrl Pts',(-3.92906233138436,-0.562395580067438,
13.9991113876699));
#65425=CARTESIAN_POINT('Ctrl Pts',(-3.81682903223787,-1.12258843310771,
14.0273862973747));
#65426=CARTESIAN_POINT('Ctrl Pts',(-3.58669355618862,-1.6292252192563,14.0556612070795));
#65427=CARTESIAN_POINT('Ctrl Pts',(-3.0495949541736,-2.81163270479997,14.121650226831));
#65428=CARTESIAN_POINT('Ctrl Pts',(-1.87030755575485,-3.70233135984722,
14.1876392465825));
#65429=CARTESIAN_POINT('Ctrl Pts',(-0.586083352258435,-3.89554255338986,
14.2536282663341));
#65430=CARTESIAN_POINT('Ctrl Pts',(0.698140851238002,-4.08875374693251,
14.3196172860856));
#65431=CARTESIAN_POINT('Ctrl Pts',(2.08730185981211,-3.58447747897051,14.3856063058372));
#65432=CARTESIAN_POINT('Ctrl Pts',(2.94853484413587,-2.61244861269697,14.4515953255887));
#65433=CARTESIAN_POINT('Ctrl Pts',(3.8097678284596,-1.64041974642346,14.5175843453403));
#65434=CARTESIAN_POINT('Ctrl Pts',(4.14307278853302,-0.200638281838427,
14.5835733650918));
#65435=CARTESIAN_POINT('Ctrl Pts',(3.79660484433925,1.05096961754631,14.6495623848434));
#65436=CARTESIAN_POINT('Ctrl Pts',(3.45013690014547,2.30257751693109,14.7155514045949));
#65437=CARTESIAN_POINT('Ctrl Pts',(2.42389605168447,3.36601185111556,14.7815404243465));
#65438=CARTESIAN_POINT('Ctrl Pts',(1.18541035034992,3.7568002052743,14.847529444098));
#65439=CARTESIAN_POINT('Ctrl Pts',(-0.0530753509846368,4.14758855943303,
14.9135184638496));
#65440=CARTESIAN_POINT('Ctrl Pts',(-1.50380590519273,3.86573093356604,14.9795074836011));
#65441=CARTESIAN_POINT('Ctrl Pts',(-2.50586703457503,3.03963416978028,15.0454965033527));
#65442=CARTESIAN_POINT('Ctrl Pts',(-3.39339536200238,2.30795797003797,15.1039431615568));
#65443=CARTESIAN_POINT('Ctrl Pts',(-3.9289562489058,1.14934281299856,15.1623898197609));
#65444=CARTESIAN_POINT('Ctrl Pts',(-3.937381585586,-0.00245136677763253,
15.2208364779651));
#65445=CARTESIAN_POINT('Origin',(0.,0.,0.));
#65446=CARTESIAN_POINT('',(-3.93427892592546,-0.0035228168194773,16.654163522035));
#65447=CARTESIAN_POINT('',(-3.93429847074092,0.00343138669546231,16.4708364779651));
#65448=CARTESIAN_POINT('',(-3.933,-4.81653586104654E-16,0.));
#65449=CARTESIAN_POINT('Ctrl Pts',(-3.93427892592546,-0.0035228168194773,
16.654163522035));
#65450=CARTESIAN_POINT('Ctrl Pts',(-3.92458523529087,1.04238322102138,16.6011984217927));
#65451=CARTESIAN_POINT('Ctrl Pts',(-3.49510551886889,2.09531909947515,16.5482333215504));
#65452=CARTESIAN_POINT('Ctrl Pts',(-2.74837386927502,2.82245201232602,16.4952682213081));
#65453=CARTESIAN_POINT('Ctrl Pts',(-1.81370395226269,3.73259056033171,16.4289728046414));
#65454=CARTESIAN_POINT('Ctrl Pts',(-0.381993636524734,4.13229175872001,
16.3626773879748));
#65455=CARTESIAN_POINT('Ctrl Pts',(0.888950886713486,3.83791096929153,16.2963819713081));
#65456=CARTESIAN_POINT('Ctrl Pts',(2.15989540995167,3.54353017986306,16.2300865546414));
#65457=CARTESIAN_POINT('Ctrl Pts',(3.27007414069013,2.55506740261785,16.1637911379748));
#65458=CARTESIAN_POINT('Ctrl Pts',(3.70941012102833,1.32667661515893,16.0974957213081));
#65459=CARTESIAN_POINT('Ctrl Pts',(4.14874610136655,0.0982858276999579,
16.0312003046414));
#65460=CARTESIAN_POINT('Ctrl Pts',(3.91723933130444,-1.37003296997274,15.9649048879748));
#65461=CARTESIAN_POINT('Ctrl Pts',(3.1212567099161,-2.40365364351869,15.8986094713081));
#65462=CARTESIAN_POINT('Ctrl Pts',(2.32527408852779,-3.4372743170646,15.8323140546414));
#65463=CARTESIAN_POINT('Ctrl Pts',(0.964815615813289,-4.03619686648378,
15.7660186379748));
#65464=CARTESIAN_POINT('Ctrl Pts',(-0.335049519007167,-3.92524344557252,
15.6997232213081));
#65465=CARTESIAN_POINT('Ctrl Pts',(-1.63491465382764,-3.81429002466125,
15.6334278046414));
#65466=CARTESIAN_POINT('Ctrl Pts',(-2.87418645075407,-2.99346063341953,
15.5671323879748));
#65467=CARTESIAN_POINT('Ctrl Pts',(-3.48347552167619,-1.83988928391893,
15.5008369713081));
#65468=CARTESIAN_POINT('Ctrl Pts',(-3.77963514100862,-1.27916816147398,
15.468612488217));
#65469=CARTESIAN_POINT('Ctrl Pts',(-3.92694999984484,-0.639830761090415,
15.436388005126));
#65470=CARTESIAN_POINT('Ctrl Pts',(-3.92651200951893,-0.000303167493754808,
15.404163522035));
#65471=CARTESIAN_POINT('Ctrl Pts',(-3.937381585586,-0.00245136677763253,
15.2208364779651));
#65472=CARTESIAN_POINT('Ctrl Pts',(-3.93846884938094,-0.151086864494689,
15.2283788395125));
#65473=CARTESIAN_POINT('Ctrl Pts',(-3.9307776674093,-0.299608771734014,
15.2359212010599));
#65474=CARTESIAN_POINT('Ctrl Pts',(-3.91393159770783,-0.447084924292802,
15.2434635626073));
#65475=CARTESIAN_POINT('Ctrl Pts',(-3.76654332690187,-1.73737135287563,
15.3094525823588));
#65476=CARTESIAN_POINT('Ctrl Pts',(-2.91837508073346,-2.94760830833676,
15.3754416021104));
#65477=CARTESIAN_POINT('Ctrl Pts',(-1.75582976645362,-3.52644400385163,
15.4414306218619));
#65478=CARTESIAN_POINT('Ctrl Pts',(-0.593284452173774,-4.10527969936651,
15.5074196416135));
#65479=CARTESIAN_POINT('Ctrl Pts',(0.883637930217515,-4.05271413493511,
15.573408661365));
#65480=CARTESIAN_POINT('Ctrl Pts',(2.00209080232236,-3.39269478443345,15.6393976811166));
#65481=CARTESIAN_POINT('Ctrl Pts',(3.1205436744272,-2.73267543393178,15.7053867008681));
#65482=CARTESIAN_POINT('Ctrl Pts',(3.88052703624564,-1.46520229735984,15.7713757206197));
#65483=CARTESIAN_POINT('Ctrl Pts',(3.93581266973757,-0.167702444224742,
15.8373647403712));
#65484=CARTESIAN_POINT('Ctrl Pts',(3.99109830322949,1.12979740891036,15.9033537601228));
#65485=CARTESIAN_POINT('Ctrl Pts',(3.34168620839496,2.45732397860861,15.9693427798743));
#65486=CARTESIAN_POINT('Ctrl Pts',(2.28343127320179,3.21009144754939,16.0353317996259));
#65487=CARTESIAN_POINT('Ctrl Pts',(1.22517633800864,3.96285891649017,16.1013208193774));
#65488=CARTESIAN_POINT('Ctrl Pts',(-0.241921437543155,4.14086728467346,
16.167309839129));
#65489=CARTESIAN_POINT('Ctrl Pts',(-1.44949130477761,3.66302067130938,16.2332988588805));
#65490=CARTESIAN_POINT('Ctrl Pts',(-2.65706117201209,3.18517405794529,16.299287878632));
#65491=CARTESIAN_POINT('Ctrl Pts',(-3.60510313092923,2.05147246303385,16.3652768983836));
#65492=CARTESIAN_POINT('Ctrl Pts',(-3.86171446555683,0.778400197568591,
16.4312659181351));
#65493=CARTESIAN_POINT('Ctrl Pts',(-3.91300711095021,0.523932699601581,
16.4444561047451));
#65494=CARTESIAN_POINT('Ctrl Pts',(-3.93667444784825,0.26389680817035,16.4576462913551));
#65495=CARTESIAN_POINT('Ctrl Pts',(-3.93429847074092,0.00343138669546231,
16.4708364779651));
#65496=CARTESIAN_POINT('Origin',(0.,0.,0.));
#65497=CARTESIAN_POINT('',(-3.93834707504816,0.00194035199596952,17.904163522035));
#65498=CARTESIAN_POINT('',(-3.9266456040214,-0.000298839343342066,17.7208364779651));
#65499=CARTESIAN_POINT('',(-3.933,-4.81653586104654E-16,0.));
#65500=CARTESIAN_POINT('Ctrl Pts',(-3.93834707504816,0.00194035199596952,
17.904163522035));
#65501=CARTESIAN_POINT('Ctrl Pts',(-3.93900955662444,0.111515013993062,
17.8985996717927));
#65502=CARTESIAN_POINT('Ctrl Pts',(-3.93483467582154,0.221038430779974,
17.8930358215504));
#65503=CARTESIAN_POINT('Ctrl Pts',(-3.92565930759555,0.330141315023366,
17.8874719713081));
#65504=CARTESIAN_POINT('Ctrl Pts',(-3.81633126440203,1.63014416475303,17.8211765546414));
#65505=CARTESIAN_POINT('Ctrl Pts',(-2.99705204268746,2.87044131989379,17.7548811379748));
#65506=CARTESIAN_POINT('Ctrl Pts',(-1.84424342167773,3.48117228657177,17.6885857213081));
#65507=CARTESIAN_POINT('Ctrl Pts',(-0.691434800668018,4.09190325324974,
17.6222903046414));
#65508=CARTESIAN_POINT('Ctrl Pts',(0.794903219636835,4.07306803146494,17.5559948879748));
#65509=CARTESIAN_POINT('Ctrl Pts',(1.93186548638391,3.43332055446555,17.4896994713081));
#65510=CARTESIAN_POINT('Ctrl Pts',(3.06882775313098,2.79357307746616,17.4234040546414));
#65511=CARTESIAN_POINT('Ctrl Pts',(3.85641426632028,1.53291334525214,17.3571086379748));
#65512=CARTESIAN_POINT('Ctrl Pts',(3.93276461410269,0.230557535679648,17.2908132213081));
#65513=CARTESIAN_POINT('Ctrl Pts',(4.0091149618851,-1.07179827389284,17.2245178046414));
#65514=CARTESIAN_POINT('Ctrl Pts',(3.37422914426067,-2.41585016082385,17.1582223879748));
#65515=CARTESIAN_POINT('Ctrl Pts',(2.31980850399665,-3.18406702064856,17.0919269713081));
#65516=CARTESIAN_POINT('Ctrl Pts',(1.26538786373261,-3.95228388047328,17.0256315546414));
#65517=CARTESIAN_POINT('Ctrl Pts',(-0.208567599171001,-4.14466571319169,
16.9593361379748));
#65518=CARTESIAN_POINT('Ctrl Pts',(-1.42484195742051,-3.67282176038683,
16.8930407213081));
#65519=CARTESIAN_POINT('Ctrl Pts',(-2.64111631566999,-3.20097780758199,
16.8267453046414));
#65520=CARTESIAN_POINT('Ctrl Pts',(-3.59970956926536,-2.06490806925393,
16.7604498879748));
#65521=CARTESIAN_POINT('Ctrl Pts',(-3.86019143691972,-0.78658525127837,
16.6941544713081));
#65522=CARTESIAN_POINT('Ctrl Pts',(-3.9125676929753,-0.52954715554103,16.6808241548837));
#65523=CARTESIAN_POINT('Ctrl Pts',(-3.93671864496475,-0.266757633157094,
16.6674938384594));
#65524=CARTESIAN_POINT('Ctrl Pts',(-3.93427892592546,-0.0035228168194773,
16.654163522035));
#65525=CARTESIAN_POINT('Ctrl Pts',(-3.93429847074092,0.00343138669546231,
16.4708364779651));
#65526=CARTESIAN_POINT('Ctrl Pts',(-3.92478770167089,-1.03918239385564,
16.5236353111066));
#65527=CARTESIAN_POINT('Ctrl Pts',(-3.4979820902233,-2.08867858084047,16.5764341442482));
#65528=CARTESIAN_POINT('Ctrl Pts',(-2.75534870673093,-2.8154571538885,16.6292329773898));
#65529=CARTESIAN_POINT('Ctrl Pts',(-1.82719090293942,-3.72379930386122,
16.6952219971413));
#65530=CARTESIAN_POINT('Ctrl Pts',(-0.405694585018322,-4.12804066778764,
16.7612110168929));
#65531=CARTESIAN_POINT('Ctrl Pts',(0.861544310291354,-3.84401962566144,
16.8272000366444));
#65532=CARTESIAN_POINT('Ctrl Pts',(2.12878320560107,-3.55999858353522,16.893189056396));
#65533=CARTESIAN_POINT('Ctrl Pts',(3.24176467829938,-2.58771513535637,16.9591780761475));
#65534=CARTESIAN_POINT('Ctrl Pts',(3.69344395429821,-1.37011577522619,17.0251670958991));
#65535=CARTESIAN_POINT('Ctrl Pts',(4.14512323029704,-0.152516415096028,
17.0911561156506));
#65536=CARTESIAN_POINT('Ctrl Pts',(3.93550030959638,1.31039885698542,17.1571451354021));
#65537=CARTESIAN_POINT('Ctrl Pts',(3.16007382274637,2.35216472974554,17.2231341551537));
#65538=CARTESIAN_POINT('Ctrl Pts',(2.38464733589636,3.39393060250563,17.2891231749052));
#65539=CARTESIAN_POINT('Ctrl Pts',(1.04341728289697,4.0145470759444,17.3551121946568));
#65540=CARTESIAN_POINT('Ctrl Pts',(-0.252587576200152,3.93127778176702,
17.4211012144083));
#65541=CARTESIAN_POINT('Ctrl Pts',(-1.5485924352973,3.84800848758964,17.4870902341599));
#65542=CARTESIAN_POINT('Ctrl Pts',(-2.79937210049219,3.06085342579612,17.5530792539114));
#65543=CARTESIAN_POINT('Ctrl Pts',(-3.43510460409732,1.92841951866681,17.619068273663));
#65544=CARTESIAN_POINT('Ctrl Pts',(-3.76191329414888,1.34627334923204,17.6529910084304));
#65545=CARTESIAN_POINT('Ctrl Pts',(-3.92618702824121,0.672882336433972,
17.6869137431977));
#65546=CARTESIAN_POINT('Ctrl Pts',(-3.9266456040214,-0.000298839343342066,
17.7208364779651));
#65547=CARTESIAN_POINT('Origin',(0.,0.,0.));
#65548=CARTESIAN_POINT('',(-3.9282768393018,0.00257866899793263,19.154163522035));
#65549=CARTESIAN_POINT('',(-3.93538156611592,-0.00321517502500232,18.9708364779651));
#65550=CARTESIAN_POINT('',(-3.933,-4.81653586104654E-16,0.));
#65551=CARTESIAN_POINT('Ctrl Pts',(-3.9282768393018,0.00257866899793263,
19.154163522035));
#65552=CARTESIAN_POINT('Ctrl Pts',(-3.93117933039081,0.487427862220609,
19.129705505126));
#65553=CARTESIAN_POINT('Ctrl Pts',(-3.84811414897009,0.971317557029167,
19.1052474882171));
#65554=CARTESIAN_POINT('Ctrl Pts',(-3.67460044557047,1.42024851790461,19.0807894713081));
#65555=CARTESIAN_POINT('Ctrl Pts',(-3.20427763456445,2.63711189716341,19.0144940546414));
#65556=CARTESIAN_POINT('Ctrl Pts',(-2.06940736477127,3.5971248902646,18.9481986379748));
#65557=CARTESIAN_POINT('Ctrl Pts',(-0.791411240478813,3.8592049097762,18.8819032213081));
#65558=CARTESIAN_POINT('Ctrl Pts',(0.48658488381363,4.1212849292878,18.8156078046414));
#65559=CARTESIAN_POINT('Ctrl Pts',(1.90770686260538,3.68543197520983,18.7493123879748));
#65560=CARTESIAN_POINT('Ctrl Pts',(2.81901336701189,2.75190078378659,18.6830169713081));
#65561=CARTESIAN_POINT('Ctrl Pts',(3.7303198714184,1.81836959236335,18.6167215546414));
#65562=CARTESIAN_POINT('Ctrl Pts',(4.1318109014397,0.387160163594836,18.5504261379748));
#65563=CARTESIAN_POINT('Ctrl Pts',(3.83901947212335,-0.884151446221029,
18.4841307213081));
#65564=CARTESIAN_POINT('Ctrl Pts',(3.546228042807,-2.15546305603691,18.4178353046414));
#65565=CARTESIAN_POINT('Ctrl Pts',(2.55915415415299,-3.26687684690014,18.3515398879748));
#65566=CARTESIAN_POINT('Ctrl Pts',(1.33131365222046,-3.70774840659508,18.2852444713081));
#65567=CARTESIAN_POINT('Ctrl Pts',(0.103473150287937,-4.14861996629002,
18.2189490546414));
#65568=CARTESIAN_POINT('Ctrl Pts',(-1.36513396492305,-3.91894929481668,
18.1526536379748));
#65569=CARTESIAN_POINT('Ctrl Pts',(-2.39974909019232,-3.12425968692074,
18.0863582213081));
#65570=CARTESIAN_POINT('Ctrl Pts',(-3.34753402561069,-2.39626449305453,
18.0256266548837));
#65571=CARTESIAN_POINT('Ctrl Pts',(-3.93111583371302,-1.1941092492171,17.9648950884594));
#65572=CARTESIAN_POINT('Ctrl Pts',(-3.93834707504816,0.00194035199596952,
17.904163522035));
#65573=CARTESIAN_POINT('Ctrl Pts',(-3.9266456040214,-0.000298839343342066,
17.7208364779651));
#65574=CARTESIAN_POINT('Ctrl Pts',(-3.92707908386185,-0.636639617187392,
17.7529027629493));
#65575=CARTESIAN_POINT('Ctrl Pts',(-3.7811366333853,-1.2727928965762,17.7849690479334));
#65576=CARTESIAN_POINT('Ctrl Pts',(-3.48773693817145,-1.83151208873438,
17.8170353329176));
#65577=CARTESIAN_POINT('Ctrl Pts',(-2.88395142662511,-2.98129703654113,
17.8830243526692));
#65578=CARTESIAN_POINT('Ctrl Pts',(-1.65569506151712,-3.80315417968951,
17.9490133724207));
#65579=CARTESIAN_POINT('Ctrl Pts',(-0.362528793721696,-3.92266725007212,
18.0150023921723));
#65580=CARTESIAN_POINT('Ctrl Pts',(0.930637474073712,-4.04218032045474,
18.0809914119238));
#65581=CARTESIAN_POINT('Ctrl Pts',(2.28871364455655,-3.45934931807162,18.1469804316753));
#65582=CARTESIAN_POINT('Ctrl Pts',(3.0929963143472,-2.4396965550044,18.2129694514269));
#65583=CARTESIAN_POINT('Ctrl Pts',(3.89727898413784,-1.4200437919372,18.2789584711784));
#65584=CARTESIAN_POINT('Ctrl Pts',(4.1477681532363,0.0364307318140862,18.34494749093));
#65585=CARTESIAN_POINT('Ctrl Pts',(3.73034761461436,1.26619593871039,18.4109365106815));
#65586=CARTESIAN_POINT('Ctrl Pts',(3.3129270759924,2.49596114560672,18.4769255304331));
#65587=CARTESIAN_POINT('Ctrl Pts',(2.22759682964998,3.49901703564806,18.5429145501846));
#65588=CARTESIAN_POINT('Ctrl Pts',(0.96880448596242,3.8183980082025,18.6089035699362));
#65589=CARTESIAN_POINT('Ctrl Pts',(-0.289987857725137,4.13777898075694,
18.6748925896877));
#65590=CARTESIAN_POINT('Ctrl Pts',(-1.72224229875783,3.77348503582448,18.7408816094393));
#65591=CARTESIAN_POINT('Ctrl Pts',(-2.67546178547362,2.89147881118572,18.8068706291908));
#65592=CARTESIAN_POINT('Ctrl Pts',(-3.46496405315379,2.16095879542366,18.8615259121156));
#65593=CARTESIAN_POINT('Ctrl Pts',(-3.92585074558825,1.07529075325076,18.9161811950403));
#65594=CARTESIAN_POINT('Ctrl Pts',(-3.93538156611592,-0.00321517502500232,
18.9708364779651));
#65595=CARTESIAN_POINT('Origin',(0.,0.,0.));
#65596=CARTESIAN_POINT('',(-3.92891717919508,-0.00290821770756955,20.404163522035));
#65597=CARTESIAN_POINT('',(-3.93645074190752,0.00287690968989754,20.2208364779651));
#65598=CARTESIAN_POINT('',(-3.933,-4.81653586104654E-16,0.));
#65599=CARTESIAN_POINT('Ctrl Pts',(-3.92891717919508,-0.00290821770756955,
20.404163522035));
#65600=CARTESIAN_POINT('Ctrl Pts',(-3.92305522360385,0.856142276174852,
20.3608113384593));
#65601=CARTESIAN_POINT('Ctrl Pts',(-3.64607827536016,1.71863158079485,20.3174591548837));
#65602=CARTESIAN_POINT('Ctrl Pts',(-3.12725777950586,2.39584078513516,20.2741069713081));
#65603=CARTESIAN_POINT('Ctrl Pts',(-2.33386242750779,3.43144874462641,20.2078115546414));
#65604=CARTESIAN_POINT('Ctrl Pts',(-0.974905937332626,4.03377152685725,
20.1415161379748));
#65605=CARTESIAN_POINT('Ctrl Pts',(0.325232594901768,3.92606903230323,20.0752207213081));
#65606=CARTESIAN_POINT('Ctrl Pts',(1.62537112713614,3.8183665377492,20.0089253046414));
#65607=CARTESIAN_POINT('Ctrl Pts',(2.86669170142975,3.00063876641033,19.9426298879748));
#65608=CARTESIAN_POINT('Ctrl Pts',(3.47886360905618,1.84859467617474,19.8763344713081));
#65609=CARTESIAN_POINT('Ctrl Pts',(4.09103551668261,0.696550585939142,19.8100390546414));
#65610=CARTESIAN_POINT('Ctrl Pts',(4.07405875764185,-0.789809823193177,
19.7437436379748));
#65611=CARTESIAN_POINT('Ctrl Pts',(3.43573338553496,-1.92757111171479,19.6774482213081));
#65612=CARTESIAN_POINT('Ctrl Pts',(2.79740801342808,-3.06533240023639,19.6111528046414));
#65613=CARTESIAN_POINT('Ctrl Pts',(1.5377340282551,-3.8544945681473,19.5448573879748));
#65614=CARTESIAN_POINT('Ctrl Pts',(0.23547470165254,-3.93247326145755,19.4785619713081));
#65615=CARTESIAN_POINT('Ctrl Pts',(-1.06678462495002,-4.01045195476781,
19.4122665546415));
#65616=CARTESIAN_POINT('Ctrl Pts',(-2.41162929298214,-3.37724717347741,
19.3459711379748));
#65617=CARTESIAN_POINT('Ctrl Pts',(-3.18116395088876,-2.32378790012402,
19.2796757213081));
#65618=CARTESIAN_POINT('Ctrl Pts',(-3.66679826362155,-1.65897577639373,
19.2378383215504));
#65619=CARTESIAN_POINT('Ctrl Pts',(-3.92331189547844,-0.82679476690109,
19.1960009217927));
#65620=CARTESIAN_POINT('Ctrl Pts',(-3.9282768393018,0.00257866899793263,
19.154163522035));
#65621=CARTESIAN_POINT('Ctrl Pts',(-3.93538156611592,-0.00321517502500232,
18.9708364779651));
#65622=CARTESIAN_POINT('Ctrl Pts',(-3.93735794983994,-0.226862400015945,
18.9821702147919));
#65623=CARTESIAN_POINT('Ctrl Pts',(-3.91992542781245,-0.450201644536789,
18.9935039516187));
#65624=CARTESIAN_POINT('Ctrl Pts',(-3.88198951431208,-0.670002158083677,
19.0048376884455));
#65625=CARTESIAN_POINT('Ctrl Pts',(-3.66111322403586,-1.94975839836931,
19.070826708197));
#65626=CARTESIAN_POINT('Ctrl Pts',(-2.74517611108449,-3.10955237459557,
19.1368157279486));
#65627=CARTESIAN_POINT('Ctrl Pts',(-1.55145477700773,-3.62101278042009,
19.2028047477001));
#65628=CARTESIAN_POINT('Ctrl Pts',(-0.357733442930951,-4.13247318624461,
19.2687937674516));
#65629=CARTESIAN_POINT('Ctrl Pts',(1.11377211227119,-3.99560002166745,19.3347827872032));
#65630=CARTESIAN_POINT('Ctrl Pts',(2.19268307268018,-3.27274906215669,19.4007718069548));
#65631=CARTESIAN_POINT('Ctrl Pts',(3.27159403308916,-2.54989810264594,19.4667608267063));
#65632=CARTESIAN_POINT('Ctrl Pts',(3.9579103987049,-1.24106934820161,19.5327498464579));
#65633=CARTESIAN_POINT('Ctrl Pts',(3.93896467676769,0.0574696114667197,
19.5987388662094));
#65634=CARTESIAN_POINT('Ctrl Pts',(3.92001895483048,1.35600857113501,19.6647278859609));
#65635=CARTESIAN_POINT('Ctrl Pts',(3.19581114534032,2.64425773602735,19.7307169057125));
#65636=CARTESIAN_POINT('Ctrl Pts',(2.09627107566941,3.33532503039472,19.796705925464));
#65637=CARTESIAN_POINT('Ctrl Pts',(0.996731005998481,4.0263923247621,19.8626949452156));
#65638=CARTESIAN_POINT('Ctrl Pts',(-0.47814132385321,4.12027774860455,19.9286839649671));
#65639=CARTESIAN_POINT('Ctrl Pts',(-1.65643328493112,3.57420959844803,19.9946729847187));
#65640=CARTESIAN_POINT('Ctrl Pts',(-2.83472524600906,3.02814144829149,20.0606620044702));
#65641=CARTESIAN_POINT('Ctrl Pts',(-3.71643683831319,1.84211972413594,20.1266510242218));
#65642=CARTESIAN_POINT('Ctrl Pts',(-3.89988369773019,0.556464397103722,
20.1926400439733));
#65643=CARTESIAN_POINT('Ctrl Pts',(-3.92601202070485,0.373348601469244,
20.2020388553039));
#65644=CARTESIAN_POINT('Ctrl Pts',(-3.93797514673285,0.188211610232611,
20.2114376666345));
#65645=CARTESIAN_POINT('Ctrl Pts',(-3.93645074190752,0.00287690968989754,
20.2208364779651));
#65646=CARTESIAN_POINT('Origin',(0.,0.,0.));
#65647=CARTESIAN_POINT('',(-3.93886994768263,-0.00145307456529742,21.654163522035));
#65648=CARTESIAN_POINT('',(-3.92682300552281,0.000912804021836195,21.4708364779651));
#65649=CARTESIAN_POINT('',(-3.933,-4.81653586104654E-16,0.));
#65650=CARTESIAN_POINT('Ctrl Pts',(-3.93886994768263,-0.00145307456529742,
21.654163522035));
#65651=CARTESIAN_POINT('Ctrl Pts',(-3.93307041227624,1.22399755147868,21.5919171717927));
#65652=CARTESIAN_POINT('Ctrl Pts',(-3.31597754125522,2.45448525381708,21.5296708215504));
#65653=CARTESIAN_POINT('Ctrl Pts',(-2.3277636632771,3.17825590774622,21.4674244713081));
#65654=CARTESIAN_POINT('Ctrl Pts',(-1.27526740379634,3.94910716065609,21.4011290546414));
#65655=CARTESIAN_POINT('Ctrl Pts',(0.198202360151425,4.14517431985207,21.3348336379748));
#65656=CARTESIAN_POINT('Ctrl Pts',(1.41565285799402,3.67637338594032,21.2685382213081));
#65657=CARTESIAN_POINT('Ctrl Pts',(2.63310335583664,3.20757245202857,21.2022428046414));
#65658=CARTESIAN_POINT('Ctrl Pts',(3.59453458757408,2.07390342500907,21.1359473879748));
#65659=CARTESIAN_POINT('Ctrl Pts',(3.85821234921109,0.796235992399213,21.0696519713081));
#65660=CARTESIAN_POINT('Ctrl Pts',(4.1218901108481,-0.481431440210624,21.0033565546414));
#65661=CARTESIAN_POINT('Ctrl Pts',(3.6878144023847,-1.90309727841081,20.9370611379748));
#65662=CARTESIAN_POINT('Ctrl Pts',(2.75542339601885,-2.81557031449561,20.8707657213081));
#65663=CARTESIAN_POINT('Ctrl Pts',(1.823032389653,-3.72804335058041,20.8044703046414));
#65664=CARTESIAN_POINT('Ctrl Pts',(0.392326085384676,-4.13132358454981,
20.7381748879748));
#65665=CARTESIAN_POINT('Ctrl Pts',(-0.879350623459857,-3.84012197309118,
20.6718794713081));
#65666=CARTESIAN_POINT('Ctrl Pts',(-2.15102733230437,-3.54892036163256,
20.6055840546414));
#65667=CARTESIAN_POINT('Ctrl Pts',(-3.26367444572511,-2.56323690474595,
20.5392886379748));
#65668=CARTESIAN_POINT('Ctrl Pts',(-3.70608089552499,-1.33594860792683,
20.4729932213081));
#65669=CARTESIAN_POINT('Ctrl Pts',(-3.85918701973527,-0.91121394481419,
20.4500499882171));
#65670=CARTESIAN_POINT('Ctrl Pts',(-3.93201949613523,-0.457542658063658,
20.427106755126));
#65671=CARTESIAN_POINT('Ctrl Pts',(-3.92891717919508,-0.00290821770756955,
20.404163522035));
#65672=CARTESIAN_POINT('Ctrl Pts',(-3.93645074190752,0.00287690968989754,
20.2208364779651));
#65673=CARTESIAN_POINT('Ctrl Pts',(-3.92727230606611,-1.11302263999166,
20.277426686386));
#65674=CARTESIAN_POINT('Ctrl Pts',(-3.42913855164522,-2.23608962586235,
20.334016894807));
#65675=CARTESIAN_POINT('Ctrl Pts',(-2.58996741576936,-2.96830157940845,
20.390607103228));
#65676=CARTESIAN_POINT('Ctrl Pts',(-1.61142214786158,-3.82212329897966,
20.4565961229795));
#65677=CARTESIAN_POINT('Ctrl Pts',(-0.169149485516115,-4.14447780821319,
20.522585142731));
#65678=CARTESIAN_POINT('Ctrl Pts',(1.0797894842757,-3.78850896141388,20.5885741624826));
#65679=CARTESIAN_POINT('Ctrl Pts',(2.32872845406747,-3.43254011461459,20.6545631822341));
#65680=CARTESIAN_POINT('Ctrl Pts',(3.3843337313056,-2.39824791178247,20.7205522019857));
#65681=CARTESIAN_POINT('Ctrl Pts',(3.7656996114002,-1.15682838734449,20.7865412217372));
#65682=CARTESIAN_POINT('Ctrl Pts',(4.14706549149481,0.0845911370935058,
20.8525302414888));
#65683=CARTESIAN_POINT('Ctrl Pts',(3.85419197444593,1.53313798313737,20.9185192612403));
#65684=CARTESIAN_POINT('Ctrl Pts',(3.0205044495625,2.52889271248087,20.9845082809919));
#65685=CARTESIAN_POINT('Ctrl Pts',(2.18681692467907,3.52464744182437,21.0504973007434));
#65686=CARTESIAN_POINT('Ctrl Pts',(0.812315391961076,4.06761005446749,21.116486320495));
#65687=CARTESIAN_POINT('Ctrl Pts',(-0.476813786790554,3.91042121692691,
21.1824753402465));
#65688=CARTESIAN_POINT('Ctrl Pts',(-1.76594296554219,3.75323237938633,21.2484643599981));
#65689=CARTESIAN_POINT('Ctrl Pts',(-2.96969979032745,2.89589209166208,21.3144533797496));
#65690=CARTESIAN_POINT('Ctrl Pts',(-3.53968464960523,1.72898179933011,21.3804423995011));
#65691=CARTESIAN_POINT('Ctrl Pts',(-3.79994641379366,1.19615688935483,21.4105737589891));
#65692=CARTESIAN_POINT('Ctrl Pts',(-3.92807036204732,0.598788410850091,
21.4407051184771));
#65693=CARTESIAN_POINT('Ctrl Pts',(-3.92682300552281,0.000912804021836195,
21.4708364779651));
#65694=CARTESIAN_POINT('Origin',(0.,0.,0.));
#65695=CARTESIAN_POINT('',(-3.93336305982959,0.00361627372896939,22.904163522035));
#65696=CARTESIAN_POINT('',(-3.93314739898817,-0.00354003882696159,22.7208364779651));
#65697=CARTESIAN_POINT('',(-3.933,-4.81653586104654E-16,0.));
#65698=CARTESIAN_POINT('Ctrl Pts',(-3.93336305982959,0.00361627372896939,
22.904163522035));
#65699=CARTESIAN_POINT('Ctrl Pts',(-3.93608756649877,0.296938794665777,
22.8893184217927));
#65700=CARTESIAN_POINT('Ctrl Pts',(-3.90606924847603,0.589708845978146,
22.8744733215504));
#65701=CARTESIAN_POINT('Ctrl Pts',(-3.84121847047142,0.874548425935453,
22.8596282213081));
#65702=CARTESIAN_POINT('Ctrl Pts',(-3.55160713213065,2.14658824568881,22.7933328046414));
#65703=CARTESIAN_POINT('Ctrl Pts',(-2.56731564801377,3.26046694217167,22.7270373879748));
#65704=CARTESIAN_POINT('Ctrl Pts',(-1.34058147503169,3.70440759042506,22.6607419713081));
#65705=CARTESIAN_POINT('Ctrl Pts',(-0.113847302049577,4.14834823867847,
22.5944465546415));
#65706=CARTESIAN_POINT('Ctrl Pts',(1.35532955979775,3.92235083870236,22.5281511379748));
#65707=CARTESIAN_POINT('Ctrl Pts',(2.39192873445742,3.13025098298425,22.4618557213081));
#65708=CARTESIAN_POINT('Ctrl Pts',(3.42852790911707,2.33815112726615,22.3955603046414));
#65709=CARTESIAN_POINT('Ctrl Pts',(4.03254939658908,0.979948815806054,22.3292648879748));
#65710=CARTESIAN_POINT('Ctrl Pts',(3.926472619055,-0.320323366316481,22.2629694713081));
#65711=CARTESIAN_POINT('Ctrl Pts',(3.82039584152092,-1.62059554843902,22.1966740546414));
#65712=CARTESIAN_POINT('Ctrl Pts',(3.00422079898074,-2.86293760122399,22.1303786379748));
#65713=CARTESIAN_POINT('Ctrl Pts',(1.85294304060728,-3.47654949273874,22.0640832213081));
#65714=CARTESIAN_POINT('Ctrl Pts',(0.701665282233811,-4.09016138425349,
21.9977878046415));
#65715=CARTESIAN_POINT('Ctrl Pts',(-0.784715191972952,-4.075043114498,21.9314923879748));
#65716=CARTESIAN_POINT('Ctrl Pts',(-1.92327372351062,-3.4381408452317,21.8651969713081));
#65717=CARTESIAN_POINT('Ctrl Pts',(-3.06183225504826,-2.80123857596541,
21.7989015546414));
#65718=CARTESIAN_POINT('Ctrl Pts',(-3.85256884391683,-1.54255230718833,
21.7326061379748));
#65719=CARTESIAN_POINT('Ctrl Pts',(-3.93217576084423,-0.240391499487906,
21.6663107213081));
#65720=CARTESIAN_POINT('Ctrl Pts',(-3.93703784197572,-0.160860577582587,
21.6622616548837));
#65721=CARTESIAN_POINT('Ctrl Pts',(-3.93924720199552,-0.0811674829656328,
21.6582125884594));
#65722=CARTESIAN_POINT('Ctrl Pts',(-3.93886994768263,-0.00145307456529742,
21.654163522035));
#65723=CARTESIAN_POINT('Ctrl Pts',(-3.92682300552281,0.000912804021836195,
21.4708364779651));
#65724=CARTESIAN_POINT('Ctrl Pts',(-3.92533859568391,-0.710585805859282,
21.5066941382286));
#65725=CARTESIAN_POINT('Ctrl Pts',(-3.74063776254721,-1.42280261393549,
21.5425517984922));
#65726=CARTESIAN_POINT('Ctrl Pts',(-3.37738304094838,-2.02781391547153,
21.5784094587558));
#65727=CARTESIAN_POINT('Ctrl Pts',(-2.70888367924349,-3.14121904100145,
21.6443984785073));
#65728=CARTESIAN_POINT('Ctrl Pts',(-1.43567206206342,-3.89154899512166,
21.7103874982589));
#65729=CARTESIAN_POINT('Ctrl Pts',(-0.137789558142141,-3.93697339573595,
21.7763765180104));
#65730=CARTESIAN_POINT('Ctrl Pts',(1.16009294577916,-3.98239779635025,21.842365537762));
#65731=CARTESIAN_POINT('Ctrl Pts',(2.4826463364417,-3.32291664345865,21.9083545575135));
#65732=CARTESIAN_POINT('Ctrl Pts',(3.22735044469825,-2.25897202022772,21.9743435772651));
#65733=CARTESIAN_POINT('Ctrl Pts',(3.97205455295482,-1.19502739699677,22.0403325970166));
#65734=CARTESIAN_POINT('Ctrl Pts',(4.13890937880536,0.273380696573503,22.1063216167682));
#65735=CARTESIAN_POINT('Ctrl Pts',(3.65190029886735,1.47728456574835,22.1723106365197));
#65736=CARTESIAN_POINT('Ctrl Pts',(3.16489121892935,2.68118843492317,22.2382996562713));
#65737=CARTESIAN_POINT('Ctrl Pts',(2.0240182332028,3.62058807970259,22.3042886760228));
#65738=CARTESIAN_POINT('Ctrl Pts',(0.749032747709332,3.86751799270859,22.3702776957744));
#65739=CARTESIAN_POINT('Ctrl Pts',(-0.525952737784169,4.1144479057146,22.4362667155259));
#65740=CARTESIAN_POINT('Ctrl Pts',(-1.93505072304459,3.6689080869472,22.5022557352774));
#65741=CARTESIAN_POINT('Ctrl Pts',(-2.8363136221232,2.73387463465757,22.568244755029));
#65742=CARTESIAN_POINT('Ctrl Pts',(-3.53100120856598,2.01315692523182,22.6191086626744));
#65743=CARTESIAN_POINT('Ctrl Pts',(-3.92397248148655,1.00161997425012,22.6699725703197));
#65744=CARTESIAN_POINT('Ctrl Pts',(-3.93314739898817,-0.00354003882696159,
22.7208364779651));
#65745=CARTESIAN_POINT('Origin',(0.,0.,0.));
#65746=CARTESIAN_POINT('',(-3.92649966780813,-0.000194383930052777,24.154163522035));
#65747=CARTESIAN_POINT('',(-3.93821094167311,0.00191457267368049,23.9708364779651));
#65748=CARTESIAN_POINT('',(-3.933,-4.81653586104654E-16,0.));
#65749=CARTESIAN_POINT('Ctrl Pts',(-3.92649966780813,-0.000194383930052777,
24.154163522035));
#65750=CARTESIAN_POINT('Ctrl Pts',(-3.92620568854956,0.669400878559864,
24.120424255126));
#65751=CARTESIAN_POINT('Ctrl Pts',(-3.76395243069231,1.33912979693549,24.0866849882171));
#65752=CARTESIAN_POINT('Ctrl Pts',(-3.44054292979195,1.9189733284899,24.0529457213081));
#65753=CARTESIAN_POINT('Ctrl Pts',(-2.80506475908943,3.05832732303874,23.9866503046415));
#65754=CARTESIAN_POINT('Ctrl Pts',(-1.54736817451896,3.85063709663954,23.9203548879748));
#65755=CARTESIAN_POINT('Ctrl Pts',(-0.245307921498792,3.93187211272784,
23.8540594713081));
#65756=CARTESIAN_POINT('Ctrl Pts',(1.05675233152134,4.01310712881613,23.7877640546414));
#65757=CARTESIAN_POINT('Ctrl Pts',(2.40317625299117,3.38326738739196,23.7214686379748));
#65758=CARTESIAN_POINT('Ctrl Pts',(3.1753428957673,2.33173578724029,23.6551732213081));
#65759=CARTESIAN_POINT('Ctrl Pts',(3.94750953854344,1.28020418708861,23.5888778046414));
#65760=CARTESIAN_POINT('Ctrl Pts',(4.14541890262589,-0.193019271790565,
23.5225823879748));
#65761=CARTESIAN_POINT('Ctrl Pts',(3.67814057872457,-1.41105498487359,23.4562869713081));
#65762=CARTESIAN_POINT('Ctrl Pts',(3.21086225482324,-2.62909069795662,23.3899915546414));
#65763=CARTESIAN_POINT('Ctrl Pts',(2.07839624293814,-3.59193866524351,23.3236961379748));
#65764=CARTESIAN_POINT('Ctrl Pts',(0.801059499496516,-3.85721375677617,
23.2574007213081));
#65765=CARTESIAN_POINT('Ctrl Pts',(-0.476277243945107,-4.12248884830884,
23.1911053046414));
#65766=CARTESIAN_POINT('Ctrl Pts',(-1.89848471894325,-3.69019106408728,
23.1248098879748));
#65767=CARTESIAN_POINT('Ctrl Pts',(-2.81212286016002,-2.75894170046458,
23.0585144713081));
#65768=CARTESIAN_POINT('Ctrl Pts',(-3.52117597161916,-2.03622093276366,
23.0070641548837));
#65769=CARTESIAN_POINT('Ctrl Pts',(-3.92392043378181,-1.01298423891683,
22.9556138384594));
#65770=CARTESIAN_POINT('Ctrl Pts',(-3.93336305982959,0.00361627372896939,
22.904163522035));
#65771=CARTESIAN_POINT('Ctrl Pts',(-3.93314739898817,-0.00354003882696159,
22.7208364779651));
#65772=CARTESIAN_POINT('Ctrl Pts',(-3.9358756922358,-0.302438778350537,
22.7359615900713));
#65773=CARTESIAN_POINT('Ctrl Pts',(-3.90466658238743,-0.60077363364454,
22.7510867021775));
#65774=CARTESIAN_POINT('Ctrl Pts',(-3.83736180721441,-0.890729948748711,
22.7662118142836));
#65775=CARTESIAN_POINT('Ctrl Pts',(-3.54371928033023,-2.15577399405356,
22.8322008340352));
#65776=CARTESIAN_POINT('Ctrl Pts',(-2.56300641366511,-3.26133499885145,
22.8981898537867));
#65777=CARTESIAN_POINT('Ctrl Pts',(-1.34200992031493,-3.7037487569815,22.9641788735383));
#65778=CARTESIAN_POINT('Ctrl Pts',(-0.121013426964719,-4.14616251511156,
23.0301678932898));
#65779=CARTESIAN_POINT('Ctrl Pts',(1.34026669307056,-3.92542902657374,23.0961569130414));
#65780=CARTESIAN_POINT('Ctrl Pts',(2.37611006032544,-3.14210860128767,23.1621459327929));
#65781=CARTESIAN_POINT('Ctrl Pts',(3.41195342758027,-2.35878817600163,23.2281349525445));
#65782=CARTESIAN_POINT('Ctrl Pts',(4.02236004205474,-1.01288081396738,23.294123972296));
#65783=CARTESIAN_POINT('Ctrl Pts',(3.92924487580339,0.282453867097757,23.3601129920475));
#65784=CARTESIAN_POINT('Ctrl Pts',(3.83612970955204,1.57778854816291,23.4261020117991));
#65785=CARTESIAN_POINT('Ctrl Pts',(3.03949276257486,2.82255054825896,23.4920910315506));
#65786=CARTESIAN_POINT('Ctrl Pts',(1.9022606519978,3.44965938795798,23.5580800513022));
#65787=CARTESIAN_POINT('Ctrl Pts',(0.765028541420735,4.076768227657,23.6240690710537));
#65788=CARTESIAN_POINT('Ctrl Pts',(-0.712798732756265,4.08622390695897,
23.6900580908053));
#65789=CARTESIAN_POINT('Ctrl Pts',(-1.85796234749118,3.47371866972136,23.7560471105568));
#65790=CARTESIAN_POINT('Ctrl Pts',(-3.00312596222609,2.86121343248376,23.8220361303084));
#65791=CARTESIAN_POINT('Ctrl Pts',(-3.81562591751894,1.62674727870669,23.8880251500599));
#65792=CARTESIAN_POINT('Ctrl Pts',(-3.92530883132,0.332710173915526,23.9540141698115));
#65793=CARTESIAN_POINT('Ctrl Pts',(-3.93462916866347,0.222748996429926,
23.9596216058627));
#65794=CARTESIAN_POINT('Ctrl Pts',(-3.93887460484717,0.112357669032555,
23.9652290419139));
#65795=CARTESIAN_POINT('Ctrl Pts',(-3.93821094167311,0.00191457267368049,
23.9708364779651));
#65796=CARTESIAN_POINT('Origin',(0.,0.,0.));
#65797=CARTESIAN_POINT('',(-3.93407891385469,-0.00354965325188361,25.404163522035));
#65798=CARTESIAN_POINT('',(-3.92767634141232,0.00202018669269811,25.2208364779651));
#65799=CARTESIAN_POINT('',(-3.933,-4.81653586104654E-16,0.));
#65800=CARTESIAN_POINT('Ctrl Pts',(-3.93407891385469,-0.00354965325188361,
25.404163522035));
#65801=CARTESIAN_POINT('Ctrl Pts',(-3.9244242454102,1.0359427451275,25.3515300884594));
#65802=CARTESIAN_POINT('Ctrl Pts',(-3.50088813201609,2.08238911627919,25.2988966548837));
#65803=CARTESIAN_POINT('Ctrl Pts',(-2.76245569162327,2.80867100939486,25.2462632213081));
#65804=CARTESIAN_POINT('Ctrl Pts',(-1.83234942664463,3.72347282737578,25.1799678046414));
#65805=CARTESIAN_POINT('Ctrl Pts',(-0.40265608081936,4.13032957499881,25.1136723879748));
#65806=CARTESIAN_POINT('Ctrl Pts',(0.869744861155389,3.84230896254983,25.0473769713081));
#65807=CARTESIAN_POINT('Ctrl Pts',(2.14214580313014,3.55428835010084,24.9810815546414));
#65808=CARTESIAN_POINT('Ctrl Pts',(3.25725434125437,2.57139037757985,24.9147861379748));
#65809=CARTESIAN_POINT('Ctrl Pts',(3.70272849391131,1.34521224629211,24.8484907213081));
#65810=CARTESIAN_POINT('Ctrl Pts',(4.14820264656826,0.119034115004331,24.7821953046414));
#65811=CARTESIAN_POINT('Ctrl Pts',(3.92404241375788,-1.3504241750502,24.7158998879748));
#65812=CARTESIAN_POINT('Ctrl Pts',(3.13323929267643,-2.38801294427511,24.6496044713081));
#65813=CARTESIAN_POINT('Ctrl Pts',(2.342436171595,-3.42560171349998,24.5833090546414));
#65814=CARTESIAN_POINT('Ctrl Pts',(0.984990162242543,-4.03132096189525,
24.5170136379748));
#65815=CARTESIAN_POINT('Ctrl Pts',(-0.31541363694263,-3.92687006721989,
24.4507182213081));
#65816=CARTESIAN_POINT('Ctrl Pts',(-1.6158174361278,-3.82241917254453,24.3844228046415));
#65817=CARTESIAN_POINT('Ctrl Pts',(-2.85917902514569,-3.00779813479854,
24.3181273879748));
#65818=CARTESIAN_POINT('Ctrl Pts',(-3.47422994123735,-1.85728850817714,
24.2518319713081));
#65819=CARTESIAN_POINT('Ctrl Pts',(-3.77626725753592,-1.29229977162088,
24.2192758215504));
#65820=CARTESIAN_POINT('Ctrl Pts',(-3.92678333825044,-0.64630930105307,
24.1867196717927));
#65821=CARTESIAN_POINT('Ctrl Pts',(-3.92649966780813,-0.000194383930052777,
24.154163522035));
#65822=CARTESIAN_POINT('Ctrl Pts',(-3.93821094167311,0.00191457267368049,
23.9708364779651));
#65823=CARTESIAN_POINT('Ctrl Pts',(-3.93106453231111,-1.18735071827648,
24.0312180616654));
#65824=CARTESIAN_POINT('Ctrl Pts',(-3.3546954866468,-2.38261875282536,24.0915996453658));
#65825=CARTESIAN_POINT('Ctrl Pts',(-2.41612259034546,-3.11144614439781,
24.1519812290661));
#65826=CARTESIAN_POINT('Ctrl Pts',(-1.39038756326069,-3.90795730211473,
24.2179702488177));
#65827=CARTESIAN_POINT('Ctrl Pts',(0.0679483632180516,-4.14737156174339,
24.2839592685692));
#65828=CARTESIAN_POINT('Ctrl Pts',(1.29450610594822,-3.72061815062074,24.3499482883208));
#65829=CARTESIAN_POINT('Ctrl Pts',(2.52106384867842,-3.29386473949807,24.4159373080723));
#65830=CARTESIAN_POINT('Ctrl Pts',(3.51584340766002,-2.20094365762405,24.4819263278238));
#65831=CARTESIAN_POINT('Ctrl Pts',(3.82564965869348,-0.939760698265326,
24.5479153475754));
#65832=CARTESIAN_POINT('Ctrl Pts',(4.13545590972695,0.321422261093383,24.6139043673269));
#65833=CARTESIAN_POINT('Ctrl Pts',(3.76028885281226,1.75086709793682,24.6798933870785));
#65834=CARTESIAN_POINT('Ctrl Pts',(2.871064626524,2.69735674158764,24.74588240683));
#65835=CARTESIAN_POINT('Ctrl Pts',(1.98184040023576,3.64384638523844,24.8118714265816));
#65836=CARTESIAN_POINT('Ctrl Pts',(0.578559004573957,4.10738083569666,24.8778604463331));
#65837=CARTESIAN_POINT('Ctrl Pts',(-0.699481858119317,3.87678611883963,
24.9438494660847));
#65838=CARTESIAN_POINT('Ctrl Pts',(-1.97752272081263,3.64619140198259,25.0098384858362));
#65839=CARTESIAN_POINT('Ctrl Pts',(-3.13032305053739,2.72146751781024,25.0758275055878));
#65840=CARTESIAN_POINT('Ctrl Pts',(-3.63269766039478,1.52389408727378,25.1418165253393));
#65841=CARTESIAN_POINT('Ctrl Pts',(-3.83322404099964,1.04587417778395,25.1681565095479));
#65842=CARTESIAN_POINT('Ctrl Pts',(-3.93012045155741,0.524382140035048,
25.1944964937565));
#65843=CARTESIAN_POINT('Ctrl Pts',(-3.92767634141232,0.00202018669269811,
25.2208364779651));
#65844=CARTESIAN_POINT('Origin',(0.,0.,0.));
#65845=CARTESIAN_POINT('',(-3.93847239432236,0.00183746061217384,26.654163522035));
#65846=CARTESIAN_POINT('',(-3.93096036061645,-0.0034105068734492,26.4708364779651));
#65847=CARTESIAN_POINT('',(-3.933,-4.81653586104654E-16,0.));
#65848=CARTESIAN_POINT('Ctrl Pts',(-3.93847239432236,0.00183746061217384,
26.654163522035));
#65849=CARTESIAN_POINT('Ctrl Pts',(-3.93906782029507,0.104871598938666,
26.6489313384594));
#65850=CARTESIAN_POINT('Ctrl Pts',(-3.93537654477555,0.207862391149194,
26.6436991548837));
#65851=CARTESIAN_POINT('Ctrl Pts',(-3.92726137617655,0.310503414455952,
26.6384669713081));
#65852=CARTESIAN_POINT('Ctrl Pts',(-3.82443652765684,1.61103679767247,26.5721715546415));
#65853=CARTESIAN_POINT('Ctrl Pts',(-3.01137076827103,2.8554159790709,26.5058761379748));
#65854=CARTESIAN_POINT('Ctrl Pts',(-1.86163107209072,3.47190495817833,26.4395807213081));
#65855=CARTESIAN_POINT('Ctrl Pts',(-0.711891375910411,4.08839393728577,
26.3732853046414));
#65856=CARTESIAN_POINT('Ctrl Pts',(0.774522257064396,4.07699271410221,26.3069898879748));
#65857=CARTESIAN_POINT('Ctrl Pts',(1.91466993337585,3.44293963546029,26.2406944713081));
#65858=CARTESIAN_POINT('Ctrl Pts',(3.05481760968731,2.80888655681837,26.1743990546414));
#65859=CARTESIAN_POINT('Ctrl Pts',(3.84869932933542,1.55218162271808,26.1081036379748));
#65860=CARTESIAN_POINT('Ctrl Pts',(3.93156231758308,0.250223959999214,26.0418082213081));
#65861=CARTESIAN_POINT('Ctrl Pts',(4.01442530583075,-1.05173370271969,25.9755128046415));
#65862=CARTESIAN_POINT('Ctrl Pts',(3.38626956267792,-2.39894409405719,25.9092173879748));
#65863=CARTESIAN_POINT('Ctrl Pts',(2.33570426580363,-3.17242491950617,25.8429219713081));
#65864=CARTESIAN_POINT('Ctrl Pts',(1.28513896892936,-3.94590574495512,25.7766265546414));
#65865=CARTESIAN_POINT('Ctrl Pts',(-0.187835881666348,-4.1456570045156,
25.7103311379748));
#65866=CARTESIAN_POINT('Ctrl Pts',(-1.40645490573152,-3.67990202116044,
25.6440357213081));
#65867=CARTESIAN_POINT('Ctrl Pts',(-2.62507392979665,-3.21414703780529,
25.5777403046415));
#65868=CARTESIAN_POINT('Ctrl Pts',(-3.58933712733127,-2.08288581153454,
25.5114448879748));
#65869=CARTESIAN_POINT('Ctrl Pts',(-3.8562091340326,-0.805881754229776,
25.4451494713081));
#65870=CARTESIAN_POINT('Ctrl Pts',(-3.91120540717406,-0.542720155505481,
25.4314874882171));
#65871=CARTESIAN_POINT('Ctrl Pts',(-3.93658496197046,-0.273369169197457,
25.417825505126));
#65872=CARTESIAN_POINT('Ctrl Pts',(-3.93407891385469,-0.00354965325188361,
25.404163522035));
#65873=CARTESIAN_POINT('Ctrl Pts',(-3.92767634141232,0.00202018669269811,
25.2208364779651));
#65874=CARTESIAN_POINT('Ctrl Pts',(-3.92399727276726,-0.784280499380038,
25.260485513508));
#65875=CARTESIAN_POINT('Ctrl Pts',(-3.69522588961778,-1.57255229767332,
25.300134549051));
#65876=CARTESIAN_POINT('Ctrl Pts',(-3.25599248064403,-2.21748922140678,
25.339783584594));
#65877=CARTESIAN_POINT('Ctrl Pts',(-2.52496380104585,-3.29087612265032,
25.4057726043455));
#65878=CARTESIAN_POINT('Ctrl Pts',(-1.21095755185952,-3.96722694823681,
25.4717616240971));
#65879=CARTESIAN_POINT('Ctrl Pts',(0.0873999482272789,-3.93841424054347,
25.5377506438486));
#65880=CARTESIAN_POINT('Ctrl Pts',(1.38575744831402,-3.90960153285012,25.6037396636002));
#65881=CARTESIAN_POINT('Ctrl Pts',(2.66846619930122,-3.17562529187698,25.6697286833517));
#65882=CARTESIAN_POINT('Ctrl Pts',(3.35115819074181,-2.07086558271892,25.7357177031032));
#65883=CARTESIAN_POINT('Ctrl Pts',(4.03385018218244,-0.966105873560801,
25.8017067228548));
#65884=CARTESIAN_POINT('Ctrl Pts',(4.11652541407643,0.509437303782197,25.8676957426063));
#65885=CARTESIAN_POINT('Ctrl Pts',(3.56151924841617,1.68354570007079,25.9336847623579));
#65886=CARTESIAN_POINT('Ctrl Pts',(3.00651308275592,2.85765409635936,25.9996737821094));
#65887=CARTESIAN_POINT('Ctrl Pts',(1.8138255195414,3.73032771159348,26.065662801861));
#65888=CARTESIAN_POINT('Ctrl Pts',(0.526813308981318,3.90399964376866,26.1316518216125));
#65889=CARTESIAN_POINT('Ctrl Pts',(-0.760198901578725,4.07767157594384,
26.1976408413641));
#65890=CARTESIAN_POINT('Ctrl Pts',(-2.14153575948438,3.55234182506012,26.2636298611156));
#65891=CARTESIAN_POINT('Ctrl Pts',(-2.9878969104734,2.56733666149362,26.3296188808671));
#65892=CARTESIAN_POINT('Ctrl Pts',(-3.59163921219624,1.86469419738052,26.3766914132331));
#65893=CARTESIAN_POINT('Ctrl Pts',(-3.92315787657576,0.928144826430376,
26.4237639455991));
#65894=CARTESIAN_POINT('Ctrl Pts',(-3.93096036061645,-0.0034105068734492,
26.4708364779651));
#65895=CARTESIAN_POINT('Origin',(0.,0.,0.));
#65896=CARTESIAN_POINT('',(-3.92840989342865,0.00265517403989252,27.904163522035));
#65897=CARTESIAN_POINT('',(-3.93924705030466,0.000656224253225424,27.7208364779651));
#65898=CARTESIAN_POINT('',(-3.933,-4.81653586104654E-16,0.));
#65899=CARTESIAN_POINT('Ctrl Pts',(-3.92840989342865,0.00265517403989252,
27.904163522035));
#65900=CARTESIAN_POINT('Ctrl Pts',(-3.93136414635793,0.480888864434302,
27.8800371717927));
#65901=CARTESIAN_POINT('Ctrl Pts',(-3.85060148071847,0.958158959844772,
27.8559108215504));
#65902=CARTESIAN_POINT('Ctrl Pts',(-3.68165771049416,1.40185262775938,27.8317844713081));
#65903=CARTESIAN_POINT('Ctrl Pts',(-3.21742679583935,2.62105305763651,27.7654890546414));
#65904=CARTESIAN_POINT('Ctrl Pts',(-2.08737212377921,3.5867299779047,27.6991936379748));
#65905=CARTESIAN_POINT('Ctrl Pts',(-0.810702749059684,3.85519848255106,
27.6328982213081));
#65906=CARTESIAN_POINT('Ctrl Pts',(0.465966625659809,4.12366698719743,27.5666028046414));
#65907=CARTESIAN_POINT('Ctrl Pts',(1.88925070303869,3.69492707622201,27.5003073879748));
#65908=CARTESIAN_POINT('Ctrl Pts',(2.80521476759667,2.76596536400124,27.4340119713081));
#65909=CARTESIAN_POINT('Ctrl Pts',(3.72117883215465,1.83700365178048,27.3677165546414));
#65910=CARTESIAN_POINT('Ctrl Pts',(4.12982288389174,0.407820138314366,27.3014211379748));
#65911=CARTESIAN_POINT('Ctrl Pts',(3.84339344762151,-0.864939936629703,
27.2351257213081));
#65912=CARTESIAN_POINT('Ctrl Pts',(3.55696401135128,-2.13770001157377,27.1688303046415));
#65913=CARTESIAN_POINT('Ctrl Pts',(2.57546108707372,-3.2540366479958,27.1025348879748));
#65914=CARTESIAN_POINT('Ctrl Pts',(1.34984091446835,-3.70104360860882,27.0362394713081));
#65915=CARTESIAN_POINT('Ctrl Pts',(0.124220741862938,-4.14805056922186,
26.9699440546414));
#65916=CARTESIAN_POINT('Ctrl Pts',(-1.3455166790703,-3.92572785402585,26.9036486379748));
#65917=CARTESIAN_POINT('Ctrl Pts',(-2.38409342071011,-3.13622270391051,
26.8373532213081));
#65918=CARTESIAN_POINT('Ctrl Pts',(-3.34070334710301,-2.40902707814848,
26.7762899882171));
#65919=CARTESIAN_POINT('Ctrl Pts',(-3.9315233577615,-1.20064282587445,26.715226755126));
#65920=CARTESIAN_POINT('Ctrl Pts',(-3.93847239432236,0.00183746061217384,
26.654163522035));
#65921=CARTESIAN_POINT('Ctrl Pts',(-3.93096036061645,-0.0034105068734492,
26.4708364779651));
#65922=CARTESIAN_POINT('Ctrl Pts',(-3.93409585351461,-0.377763740610767,
26.4897529653507));
#65923=CARTESIAN_POINT('Ctrl Pts',(-3.88495439272852,-0.751310486780916,
26.5086694527362));
#65924=CARTESIAN_POINT('Ctrl Pts',(-3.78019431150709,-1.10854699869474,
26.5275859401218));
#65925=CARTESIAN_POINT('Ctrl Pts',(-3.41474511747934,-2.35474491906723,
26.5935749598733));
#65926=CARTESIAN_POINT('Ctrl Pts',(-2.37246128535146,-3.40246018356284,
26.6595639796249));
#65927=CARTESIAN_POINT('Ctrl Pts',(-1.1281796234269,-3.77438156766775,26.7255529993764));
#65928=CARTESIAN_POINT('Ctrl Pts',(0.116102038497622,-4.14630295177265,
26.791542019128));
#65929=CARTESIAN_POINT('Ctrl Pts',(1.56238153021876,-3.84243045548688,26.8575310388795));
#65930=CARTESIAN_POINT('Ctrl Pts',(2.55177235978977,-3.00120031068882,26.9235200586311));
#65931=CARTESIAN_POINT('Ctrl Pts',(3.5411631893608,-2.15997016589073,26.9895090783826));
#65932=CARTESIAN_POINT('Ctrl Pts',(4.07366535678164,-0.78138237258023,27.0554980981342));
#65933=CARTESIAN_POINT('Ctrl Pts',(3.90668502935641,0.506515115735212,27.1214871178857));
#65934=CARTESIAN_POINT('Ctrl Pts',(3.73970470193117,1.79441260405062,27.1874761376373));
#65935=CARTESIAN_POINT('Ctrl Pts',(2.87324187965999,2.99161978737102,27.2534651573888));
#65936=CARTESIAN_POINT('Ctrl Pts',(1.70203399236642,3.55272089670649,27.3194541771404));
#65937=CARTESIAN_POINT('Ctrl Pts',(0.530826105072816,4.11382200604197,27.3854431968919));
#65938=CARTESIAN_POINT('Ctrl Pts',(-0.945126847243146,4.03881704139246,
27.4514322166435));
#65939=CARTESIAN_POINT('Ctrl Pts',(-2.05341993275692,3.36187627089729,27.517421236395));
#65940=CARTESIAN_POINT('Ctrl Pts',(-3.16171301827067,2.68493550040213,27.5834102561465));
#65941=CARTESIAN_POINT('Ctrl Pts',(-3.90234623698222,1.40605892406135,27.6493992758981));
#65942=CARTESIAN_POINT('Ctrl Pts',(-3.93790678169248,0.107868715418545,
27.7153882956496));
#65943=CARTESIAN_POINT('Ctrl Pts',(-3.93888543102711,0.0721416759634396,
27.7172043564214));
#65944=CARTESIAN_POINT('Ctrl Pts',(-3.9393300680325,0.0364000086293204,
27.7190204171933));
#65945=CARTESIAN_POINT('Ctrl Pts',(-3.93924705030466,0.000656224253225424,
27.7208364779651));
#65946=CARTESIAN_POINT('Origin',(0.,0.,0.));
#65947=CARTESIAN_POINT('',(-3.92876997665636,-0.00284051892226578,29.154163522035));
#65948=CARTESIAN_POINT('',(-3.92912953761977,0.00289384936589777,28.9708364779651));
#65949=CARTESIAN_POINT('',(-3.933,-4.81653586104654E-16,0.));
#65950=CARTESIAN_POINT('Ctrl Pts',(-3.92876997665636,-0.00284051892226578,
29.154163522035));
#65951=CARTESIAN_POINT('Ctrl Pts',(-3.92310187586187,0.849718058506195,
29.111143005126));
#65952=CARTESIAN_POINT('Ctrl Pts',(-3.65068494473056,1.70557539765092,29.0681224882171));
#65953=CARTESIAN_POINT('Ctrl Pts',(-3.13920121202234,2.38017016989005,29.0251019713081));
#65954=CARTESIAN_POINT('Ctrl Pts',(-2.35099526717338,3.41973326024983,28.9588065546414));
#65955=CARTESIAN_POINT('Ctrl Pts',(-0.995068227481178,4.02884518692243,
28.8925111379748));
#65956=CARTESIAN_POINT('Ctrl Pts',(0.30559270653279,3.92764654531323,28.8262157213081));
#65957=CARTESIAN_POINT('Ctrl Pts',(1.60625364054687,3.82644790370401,28.7599203046414));
#65958=CARTESIAN_POINT('Ctrl Pts',(2.85164846888267,3.01493869381287,28.6936248879748));
#65959=CARTESIAN_POINT('Ctrl Pts',(3.46957454719653,1.86597072555893,28.6273294713081));
#65960=CARTESIAN_POINT('Ctrl Pts',(4.08750062551035,0.717002757305092,28.5610340546415));
#65961=CARTESIAN_POINT('Ctrl Pts',(4.0779579538023,-0.76942396931155,28.4947386379748));
#65962=CARTESIAN_POINT('Ctrl Pts',(3.44533095848979,-1.9103635448963,28.4284432213081));
#65963=CARTESIAN_POINT('Ctrl Pts',(2.81270396317727,-3.05130312048108,28.3621478046414));
#65964=CARTESIAN_POINT('Ctrl Pts',(1.55699264426028,-3.84675554503403,28.2958523879748));
#65965=CARTESIAN_POINT('Ctrl Pts',(0.255139607303237,-3.9312463758943,28.2295569713081));
#65966=CARTESIAN_POINT('Ctrl Pts',(-1.04671342965381,-4.01573720675458,
28.1632615546415));
#65967=CARTESIAN_POINT('Ctrl Pts',(-2.39470818465087,-3.38926644392217,
28.0969661379748));
#65968=CARTESIAN_POINT('Ctrl Pts',(-3.16950198352466,-2.33966909276295,
28.0306707213081));
#65969=CARTESIAN_POINT('Ctrl Pts',(-3.66233139485763,-1.67204314446506,
27.9885016548837));
#65970=CARTESIAN_POINT('Ctrl Pts',(-3.92324632385603,-0.833222115898168,
27.9463325884593));
#65971=CARTESIAN_POINT('Ctrl Pts',(-3.92840989342865,0.00265517403989252,
27.904163522035));
#65972=CARTESIAN_POINT('Ctrl Pts',(-3.93924705030466,0.000656224253225424,
27.7208364779651));
#65973=CARTESIAN_POINT('Ctrl Pts',(-3.93631350682071,-1.26239864932264,
27.7850094369448));
#65974=CARTESIAN_POINT('Ctrl Pts',(-3.27451985550136,-2.5280969835108,27.8491823959246));
#65975=CARTESIAN_POINT('Ctrl Pts',(-2.23438232319365,-3.24442307889484,
27.9133553549043));
#65976=CARTESIAN_POINT('Ctrl Pts',(-1.16480944927562,-3.98102082362052,
27.9793443746558));
#65977=CARTESIAN_POINT('Ctrl Pts',(0.304824169269371,-4.13671247212701,
28.0453333944074));
#65978=CARTESIAN_POINT('Ctrl Pts',(1.50499252110454,-3.64056904789417,28.1113224141589));
#65979=CARTESIAN_POINT('Ctrl Pts',(2.70516087293964,-3.14442562366137,28.1773114339105));
#65980=CARTESIAN_POINT('Ctrl Pts',(3.63586395806496,-1.9964471266893,28.243300453662));
#65981=CARTESIAN_POINT('Ctrl Pts',(3.87309819051212,-0.719622045046852,
28.3092894734135));
#65982=CARTESIAN_POINT('Ctrl Pts',(4.11033242295931,0.557203036595705,28.3752784931651));
#65983=CARTESIAN_POINT('Ctrl Pts',(3.65409780272822,1.96287470290867,28.4412675129166));
#65984=CARTESIAN_POINT('Ctrl Pts',(2.71224269533156,2.85700630777853,28.5072565326682));
#65985=CARTESIAN_POINT('Ctrl Pts',(1.77038758793493,3.75113791264836,28.5732455524197));
#65986=CARTESIAN_POINT('Ctrl Pts',(0.342911993372745,4.13372945607512,28.6392345721713));
#65987=CARTESIAN_POINT('Ctrl Pts',(-0.919864152115334,3.83048240078438,
28.7052235919229));
#65988=CARTESIAN_POINT('Ctrl Pts',(-2.18264029760341,3.52723534549364,28.7712126116744));
#65989=CARTESIAN_POINT('Ctrl Pts',(-3.28071699401739,2.5381496914854,28.8372016314259));
#65990=CARTESIAN_POINT('Ctrl Pts',(-3.71383968715089,1.31382657120668,28.9031906511775));
#65991=CARTESIAN_POINT('Ctrl Pts',(-3.86183876734026,0.895472376128801,
28.9257392601067));
#65992=CARTESIAN_POINT('Ctrl Pts',(-3.93219744831015,0.449651723668126,
28.9482878690359));
#65993=CARTESIAN_POINT('Ctrl Pts',(-3.92912953761977,0.00289384936589777,
28.9708364779651));
#65994=CARTESIAN_POINT('Origin',(0.,0.,0.));
#65995=CARTESIAN_POINT('',(-3.93876665726707,-0.00156339645701664,30.404163522035));
#65996=CARTESIAN_POINT('',(-3.9290580015118,-0.00286337897428823,30.2208364779651));
#65997=CARTESIAN_POINT('',(-3.933,-4.81653586104654E-16,0.));
#65998=CARTESIAN_POINT('Ctrl Pts',(-3.93876665726707,-0.00156339645701664,
30.404163522035));
#65999=CARTESIAN_POINT('Ctrl Pts',(-3.93262187151115,1.2174425911067,30.3422488384594));
#66000=CARTESIAN_POINT('Ctrl Pts',(-3.32296578001872,2.44175279030972,30.2803341548837));
#66001=CARTESIAN_POINT('Ctrl Pts',(-2.34363026191953,3.16657409239259,30.2184194713081));
#66002=CARTESIAN_POINT('Ctrl Pts',(-1.29500249739966,3.94267965339049,30.1521240546414));
#66003=CARTESIAN_POINT('Ctrl Pts',(0.177468228542797,4.14611376416382,30.0858286379748));
#66004=CARTESIAN_POINT('Ctrl Pts',(1.39724815815262,3.68340764398078,30.0195332213081));
#66005=CARTESIAN_POINT('Ctrl Pts',(2.61702808776238,3.22070152379777,29.9532378046414));
#66006=CARTESIAN_POINT('Ctrl Pts',(3.58411722103958,2.09185517265848,29.8869423879748));
#66007=CARTESIAN_POINT('Ctrl Pts',(3.85418180391149,0.815522476449609,29.8206469713082));
#66008=CARTESIAN_POINT('Ctrl Pts',(4.12424638678342,-0.460810219759336,
29.7543515546415));
#66009=CARTESIAN_POINT('Ctrl Pts',(3.69728641925003,-1.88462926103782,29.6880561379748));
#66010=CARTESIAN_POINT('Ctrl Pts',(2.7694707121116,-2.8017541401688,29.6217607213081));
#66011=CARTESIAN_POINT('Ctrl Pts',(1.84165500497318,-3.71887901929977,29.5554653046414));
#66012=CARTESIAN_POINT('Ctrl Pts',(0.412983558229673,-4.12930973628314,
29.4891698879748));
#66013=CARTESIAN_POINT('Ctrl Pts',(-0.860133659870229,-3.84447192399102,
29.4228744713081));
#66014=CARTESIAN_POINT('Ctrl Pts',(-2.13325087797013,-3.5596341116989,29.3565790546415));
#66015=CARTESIAN_POINT('Ctrl Pts',(-3.25081386742647,-2.57952777013129,
29.2902836379748));
#66016=CARTESIAN_POINT('Ctrl Pts',(-3.69935293715175,-1.35446747232396,
29.2239882213081));
#66017=CARTESIAN_POINT('Ctrl Pts',(-3.85682539015349,-0.924375060777911,
29.2007133215504));
#66018=CARTESIAN_POINT('Ctrl Pts',(-3.93183652460341,-0.464090565480743,
29.1774384217927));
#66019=CARTESIAN_POINT('Ctrl Pts',(-3.92876997665636,-0.00284051892226578,
29.154163522035));
#66020=CARTESIAN_POINT('Ctrl Pts',(-3.92912953761977,0.00289384936589777,
28.9708364779651));
#66021=CARTESIAN_POINT('Ctrl Pts',(-3.92321913750707,-0.857795413495037,
29.0142768887874));
#66022=CARTESIAN_POINT('Ctrl Pts',(-3.64478664922453,-1.72196316619954,
29.0577172996098));
#66023=CARTESIAN_POINT('Ctrl Pts',(-3.12396193915647,-2.39991818272362,
29.1011577104321));
#66024=CARTESIAN_POINT('Ctrl Pts',(-2.33279280817549,-3.42977922982612,
29.1671467301837));
#66025=CARTESIAN_POINT('Ctrl Pts',(-0.982285856360496,-4.02994073748189,
29.2331357499352));
#66026=CARTESIAN_POINT('Ctrl Pts',(0.312303847731737,-3.92698507608034,
29.2991247696868));
#66027=CARTESIAN_POINT('Ctrl Pts',(1.60689355182397,-3.82402941467878,29.3651137894383));
#66028=CARTESIAN_POINT('Ctrl Pts',(2.8455660081934,-3.01795658421989,29.4311028091899));
#66029=CARTESIAN_POINT('Ctrl Pts',(3.46401497166392,-1.87599193952265,29.4970918289414));
#66030=CARTESIAN_POINT('Ctrl Pts',(4.08246393513439,-0.734027294825464,
29.5630808486929));
#66031=CARTESIAN_POINT('Ctrl Pts',(4.08068940570598,0.743829164110116,29.6290698684445));
#66032=CARTESIAN_POINT('Ctrl Pts',(3.45949981181636,1.88430531844186,29.695058888196));
#66033=CARTESIAN_POINT('Ctrl Pts',(2.83831021792669,3.0247814727737,29.7610479079476));
#66034=CARTESIAN_POINT('Ctrl Pts',(1.59770555957574,3.82787732250171,29.8270369276991));
#66035=CARTESIAN_POINT('Ctrl Pts',(0.302872341801343,3.92772374609487,29.8930259474507));
#66036=CARTESIAN_POINT('Ctrl Pts',(-0.991960875972982,4.02757016968802,
29.9590149672022));
#66037=CARTESIAN_POINT('Ctrl Pts',(-2.34102265317071,3.4241671671464,30.0250039869538));
#66038=CARTESIAN_POINT('Ctrl Pts',(-3.1297163043756,2.39240910698635,30.0909930067053));
#66039=CARTESIAN_POINT('Ctrl Pts',(-3.64700802865811,1.71569527118052,30.1342741637919));
#66040=CARTESIAN_POINT('Ctrl Pts',(-3.92323828559463,0.85470989324939,30.1775553208785));
#66041=CARTESIAN_POINT('Ctrl Pts',(-3.9290580015118,-0.00286337897428823,
30.2208364779651));
#66042=CARTESIAN_POINT('Origin',(0.,0.,0.));
#66043=CARTESIAN_POINT('',(-3.93356382969395,0.00360218745272173,31.654163522035));
#66044=CARTESIAN_POINT('',(-3.93922268899305,-0.000712863612796303,31.470836477965));
#66045=CARTESIAN_POINT('',(-3.933,-4.81653586104654E-16,0.));
#66046=CARTESIAN_POINT('Ctrl Pts',(-3.93356382969395,0.00360218745272173,
31.654163522035));
#66047=CARTESIAN_POINT('Ctrl Pts',(-3.93623015633234,0.290333862757325,
31.6396500884593));
#66048=CARTESIAN_POINT('Ctrl Pts',(-3.90755272302672,0.576536680174273,
31.6251366548837));
#66049=CARTESIAN_POINT('Ctrl Pts',(-3.84554438997229,0.855326038390887,
31.6106232213081));
#66050=CARTESIAN_POINT('Ctrl Pts',(-3.56229864696938,2.12879840927471,31.5443278046415));
#66051=CARTESIAN_POINT('Ctrl Pts',(-2.58359042039501,3.24758600458463,31.4780323879748));
#66052=CARTESIAN_POINT('Ctrl Pts',(-1.3590919126262,3.69765648218316,31.4117369713081));
#66053=CARTESIAN_POINT('Ctrl Pts',(-0.134593404857421,4.14772695978168,
31.3454415546415));
#66054=CARTESIAN_POINT('Ctrl Pts',(1.33569538410578,3.92908031966886,31.2791461379748));
#66055=CARTESIAN_POINT('Ctrl Pts',(2.37624319794866,3.14217481235523,31.2128507213081));
#66056=CARTESIAN_POINT('Ctrl Pts',(3.41679101179155,2.3552693050416,31.1465553046414));
#66057=CARTESIAN_POINT('Ctrl Pts',(4.02759785051412,1.00010493052715,31.0802598879748));
#66058=CARTESIAN_POINT('Ctrl Pts',(3.9280255740277,-0.30068152085102,31.0139644713081));
#66059=CARTESIAN_POINT('Ctrl Pts',(3.82845329754128,-1.60146797222919,30.9476690546415));
#66060=CARTESIAN_POINT('Ctrl Pts',(3.01850190584588,-2.84787650047109,30.8813736379748));
#66061=CARTESIAN_POINT('Ctrl Pts',(1.87030746179732,-3.46723871193523,30.8150782213081));
#66062=CARTESIAN_POINT('Ctrl Pts',(0.722113017748764,-4.08660092339936,
30.7487828046414));
#66063=CARTESIAN_POINT('Ctrl Pts',(-0.764324478652949,-4.07891681808573,
30.6824873879748));
#66064=CARTESIAN_POINT('Ctrl Pts',(-1.90605416978368,-3.44771689514194,
30.6161919713081));
#66065=CARTESIAN_POINT('Ctrl Pts',(-3.04778386091445,-2.81651697219814,
30.5498965546414));
#66066=CARTESIAN_POINT('Ctrl Pts',(-3.84480574677421,-1.56180123162415,
30.4836011379748));
#66067=CARTESIAN_POINT('Ctrl Pts',(-3.93092428815543,-0.260054855725923,
30.4173057213081));
#66068=CARTESIAN_POINT('Ctrl Pts',(-3.93661491298216,-0.174036791253616,
30.4129249882171));
#66069=CARTESIAN_POINT('Ctrl Pts',(-3.93920142757912,-0.0878133707686297,
30.408544255126));
#66070=CARTESIAN_POINT('Ctrl Pts',(-3.93876665726707,-0.00156339645701664,
30.404163522035));
#66071=CARTESIAN_POINT('Ctrl Pts',(-3.9290580015118,-0.00286337897428823,
30.2208364779651));
#66072=CARTESIAN_POINT('Ctrl Pts',(-3.93211136973696,-0.452797193170657,
30.24354434063));
#66073=CARTESIAN_POINT('Ctrl Pts',(-3.86072952940889,-0.901791765875257,
30.266252203295));
#66074=CARTESIAN_POINT('Ctrl Pts',(-3.71067383999213,-1.32274152209106,
30.28896006596));
#66075=CARTESIAN_POINT('Ctrl Pts',(-3.27461219919171,-2.54602097322994,
30.3549490857115));
#66076=CARTESIAN_POINT('Ctrl Pts',(-2.17416339237878,-3.53246675772921,
30.4209381054631));
#66077=CARTESIAN_POINT('Ctrl Pts',(-0.910662644202927,-3.83268039751804,
30.4869271252146));
#66078=CARTESIAN_POINT('Ctrl Pts',(0.35283810397296,-4.13289403730688,30.5529161449662));
#66079=CARTESIAN_POINT('Ctrl Pts',(1.77939079351173,-3.74687553238531,30.6189051647177));
#66080=CARTESIAN_POINT('Ctrl Pts',(2.71909593917019,-2.85048465259049,30.6848941844692));
#66081=CARTESIAN_POINT('Ctrl Pts',(3.65880108482858,-1.95409377279572,30.7508832042208));
#66082=CARTESIAN_POINT('Ctrl Pts',(4.11165868660664,-0.547330518127737,
30.8168722239723));
#66083=CARTESIAN_POINT('Ctrl Pts',(3.87135885883217,0.72892116666162,30.8828612437239));
#66084=CARTESIAN_POINT('Ctrl Pts',(3.6310590310577,2.00517285145101,30.9488502634754));
#66085=CARTESIAN_POINT('Ctrl Pts',(2.69760177373066,3.15091296636183,31.014839283227));
#66086=CARTESIAN_POINT('Ctrl Pts',(1.49624540046417,3.64417277069235,31.0808283029785));
#66087=CARTESIAN_POINT('Ctrl Pts',(0.294889027197638,4.13743257502288,31.1468173227301));
#66088=CARTESIAN_POINT('Ctrl Pts',(-1.17436646200829,3.97821206877312,31.2128063424816));
#66089=CARTESIAN_POINT('Ctrl Pts',(-2.24216732149253,3.23904788224822,31.2787953622332));
#66090=CARTESIAN_POINT('Ctrl Pts',(-3.27800464315046,2.52200982741351,31.3428090674771));
#66091=CARTESIAN_POINT('Ctrl Pts',(-3.93606189014718,1.25922849148747,31.4068227727211));
#66092=CARTESIAN_POINT('Ctrl Pts',(-3.93922268899305,-0.000712863612796303,
31.470836477965));
#66093=CARTESIAN_POINT('Origin',(0.,0.,0.));
#66094=CARTESIAN_POINT('',(-3.92649272786585,-8.54312940767876E-5,32.904163522035));
#66095=CARTESIAN_POINT('',(-3.93104799417585,0.00342476555473607,32.7208364779651));
#66096=CARTESIAN_POINT('',(-3.933,-4.81653586104654E-16,0.));
#66097=CARTESIAN_POINT('Ctrl Pts',(-3.92649272786585,-8.54312940767876E-5,
32.904163522035));
#66098=CARTESIAN_POINT('Ctrl Pts',(-3.92636480720739,0.662930438433491,
32.8707559217927));
#66099=CARTESIAN_POINT('Ctrl Pts',(-3.76745221108675,1.3260038941436,32.8373483215504));
#66100=CARTESIAN_POINT('Ctrl Pts',(-3.45009744168608,1.90174181477382,32.8039407213081));
#66101=CARTESIAN_POINT('Ctrl Pts',(-2.82032557791886,3.04425983648661,32.7376453046415));
#66102=CARTESIAN_POINT('Ctrl Pts',(-1.56660737729212,3.8428499376043,32.6713498879748));
#66103=CARTESIAN_POINT('Ctrl Pts',(-0.264969697583205,3.93059605487079,
32.6050544713081));
#66104=CARTESIAN_POINT('Ctrl Pts',(1.03666798212571,4.01834217213727,32.5387590546415));
#66105=CARTESIAN_POINT('Ctrl Pts',(2.38622514091682,3.39524430555255,32.4724636379748));
#66106=CARTESIAN_POINT('Ctrl Pts',(3.16364125068744,2.34758776708021,32.4061682213081));
#66107=CARTESIAN_POINT('Ctrl Pts',(3.94105736045805,1.2999312286079,32.3398728046414));
#66108=CARTESIAN_POINT('Ctrl Pts',(4.1463324212082,-0.172283981752003,32.2735773879748));
#66109=CARTESIAN_POINT('Ctrl Pts',(3.68515181888459,-1.39264150410918,32.2072819713081));
#66110=CARTESIAN_POINT('Ctrl Pts',(3.22397121656098,-2.61299902646635,32.1409865546415));
#66111=CARTESIAN_POINT('Ctrl Pts',(2.0963349511636,-3.5814988608208,32.0746911379748));
#66112=CARTESIAN_POINT('Ctrl Pts',(0.820340928864169,-3.85315909970353,
32.0083957213081));
#66113=CARTESIAN_POINT('Ctrl Pts',(-0.455653093435257,-4.12481933858626,
31.9421003046414));
#66114=CARTESIAN_POINT('Ctrl Pts',(-1.88000487263673,-3.69963998199727,
31.8758048879748));
#66115=CARTESIAN_POINT('Ctrl Pts',(-2.79828913252171,-2.77297173047393,
31.8095094713081));
#66116=CARTESIAN_POINT('Ctrl Pts',(-3.51554203489395,-2.04917026509265,
31.7577274882171));
#66117=CARTESIAN_POINT('Ctrl Pts',(-3.9240507341067,-1.01941794661383,31.705945505126));
#66118=CARTESIAN_POINT('Ctrl Pts',(-3.93356382969395,0.00360218745272173,
31.654163522035));
#66119=CARTESIAN_POINT('Ctrl Pts',(-3.93922268899305,-0.000712863612796303,
31.470836477965));
#66120=CARTESIAN_POINT('Ctrl Pts',(-3.93932022391611,-0.0395917322542401,
31.4728117924726));
#66121=CARTESIAN_POINT('Ctrl Pts',(-3.93879416874135,-0.0784678966759154,
31.4747871069802));
#66122=CARTESIAN_POINT('Ctrl Pts',(-3.93763638107598,-0.117325238088634,
31.4767624214878));
#66123=CARTESIAN_POINT('Ctrl Pts',(-3.89895835141275,-1.41542630510057,
31.5427514412393));
#66124=CARTESIAN_POINT('Ctrl Pts',(-3.15525606232387,-2.69252057232445,
31.6087404609909));
#66125=CARTESIAN_POINT('Ctrl Pts',(-2.04534050789141,-3.36679783887364,
31.6747294807424));
#66126=CARTESIAN_POINT('Ctrl Pts',(-0.935424953458954,-4.04107510542283,
31.740718500494));
#66127=CARTESIAN_POINT('Ctrl Pts',(0.540703866317046,-4.11253537129732,
31.8067075202455));
#66128=CARTESIAN_POINT('Ctrl Pts',(1.71056089907212,-3.5486232388958,31.8726965399971));
#66129=CARTESIAN_POINT('Ctrl Pts',(2.88041793182723,-2.98471110649425,31.9386855597486));
#66130=CARTESIAN_POINT('Ctrl Pts',(3.74400317756135,-1.78542657581666,32.0046745795002));
#66131=CARTESIAN_POINT('Ctrl Pts',(3.9078901538305,-0.4971318000896,32.0706635992517));
#66132=CARTESIAN_POINT('Ctrl Pts',(4.07177713009964,0.79116297563746,32.1366526190033));
#66133=CARTESIAN_POINT('Ctrl Pts',(3.53596583690379,2.16846799641394,32.2026416387548));
#66134=CARTESIAN_POINT('Ctrl Pts',(2.54455765667983,3.00731970580081,32.2686306585064));
#66135=CARTESIAN_POINT('Ctrl Pts',(1.55314947645591,3.84617141518765,32.3346196782579));
#66136=CARTESIAN_POINT('Ctrl Pts',(0.106144409203796,4.14656981318491,32.4006086980095));
#66137=CARTESIAN_POINT('Ctrl Pts',(-1.13724050020451,3.77166137474724,32.466597717761));
#66138=CARTESIAN_POINT('Ctrl Pts',(-2.38062540961286,3.39675293630955,32.5325867375126));
#66139=CARTESIAN_POINT('Ctrl Pts',(-3.42039016117747,2.34653766143695,32.5985757572641));
#66140=CARTESIAN_POINT('Ctrl Pts',(-3.78284557273839,1.09946571291651,32.6645647770157));
#66141=CARTESIAN_POINT('Ctrl Pts',(-3.88587272585993,0.744988255839808,
32.6833220106655));
#66142=CARTESIAN_POINT('Ctrl Pts',(-3.93417544392954,0.374605407215546,
32.7020792443153));
#66143=CARTESIAN_POINT('Ctrl Pts',(-3.93104799417585,0.00342476555473607,
32.7208364779651));
#66144=CARTESIAN_POINT('Origin',(0.,0.,0.));
#66145=CARTESIAN_POINT('',(-3.93387845178167,-0.00357291855290098,34.1541635220349));
#66146=CARTESIAN_POINT('',(-3.92762769288195,-0.00197752355235662,33.9708364779651));
#66147=CARTESIAN_POINT('',(-3.933,-4.81653586104654E-16,0.));
#66148=CARTESIAN_POINT('Ctrl Pts',(-3.93387845178167,-0.00357291855290098,
34.1541635220349));
#66149=CARTESIAN_POINT('Ctrl Pts',(-3.92427200125995,1.02950432289123,34.101861755126));
#66150=CARTESIAN_POINT('Ctrl Pts',(-3.50662895259015,2.0694535888524,34.0495599882171));
#66151=CARTESIAN_POINT('Ctrl Pts',(-2.77646841359207,2.79481975000012,33.9972582213081));
#66152=CARTESIAN_POINT('Ctrl Pts',(-1.85094906640237,3.71426195494336,33.9309628046415));
#66153=CARTESIAN_POINT('Ctrl Pts',(-0.423308453033832,4.12826407478453,
33.8646673879748));
#66154=CARTESIAN_POINT('Ctrl Pts',(0.850517079696137,3.84661084392644,33.7983719713081));
#66155=CARTESIAN_POINT('Ctrl Pts',(2.12434261242611,3.56495761306834,33.7320765546414));
#66156=CARTESIAN_POINT('Ctrl Pts',(3.24435306451751,2.58764903151097,33.6657811379748));
#66157=CARTESIAN_POINT('Ctrl Pts',(3.69595424636158,1.36371422812528,33.5994857213081));
#66158=CARTESIAN_POINT('Ctrl Pts',(4.14755542820564,0.139779424739578,33.5331903046415));
#66159=CARTESIAN_POINT('Ctrl Pts',(3.93074733980237,-1.33078160047445,33.4668948879748));
#66160=CARTESIAN_POINT('Ctrl Pts',(3.14514350025717,-2.3723125110148,33.4005994713081));
#66161=CARTESIAN_POINT('Ctrl Pts',(2.35953966071195,-3.41384342155519,33.3343040546414));
#66162=CARTESIAN_POINT('Ctrl Pts',(1.00514007002477,-4.02634421742187,33.2680086379748));
#66163=CARTESIAN_POINT('Ctrl Pts',(-0.295769865086573,-3.92839846173285,
33.2017132213081));
#66164=CARTESIAN_POINT('Ctrl Pts',(-1.59667980019788,-3.83045270604383,
33.1354178046415));
#66165=CARTESIAN_POINT('Ctrl Pts',(-2.84410007973336,-3.02206039879914,
33.0691223879748));
#66166=CARTESIAN_POINT('Ctrl Pts',(-3.46489745604721,-1.87464127402288,
33.0028269713081));
#66167=CARTESIAN_POINT('Ctrl Pts',(-3.77286248855624,-1.30542983475844,
32.9699391548837));
#66168=CARTESIAN_POINT('Ctrl Pts',(-3.92661865822607,-0.65278553701605,
32.9370513384593));
#66169=CARTESIAN_POINT('Ctrl Pts',(-3.92649272786585,-8.54312940767876E-5,
32.904163522035));
#66170=CARTESIAN_POINT('Ctrl Pts',(-3.93104799417585,0.00342476555473607,
32.7208364779651));
#66171=CARTESIAN_POINT('Ctrl Pts',(-3.92317289699638,-0.931229299076759,
32.7680682640668));
#66172=CARTESIAN_POINT('Ctrl Pts',(-3.58919907311395,-1.87094185961445,
32.8153000501685));
#66173=CARTESIAN_POINT('Ctrl Pts',(-2.9817228678744,-2.57450465531943,32.8625318362703));
#66174=CARTESIAN_POINT('Ctrl Pts',(-2.13299867989226,-3.5574744528668,32.9285208560218));
#66175=CARTESIAN_POINT('Ctrl Pts',(-0.750404232370731,-4.07948542579326,
32.9945098757734));
#66176=CARTESIAN_POINT('Ctrl Pts',(0.536187196027154,-3.9027232507419,33.0604988955249));
#66177=CARTESIAN_POINT('Ctrl Pts',(1.82277862442504,-3.72596107569055,33.1264879152765));
#66178=CARTESIAN_POINT('Ctrl Pts',(3.01336703369929,-2.85042575266138,33.192476935028));
#66179=CARTESIAN_POINT('Ctrl Pts',(3.56555199237859,-1.67498790166057,33.2584659547796));
#66180=CARTESIAN_POINT('Ctrl Pts',(4.11773695105789,-0.499550050659755,
33.3244549745311));
#66181=CARTESIAN_POINT('Ctrl Pts',(4.03151845914224,0.9757903283127,33.3904439942827));
#66182=CARTESIAN_POINT('Ctrl Pts',(3.34617536971732,2.07890737556271,33.4564330140342));
#66183=CARTESIAN_POINT('Ctrl Pts',(2.66083228029241,3.18202442281269,33.5224220337857));
#66184=CARTESIAN_POINT('Ctrl Pts',(1.37636459335825,3.91291813834024,33.5884110535373));
#66185=CARTESIAN_POINT('Ctrl Pts',(0.0779416438280532,3.938612773708,33.6544000732888));
#66186=CARTESIAN_POINT('Ctrl Pts',(-1.22048130570222,3.96430740907576,33.7203890930404));
#66187=CARTESIAN_POINT('Ctrl Pts',(-2.53285951782854,3.28480296428364,33.786378112792));
#66188=CARTESIAN_POINT('Ctrl Pts',(-3.26130836427971,2.20966360203028,33.8523671325435));
#66189=CARTESIAN_POINT('Ctrl Pts',(-3.69723370628901,1.56626839798642,33.8918569143507));
#66190=CARTESIAN_POINT('Ctrl Pts',(-3.92404344920073,0.781189220414063,
33.9313466961579));
#66191=CARTESIAN_POINT('Ctrl Pts',(-3.92762769288195,-0.00197752355235662,
33.9708364779651));
#66192=CARTESIAN_POINT('Origin',(0.,0.,0.));
#66193=CARTESIAN_POINT('',(-3.93859184179281,0.0017323510934187,35.4041635220349));
#66194=CARTESIAN_POINT('',(-3.93814916617749,-0.00196197512325486,35.2208364779651));
#66195=CARTESIAN_POINT('',(-3.933,-4.81653586104654E-16,0.));
#66196=CARTESIAN_POINT('Ctrl Pts',(-3.93859184179281,0.0017323510934187,
35.4041635220349));
#66197=CARTESIAN_POINT('Ctrl Pts',(-3.93912260889036,0.0982274365966933,
35.399263005126));
#66198=CARTESIAN_POINT('Ctrl Pts',(-3.93588505782954,0.194686303980022,
35.3943624882171));
#66199=CARTESIAN_POINT('Ctrl Pts',(-3.92876520998431,0.290857753704378,
35.3894619713081));
#66200=CARTESIAN_POINT('Ctrl Pts',(-3.8324461301253,1.5918891447566,35.3231665546415));
#66201=CARTESIAN_POINT('Ctrl Pts',(-3.02561416698513,2.84031921217913,35.2568711379748));
#66202=CARTESIAN_POINT('Ctrl Pts',(-1.87897215434241,3.46255077964548,35.1905757213081));
#66203=CARTESIAN_POINT('Ctrl Pts',(-0.732330141699747,4.08478234711179,
35.1242803046415));
#66204=CARTESIAN_POINT('Ctrl Pts',(0.754121920445437,4.08081541462198,35.0579848879748));
#66205=CARTESIAN_POINT('Ctrl Pts',(1.89742648602436,3.45247259625468,34.9916894713081));
#66206=CARTESIAN_POINT('Ctrl Pts',(3.04073105160337,2.82412977788732,34.9253940546415));
#66207=CARTESIAN_POINT('Ctrl Pts',(3.84088812061606,1.57141107364234,34.8590986379748));
#66208=CARTESIAN_POINT('Ctrl Pts',(3.93026167685899,0.26988412422172,34.7928032213081));
#66209=CARTESIAN_POINT('Ctrl Pts',(4.01963523310191,-1.03164282519879,34.7265078046414));
#66210=CARTESIAN_POINT('Ctrl Pts',(3.39822527657522,-2.38197801979493,34.6602123879748));
#66211=CARTESIAN_POINT('Ctrl Pts',(2.35154160189833,-3.16070346248766,34.5939169713081));
#66212=CARTESIAN_POINT('Ctrl Pts',(1.3048579272214,-3.93942890518042,34.5276215546415));
#66213=CARTESIAN_POINT('Ctrl Pts',(-0.16709946560576,-4.14654459596973,
34.4613261379748));
#66214=CARTESIAN_POINT('Ctrl Pts',(-1.38803267274777,-3.68689023274352,
34.3950307213081));
#66215=CARTESIAN_POINT('Ctrl Pts',(-2.60896587988981,-3.22723586951729,
34.3287353046414));
#66216=CARTESIAN_POINT('Ctrl Pts',(-3.57887490134668,-2.10081145227551,
34.2624398879748));
#66217=CARTESIAN_POINT('Ctrl Pts',(-3.85213037156966,-0.825158098631946,
34.1961444713081));
#66218=CARTESIAN_POINT('Ctrl Pts',(-3.90980919066372,-0.55589293460251,
34.1821508215504));
#66219=CARTESIAN_POINT('Ctrl Pts',(-3.93644871492879,-0.279978897620677,
34.1681571717927));
#66220=CARTESIAN_POINT('Ctrl Pts',(-3.93387845178167,-0.00357291855290098,
34.1541635220349));
#66221=CARTESIAN_POINT('Ctrl Pts',(-3.92762769288195,-0.00197752355235662,
33.9708364779651));
#66222=CARTESIAN_POINT('Ctrl Pts',(-3.93003286510151,-0.52751402815515,
33.9973357159094));
#66223=CARTESIAN_POINT('Ctrl Pts',(-3.83192067024081,-1.05218937311693,
34.0238349538538));
#66224=CARTESIAN_POINT('Ctrl Pts',(-3.62902757271598,-1.53261357085699,
34.0503341917981));
#66225=CARTESIAN_POINT('Ctrl Pts',(-3.12377845392507,-2.72897710177648,
34.1163232115497));
#66226=CARTESIAN_POINT('Ctrl Pts',(-1.9687607355672,-3.65092988390098,34.1823122313012));
#66227=CARTESIAN_POINT('Ctrl Pts',(-0.690169787889638,-3.8784547367334,
34.2483012510528));
#66228=CARTESIAN_POINT('Ctrl Pts',(0.588421159787958,-4.10597958956582,
34.3142902708043));
#66229=CARTESIAN_POINT('Ctrl Pts',(1.99058533678528,-3.63907651310612,34.3802792905558));
#66230=CARTESIAN_POINT('Ctrl Pts',(2.87753401594177,-2.69045413789849,34.4462683103074));
#66231=CARTESIAN_POINT('Ctrl Pts',(3.76448269509826,-1.74183176269087,34.512257330059));
#66232=CARTESIAN_POINT('Ctrl Pts',(4.13621587641395,-0.311490088735288,
34.5782463498105));
#66233=CARTESIAN_POINT('Ctrl Pts',(3.8233818036528,0.948945238063219,34.6442353695621));
#66234=CARTESIAN_POINT('Ctrl Pts',(3.51054773089165,2.20938056486173,34.7102243893136));
#66235=CARTESIAN_POINT('Ctrl Pts',(2.51314640405376,3.2999095445031,34.7762134090651));
#66236=CARTESIAN_POINT('Ctrl Pts',(1.28556735528643,3.72371616206282,34.8422024288167));
#66237=CARTESIAN_POINT('Ctrl Pts',(0.0579883065191089,4.14752277962253,
34.9081914485682));
#66238=CARTESIAN_POINT('Ctrl Pts',(-1.39976846417762,3.9046070351005,34.9741804683198));
#66239=CARTESIAN_POINT('Ctrl Pts',(-2.42358772202978,3.10563488431345,35.0401694880713));
#66240=CARTESIAN_POINT('Ctrl Pts',(-3.35793682135874,2.37648381223565,35.1003918180359));
#66241=CARTESIAN_POINT('Ctrl Pts',(-3.93087693228753,1.18421586887302,35.1606141480005));
#66242=CARTESIAN_POINT('Ctrl Pts',(-3.93814916617749,-0.00196197512325486,
35.2208364779651));
#66243=CARTESIAN_POINT('Origin',(0.,0.,0.));
#66244=CARTESIAN_POINT('',(-3.92854696981776,0.00272907840631081,36.6541635220349));
#66245=CARTESIAN_POINT('',(-3.93324212187193,0.00353561962986205,36.4708364779651));
#66246=CARTESIAN_POINT('',(-3.933,-4.81653586104654E-16,0.));
#66247=CARTESIAN_POINT('Ctrl Pts',(-3.92854696981776,0.00272907840631081,
36.6541635220349));
#66248=CARTESIAN_POINT('Ctrl Pts',(-3.93154855147801,0.474347357201858,
36.6303688384593));
#66249=CARTESIAN_POINT('Ctrl Pts',(-3.85305357694903,0.944999852833924,
36.6065741548837));
#66250=CARTESIAN_POINT('Ctrl Pts',(-3.6886229876758,1.38342200393479,36.5827794713081));
#66251=CARTESIAN_POINT('Ctrl Pts',(-3.23049567558203,2.60492928268355,36.5164840546415));
#66252=CARTESIAN_POINT('Ctrl Pts',(-2.10528466290456,3.57624532739106,36.4501886379748));
#66253=CARTESIAN_POINT('Ctrl Pts',(-0.829973923421927,3.85109544722928,
36.3838932213081));
#66254=CARTESIAN_POINT('Ctrl Pts',(0.445336816060738,4.12594556706751,36.3175978046415));
#66255=CARTESIAN_POINT('Ctrl Pts',(1.87074728234857,3.7043297620364,36.2513023879748));
#66256=CARTESIAN_POINT('Ctrl Pts',(2.79134596938285,2.77996084689474,36.1850069713081));
#66257=CARTESIAN_POINT('Ctrl Pts',(3.71194465641712,1.8555919317531,36.1187115546415));
#66258=CARTESIAN_POINT('Ctrl Pts',(4.12773156419788,0.428469906500936,36.0524161379748));
#66259=CARTESIAN_POINT('Ctrl Pts',(3.84767129915961,-0.845706838817057,
35.9861207213081));
#66260=CARTESIAN_POINT('Ctrl Pts',(3.56761103412134,-2.11988358413505,35.9198253046414));
#66261=CARTESIAN_POINT('Ctrl Pts',(2.59170359626402,-3.24111504951888,35.8535298879748));
#66262=CARTESIAN_POINT('Ctrl Pts',(1.36833440376772,-3.69424620751226,35.7872344713082));
#66263=CARTESIAN_POINT('Ctrl Pts',(0.144965211271464,-4.14737736550564,
35.7209390546415));
#66264=CARTESIAN_POINT('Ctrl Pts',(-1.32586573586376,-3.93240821610861,
35.6546436379748));
#66265=CARTESIAN_POINT('Ctrl Pts',(-2.36837811114245,-3.14810728406921,
35.5883482213081));
#66266=CARTESIAN_POINT('Ctrl Pts',(-3.3338286052278,-2.42178140026698,35.5269533215504));
#66267=CARTESIAN_POINT('Ctrl Pts',(-3.93194225903368,-1.207182180102,35.4655584217927));
#66268=CARTESIAN_POINT('Ctrl Pts',(-3.93859184179281,0.0017323510934187,
35.4041635220349));
#66269=CARTESIAN_POINT('Ctrl Pts',(-3.93814916617749,-0.00196197512325486,
35.2208364779651));
#66270=CARTESIAN_POINT('Ctrl Pts',(-3.93884553107946,-0.115546415687587,
35.226603167752));
#66271=CARTESIAN_POINT('Ctrl Pts',(-3.93435509495706,-0.229075014060918,
35.232369857539));
#66272=CARTESIAN_POINT('Ctrl Pts',(-3.92449851330675,-0.342135794579535,
35.238136547326));
#66273=CARTESIAN_POINT('Ctrl Pts',(-3.8117083017239,-1.63590576563339,35.3041255670775));
#66274=CARTESIAN_POINT('Ctrl Pts',(-2.99624613355058,-2.86841715068901,
35.3701145868291));
#66275=CARTESIAN_POINT('Ctrl Pts',(-1.84961489770968,-3.47817052594584,
35.4361036065806));
#66276=CARTESIAN_POINT('Ctrl Pts',(-0.702983661868818,-4.08792390120266,
35.5020926263321));
#66277=CARTESIAN_POINT('Ctrl Pts',(0.774816641639593,-4.07491926666073,
35.5680816460837));
#66278=CARTESIAN_POINT('Ctrl Pts',(1.91053947962039,-3.44508118611152,35.6340706658352));
#66279=CARTESIAN_POINT('Ctrl Pts',(3.04626231760121,-2.81524310556228,35.7000596855868));
#66280=CARTESIAN_POINT('Ctrl Pts',(3.8399076900544,-1.56857157900572,35.7660487053384));
#66281=CARTESIAN_POINT('Ctrl Pts',(3.92991185646822,-0.273017019234441,
35.8320377250899));
#66282=CARTESIAN_POINT('Ctrl Pts',(4.01991602288204,1.02253754053684,35.8980267448414));
#66283=CARTESIAN_POINT('Ctrl Pts',(3.40627898325649,2.36697513352282,35.964015764593));
#66284=CARTESIAN_POINT('Ctrl Pts',(2.36855747134988,3.147805737116,36.0300047843445));
#66285=CARTESIAN_POINT('Ctrl Pts',(1.33083595944332,3.92863634070914,36.0959938040961));
#66286=CARTESIAN_POINT('Ctrl Pts',(-0.130970024744263,4.14585995490953,
36.1619828238476));
#66287=CARTESIAN_POINT('Ctrl Pts',(-1.35090055112145,3.70051526108771,36.2279718435992));
#66288=CARTESIAN_POINT('Ctrl Pts',(-2.57083107749874,3.25517056726585,36.2939608633507));
#66289=CARTESIAN_POINT('Ctrl Pts',(-3.54888614606559,2.14725756542165,36.3599498831023));
#66290=CARTESIAN_POINT('Ctrl Pts',(-3.83948982933842,0.881511996143767,
36.4259389028538));
#66291=CARTESIAN_POINT('Ctrl Pts',(-3.90539675722059,0.594449557663731,
36.4409047612242));
#66292=CARTESIAN_POINT('Ctrl Pts',(-3.9359445283657,0.299268979327574,36.4558706195946));
#66293=CARTESIAN_POINT('Ctrl Pts',(-3.93324212187193,0.00353561962986205,
36.4708364779651));
#66294=CARTESIAN_POINT('Origin',(0.,0.,0.));
#66295=CARTESIAN_POINT('',(-3.92861605367513,-0.00280348551048665,37.9041635220349));
#66296=CARTESIAN_POINT('',(-3.92680078726362,-0.000862425370787758,37.7208364779651));
#66297=CARTESIAN_POINT('',(-3.933,-4.81653586104654E-16,0.));
#66298=CARTESIAN_POINT('Ctrl Pts',(-3.92861605367513,-0.00280348551048665,
37.9041635220349));
#66299=CARTESIAN_POINT('Ctrl Pts',(-3.92314714083183,0.843271536769385,
37.8614746717927));
#66300=CARTESIAN_POINT('Ctrl Pts',(-3.65525453228082,1.69252296329638,37.8187858215504));
#66301=CARTESIAN_POINT('Ctrl Pts',(-3.15107129829004,2.36445631166207,37.7760969713081));
#66302=CARTESIAN_POINT('Ctrl Pts',(-2.36807907938348,3.40796301304478,37.7098015546415));
#66303=CARTESIAN_POINT('Ctrl Pts',(-1.01520532603393,4.02381712229028,37.6435061379748));
#66304=CARTESIAN_POINT('Ctrl Pts',(0.285947880721249,3.92911729405849,37.5772107213081));
#66305=CARTESIAN_POINT('Ctrl Pts',(1.58710108747643,3.8344174658267,37.5109153046415));
#66306=CARTESIAN_POINT('Ctrl Pts',(2.83653374763726,3.02916370011762,37.4446198879748));
#66307=CARTESIAN_POINT('Ctrl Pts',(3.46019728219322,1.88330455174309,37.3783244713081));
#66308=CARTESIAN_POINT('Ctrl Pts',(4.08386081674918,0.737445403368564,37.3120290546415));
#66309=CARTESIAN_POINT('Ctrl Pts',(4.08175522570026,-0.749019127671417,
37.2457336379748));
#66310=CARTESIAN_POINT('Ctrl Pts',(3.45484308914238,-1.89311051940086,37.1794382213081));
#66311=CARTESIAN_POINT('Ctrl Pts',(2.82793095258448,-3.03720191113034,37.1131428046415));
#66312=CARTESIAN_POINT('Ctrl Pts',(1.57621227051757,-3.83892016354926,37.0468473879748));
#66313=CARTESIAN_POINT('Ctrl Pts',(0.274797744277373,-3.92991993716301,
36.9805519713081));
#66314=CARTESIAN_POINT('Ctrl Pts',(-1.02661678196279,-4.02091971077676,
36.9142565546415));
#66315=CARTESIAN_POINT('Ctrl Pts',(-2.37772715237623,-3.40120100558538,
36.8479611379748));
#66316=CARTESIAN_POINT('Ctrl Pts',(-3.15776053182792,-2.35549239659468,
36.7816657213081));
#66317=CARTESIAN_POINT('Ctrl Pts',(-3.65782512345545,-1.68510845881512,
36.7391649882171));
#66318=CARTESIAN_POINT('Ctrl Pts',(-3.92318571251892,-0.839649116044735,
36.696664255126));
#66319=CARTESIAN_POINT('Ctrl Pts',(-3.92854696981776,0.00272907840631081,
36.6541635220349));
#66320=CARTESIAN_POINT('Ctrl Pts',(-3.93324212187193,0.00353561962986205,
36.4708364779651));
#66321=CARTESIAN_POINT('Ctrl Pts',(-3.92402879649918,-1.00470931789247,
36.5218596393462));
#66322=CARTESIAN_POINT('Ctrl Pts',(-3.52833688498228,-2.01937942887946,
36.5728828007273));
#66323=CARTESIAN_POINT('Ctrl Pts',(-2.82974005739278,-2.74067810778768,
36.6239059621085));
#66324=CARTESIAN_POINT('Ctrl Pts',(-1.92623430419552,-3.67354450572974,
36.68989498186));
#66325=CARTESIAN_POINT('Ctrl Pts',(-0.516070499822165,-4.1156991649024,
36.7558840016115));
#66326=CARTESIAN_POINT('Ctrl Pts',(0.758318344745277,-3.86570807659067,
36.8218730213631));
#66327=CARTESIAN_POINT('Ctrl Pts',(2.03270718931276,-3.61571698827893,36.8878620411146));
#66328=CARTESIAN_POINT('Ctrl Pts',(3.17132107407428,-2.67358015248279,36.9538510608662));
#66329=CARTESIAN_POINT('Ctrl Pts',(3.6554375232991,-1.46851025784295,37.0198400806177));
#66330=CARTESIAN_POINT('Ctrl Pts',(4.13955397252392,-0.263440363203115,
37.0858291003693));
#66331=CARTESIAN_POINT('Ctrl Pts',(3.96917298621199,1.20456259028048,37.1518181201208));
#66332=CARTESIAN_POINT('Ctrl Pts',(3.22191610266395,2.26671584208094,37.2178071398724));
#66333=CARTESIAN_POINT('Ctrl Pts',(2.47465921911595,3.32886909388133,37.2837961596239));
#66334=CARTESIAN_POINT('Ctrl Pts',(1.15052643833195,3.98517264399873,37.3497851793755));
#66335=CARTESIAN_POINT('Ctrl Pts',(-0.147243479843609,3.93663134576437,
37.415774199127));
#66336=CARTESIAN_POINT('Ctrl Pts',(-1.44501339801924,3.88809004753,37.4817632188786));
#66337=CARTESIAN_POINT('Ctrl Pts',(-2.71642045358641,3.1347039009438,37.5477522386301));
#66338=CARTESIAN_POINT('Ctrl Pts',(-3.38224359437478,2.0196969376997,37.6137412583817));
#66339=CARTESIAN_POINT('Ctrl Pts',(-3.7424372333312,1.41650610375378,37.6494396649095));
#66340=CARTESIAN_POINT('Ctrl Pts',(-3.92540438127228,0.707485529535139,
37.6851380714373));
#66341=CARTESIAN_POINT('Ctrl Pts',(-3.92680078726362,-0.000862425370787757,
37.7208364779651));
#66342=CARTESIAN_POINT('Origin',(0.,0.,0.));
#66343=CARTESIAN_POINT('',(-3.93300000000003,-4.81653586104657E-16,39.067));
#66344=CARTESIAN_POINT('',(-3.936306081373,-0.00286452337122285,38.970836477965));
#66345=CARTESIAN_POINT('',(-3.933,-4.81653586104654E-16,0.));
#66346=CARTESIAN_POINT('',(-3.55519577774135,1.66475697885233,39.067));
#66347=CARTESIAN_POINT('Origin',(0.,0.,39.067));
#66348=CARTESIAN_POINT('Ctrl Pts',(-3.55517835630003,1.66474646536772,39.067));
#66349=CARTESIAN_POINT('Ctrl Pts',(-3.281770047254,2.25009079435063,39.0344714904361));
#66350=CARTESIAN_POINT('Ctrl Pts',(-2.87218003711123,2.77178961343465,39.0019429808721));
#66351=CARTESIAN_POINT('Ctrl Pts',(-2.35968662710541,3.15555731452043,38.9694144713081));
#66352=CARTESIAN_POINT('Ctrl Pts',(-1.31518859720181,3.93770319171364,38.9031190546415));
#66353=CARTESIAN_POINT('Ctrl Pts',(0.156742781769128,4.1469198966438,38.8368236379748));
#66354=CARTESIAN_POINT('Ctrl Pts',(1.37894059931111,3.68993834295183,38.7705282213081));
#66355=CARTESIAN_POINT('Ctrl Pts',(2.60113841685301,3.23295678925989,38.7042328046414));
#66356=CARTESIAN_POINT('Ctrl Pts',(3.57360267296599,2.10977697694588,38.6379373879748));
#66357=CARTESIAN_POINT('Ctrl Pts',(3.84998555909052,0.835006136376253,38.5716419713081));
#66358=CARTESIAN_POINT('Ctrl Pts',(4.12636844521508,-0.439764704193487,
38.5053465546415));
#66359=CARTESIAN_POINT('Ctrl Pts',(3.70666996135107,-1.86612657301888,38.4390511379748));
#66360=CARTESIAN_POINT('Ctrl Pts',(2.78348499916481,-2.78798189487759,38.3727557213081));
#66361=CARTESIAN_POINT('Ctrl Pts',(1.86030003697863,-3.70983721673622,38.3064603046415));
#66362=CARTESIAN_POINT('Ctrl Pts',(0.433628596470313,-4.12718599162826,
38.2401648879748));
#66363=CARTESIAN_POINT('Ctrl Pts',(-0.840914130798121,-3.84866608078101,
38.1738694713081));
#66364=CARTESIAN_POINT('Ctrl Pts',(-2.11545685806663,-3.57014616993374,
38.1075740546415));
#66365=CARTESIAN_POINT('Ctrl Pts',(-3.23787087209523,-2.59575757334711,
38.0412786379748));
#66366=CARTESIAN_POINT('Ctrl Pts',(-3.69252253687772,-1.37298362829381,
37.9749832213081));
#66367=CARTESIAN_POINT('Ctrl Pts',(-3.8544155494613,-0.937576539730567,
37.9513766548837));
#66368=CARTESIAN_POINT('Ctrl Pts',(-3.93164031536341,-0.470675683991357,
37.9277700884593));
#66369=CARTESIAN_POINT('Ctrl Pts',(-3.92861605367513,-0.00280348551048665,
37.9041635220349));
#66370=CARTESIAN_POINT('Ctrl Pts',(-3.92680078726362,-0.000862425370787757,
37.7208364779651));
#66371=CARTESIAN_POINT('Ctrl Pts',(-3.92798565790354,-0.60190588968295,
37.7511270911888));
#66372=CARTESIAN_POINT('Ctrl Pts',(-3.79844381669874,-1.20246508373146,
37.7814177044126));
#66373=CARTESIAN_POINT('Ctrl Pts',(-3.53552131443984,-1.73747658063651,
37.8117083176363));
#66374=CARTESIAN_POINT('Ctrl Pts',(-2.96273666770691,-2.90301535582683,
37.8776973373879));
#66375=CARTESIAN_POINT('Ctrl Pts',(-1.75692814823142,-3.75746512630542,
37.9436863571394));
#66376=CARTESIAN_POINT('Ctrl Pts',(-0.467423498028026,-3.91155642168368,
38.0096753768909));
#66377=CARTESIAN_POINT('Ctrl Pts',(0.822081152175291,-4.06564771706194,
38.0756643966425));
#66378=CARTESIAN_POINT('Ctrl Pts',(2.19528193310649,-3.51938053733994,38.141653416394));
#66379=CARTESIAN_POINT('Ctrl Pts',(3.02657250539957,-2.52162900267819,38.2076424361456));
#66380=CARTESIAN_POINT('Ctrl Pts',(3.85786307769267,-1.52387746801641,38.2736314558971));
#66381=CARTESIAN_POINT('Ctrl Pts',(4.14724344134762,-0.074641578414862,
38.3396204756487));
#66382=CARTESIAN_POINT('Ctrl Pts',(3.76290363779945,1.16586313888606,38.4056094954002));
#66383=CARTESIAN_POINT('Ctrl Pts',(3.37856383425128,2.40636785618698,38.4715985151518));
#66384=CARTESIAN_POINT('Ctrl Pts',(2.3205038635,3.43814140118727,38.5375875349033));
#66385=CARTESIAN_POINT('Ctrl Pts',(1.07070171926435,3.79110107416724,38.6035765546549));
#66386=CARTESIAN_POINT('Ctrl Pts',(-0.179100424971232,4.14406074714718,
38.6695655744064));
#66387=CARTESIAN_POINT('Ctrl Pts',(-1.62064474269115,3.81820654810687,38.7355545941579));
#66388=CARTESIAN_POINT('Ctrl Pts',(-2.5971139356278,2.96205423396555,38.8015436139095));
#66389=CARTESIAN_POINT('Ctrl Pts',(-3.43214814261489,2.22990981623014,38.8579745685947));
#66390=CARTESIAN_POINT('Ctrl Pts',(-3.92707614700865,1.10996207692717,38.9144055232799));
#66391=CARTESIAN_POINT('Ctrl Pts',(-3.936306081373,-0.00286452337122285,
38.970836477965));
#66392=CARTESIAN_POINT('Origin',(0.,0.,-2.31077344927314));
#66393=CARTESIAN_POINT('',(-3.22696940764995,-0.00257222088861585,39.5642265507268));
#66394=CARTESIAN_POINT('',(-3.22275,-3.94673047195213E-16,39.77725));
#66395=CARTESIAN_POINT('',(-3.22275,7.67147279210326E-13,-2.31077344927314));
#66396=CARTESIAN_POINT('',(-1.54513563095096,-2.82819261092058,39.7772500000001));
#66397=CARTESIAN_POINT('Ctrl Pts',(-3.22696940764995,-0.00257222088861592,
39.5642265507268));
#66398=CARTESIAN_POINT('Ctrl Pts',(-3.2273947683947,-0.0785187605428588,
39.5689389504846));
#66399=CARTESIAN_POINT('Ctrl Pts',(-3.19081253852192,-1.22220206883349,
39.639946766909));
#66400=CARTESIAN_POINT('Ctrl Pts',(-2.48759436411792,-2.31329607816883,
39.7109545833334));
#66401=CARTESIAN_POINT('Ctrl Pts',(-1.54513563095092,-2.82819261092061,
39.7772500000001));
#66402=CARTESIAN_POINT('Origin',(0.,0.,39.77725));
#66403=CARTESIAN_POINT('Origin',(0.,0.,-2.31077344927314));
#66404=CARTESIAN_POINT('',(-3.21915773887147,-0.00229721152486538,38.3142265507269));
#66405=CARTESIAN_POINT('',(-3.22545904493893,-0.00234722672036308,38.5607734492731));
#66406=CARTESIAN_POINT('',(-3.22275,7.67147279210326E-13,-2.31077344927314));
#66407=CARTESIAN_POINT('Ctrl Pts',(-3.21915773887147,-0.00229721152486602,
38.3142265507269));
#66408=CARTESIAN_POINT('Ctrl Pts',(-3.22163585719237,-0.385677615200072,
38.3378331171513));
#66409=CARTESIAN_POINT('Ctrl Pts',(-2.98064768969752,-1.8426918296433,38.4277351002423));
#66410=CARTESIAN_POINT('Ctrl Pts',(-0.813711880402819,-3.723849330995,38.5839325000001));
#66411=CARTESIAN_POINT('Ctrl Pts',(2.6933860485815,-2.69790671903219,38.7828187500001));
#66412=CARTESIAN_POINT('Ctrl Pts',(3.72510480439603,0.808430209081211,38.9817050000001));
#66413=CARTESIAN_POINT('Ctrl Pts',(1.33455622972935,3.56947348912338,39.1805912500001));
#66414=CARTESIAN_POINT('Ctrl Pts',(-2.19806823460843,3.06735493880013,39.3747651002423));
#66415=CARTESIAN_POINT('Ctrl Pts',(-3.22141066915511,0.989919349467212,
39.5026435338179));
#66416=CARTESIAN_POINT('Ctrl Pts',(-3.22696940764995,-0.00257222088861592,
39.5642265507268));
#66417=CARTESIAN_POINT('',(-3.17710367210759,0.540490350682096,39.7772500000001));
#66418=CARTESIAN_POINT('Origin',(0.,0.,39.77725));
#66419=CARTESIAN_POINT('Ctrl Pts',(-3.22545904493893,-0.00234722672036301,
38.5607734492731));
#66420=CARTESIAN_POINT('Ctrl Pts',(-3.2267400589162,-0.156795392107344,
38.5703315143395));
#66421=CARTESIAN_POINT('Ctrl Pts',(-3.14662046190347,-1.37623279221256,
38.6458785991574));
#66422=CARTESIAN_POINT('Ctrl Pts',(-1.59232210767045,-3.45719070782108,
38.7874147037269));
#66423=CARTESIAN_POINT('Ctrl Pts',(2.03356109694112,-3.21705406573836,38.9853817629815));
#66424=CARTESIAN_POINT('Ctrl Pts',(3.80457448616929,-0.0471873108411222,
39.1833488222361));
#66425=CARTESIAN_POINT('Ctrl Pts',(2.11292542611656,3.16852227003697,39.3813158814907));
#66426=CARTESIAN_POINT('Ctrl Pts',(-1.51168002663127,3.4916201787766,39.5792829407454));
#66427=CARTESIAN_POINT('Ctrl Pts',(-2.99782464886751,1.59432608031001,39.7112609802485));
#66428=CARTESIAN_POINT('Ctrl Pts',(-3.17710367210759,0.540490350682096,
39.7772500000001));
#66429=CARTESIAN_POINT('Origin',(0.,0.,-2.31077344927314));
#66430=CARTESIAN_POINT('',(-3.21910113068401,0.00223624140265653,37.0642265507269));
#66431=CARTESIAN_POINT('',(-3.21767028658882,-0.000706682268057368,37.3107734492731));
#66432=CARTESIAN_POINT('',(-3.22275,7.67147279210326E-13,-2.31077344927314));
#66433=CARTESIAN_POINT('Ctrl Pts',(-3.21910113068401,0.00223624140265662,
37.0642265507269));
#66434=CARTESIAN_POINT('Ctrl Pts',(-3.21470804856876,-0.688019117399231,
37.1067272838179));
#66435=CARTESIAN_POINT('Ctrl Pts',(-2.65809139214385,-2.46144279789799,
37.2155234335756));
#66436=CARTESIAN_POINT('Ctrl Pts',(0.265894155143361,-3.80259787822564,
37.3906150000001));
#66437=CARTESIAN_POINT('Ctrl Pts',(3.34291656752411,-1.83178361584359,37.58950125));
#66438=CARTESIAN_POINT('Ctrl Pts',(3.34809261142426,1.82229995960197,37.7883875000001));
#66439=CARTESIAN_POINT('Ctrl Pts',(0.276689784930593,3.80180535505515,37.98727375));
#66440=CARTESIAN_POINT('Ctrl Pts',(-2.65425757115236,2.46758184103052,38.1625534335757));
#66441=CARTESIAN_POINT('Ctrl Pts',(-3.21467644243972,0.690987374809255,
38.2715377004846));
#66442=CARTESIAN_POINT('Ctrl Pts',(-3.21915773887147,-0.00229721152486602,
38.3142265507269));
#66443=CARTESIAN_POINT('Ctrl Pts',(-3.21767028658882,-0.000706682268057576,
37.3107734492731));
#66444=CARTESIAN_POINT('Ctrl Pts',(-3.21864118459424,-0.493209307392164,
37.3410640624968));
#66445=CARTESIAN_POINT('Ctrl Pts',(-2.88124583165036,-2.05738254559314,
37.4373436954722));
#66446=CARTESIAN_POINT('Ctrl Pts',(-0.451594402129131,-3.77906146290628,
37.599612348199));
#66447=CARTESIAN_POINT('Ctrl Pts',(2.92405992033173,-2.43620673106119,37.7975794074536));
#66448=CARTESIAN_POINT('Ctrl Pts',(3.63542572274911,1.12635998382311,37.9955464667083));
#66449=CARTESIAN_POINT('Ctrl Pts',(1.03446251089667,3.6627049053714,38.1935135259629));
#66450=CARTESIAN_POINT('Ctrl Pts',(-2.33810477673144,2.90035219882563,38.3819225201512));
#66451=CARTESIAN_POINT('Ctrl Pts',(-3.21789591985027,0.909516980274446,
38.5043424945879));
#66452=CARTESIAN_POINT('Ctrl Pts',(-3.22545904493893,-0.00234722672036301,
38.5607734492731));
#66453=CARTESIAN_POINT('Origin',(0.,0.,-2.31077344927314));
#66454=CARTESIAN_POINT('',(-3.22733202596944,0.00141951042163625,35.8142265507269));
#66455=CARTESIAN_POINT('',(-3.22294839772763,0.00289713149391357,36.0607734492731));
#66456=CARTESIAN_POINT('',(-3.22275,7.67147279210326E-13,-2.31077344927314));
#66457=CARTESIAN_POINT('Ctrl Pts',(-3.22733202596944,0.00141951042163634,
35.8142265507269));
#66458=CARTESIAN_POINT('Ctrl Pts',(-3.22188327365915,-0.989180363824584,
35.8756214504846));
#66459=CARTESIAN_POINT('Ctrl Pts',(-2.20255972880747,-3.0591374276618,36.003311766909));
#66460=CARTESIAN_POINT('Ctrl Pts',(1.32400383155469,-3.57456197073556,36.1972975000001));
#66461=CARTESIAN_POINT('Ctrl Pts',(3.72301656637914,-0.818308191127896,
36.39618375));
#66462=CARTESIAN_POINT('Ctrl Pts',(2.7009133954788,2.68989738238965,36.5950700000001));
#66463=CARTESIAN_POINT('Ctrl Pts',(-0.803084758776685,3.72632936992902,
36.79395625));
#66464=CARTESIAN_POINT('Ctrl Pts',(-2.97803672572911,1.84884530856887,36.950341766909));
#66465=CARTESIAN_POINT('Ctrl Pts',(-3.22156066470263,0.388686230720639,
37.0404318671513));
#66466=CARTESIAN_POINT('Ctrl Pts',(-3.21910113068401,0.00223624140265662,
37.0642265507269));
#66467=CARTESIAN_POINT('Ctrl Pts',(-3.22294839772764,0.00289713149391371,
36.0607734492731));
#66468=CARTESIAN_POINT('Ctrl Pts',(-3.21539888225747,-0.823271536800272,
36.1117966106542));
#66469=CARTESIAN_POINT('Ctrl Pts',(-2.47182598037544,-2.73001053479381,
36.2288087917869));
#66470=CARTESIAN_POINT('Ctrl Pts',(0.732631374839026,-3.7347631354025,36.4118099926711));
#66471=CARTESIAN_POINT('Ctrl Pts',(3.53161527805439,-1.41876657738429,36.6097770519258));
#66472=CARTESIAN_POINT('Ctrl Pts',(3.11277826536447,2.18993404682541,36.8077441111804));
#66473=CARTESIAN_POINT('Ctrl Pts',(-0.14225523522422,3.80328436424815,37.0057111704351));
#66474=CARTESIAN_POINT('Ctrl Pts',(-2.78946082450622,2.23465375975559,37.1733876164659));
#66475=CARTESIAN_POINT('Ctrl Pts',(-3.21652605383795,0.579722601147174,
37.2750750427453));
#66476=CARTESIAN_POINT('Ctrl Pts',(-3.21767028658882,-0.000706682268057576,
37.3107734492731));
#66477=CARTESIAN_POINT('Origin',(0.,0.,-2.31077344927314));
#66478=CARTESIAN_POINT('',(-3.22346981451293,-0.00292769470226793,34.5642265507269));
#66479=CARTESIAN_POINT('',(-3.22696929196504,-0.00160766725765038,34.8107734492731));
#66480=CARTESIAN_POINT('',(-3.22275,7.67147279210326E-13,-2.31077344927314));
#66481=CARTESIAN_POINT('Ctrl Pts',(-3.22346981451293,-0.00292769470226783,
34.5642265507269));
#66482=CARTESIAN_POINT('Ctrl Pts',(-3.22557592068063,-0.229418253827942,
34.5782202004846));
#66483=CARTESIAN_POINT('Ctrl Pts',(-3.10033260871109,-1.52660312344819,
34.658509266909));
#66484=CARTESIAN_POINT('Ctrl Pts',(-1.34306394368559,-3.56744436540872,
34.8050937500001));
#66485=CARTESIAN_POINT('Ctrl Pts',(2.27535763353318,-3.05830470675803,35.00398));
#66486=CARTESIAN_POINT('Ctrl Pts',(3.80293119371364,0.261140562795601,35.2028662500001));
#66487=CARTESIAN_POINT('Ctrl Pts',(1.83595469168445,3.34062126768144,35.4017525000001));
#66488=CARTESIAN_POINT('Ctrl Pts',(-1.81809823225042,3.35037293181705,35.6006387500001));
#66489=CARTESIAN_POINT('Ctrl Pts',(-3.18922508991673,1.22879610595737,35.7381301002423));
#66490=CARTESIAN_POINT('Ctrl Pts',(-3.22776694324977,0.0804888053123557,
35.8093260338179));
#66491=CARTESIAN_POINT('Ctrl Pts',(-3.22733202596944,0.00141951042163634,
35.8142265507269));
#66492=CARTESIAN_POINT('Ctrl Pts',(-3.22696929196504,-0.00160766725764983,
34.8107734492731));
#66493=CARTESIAN_POINT('Ctrl Pts',(-3.22753990218318,-0.0946801960727776,
34.81654013906));
#66494=CARTESIAN_POINT('Ctrl Pts',(-3.18175512899714,-1.25222502802182,
34.8882958485986));
#66495=CARTESIAN_POINT('Ctrl Pts',(-1.78696199451318,-3.36035276851525,
35.0260405778887));
#66496=CARTESIAN_POINT('Ctrl Pts',(1.84582284769266,-3.32838428188693,35.2240076371433));
#66497=CARTESIAN_POINT('Ctrl Pts',(3.79679204988465,-0.263768978904437,
35.421974696398));
#66498=CARTESIAN_POINT('Ctrl Pts',(2.28832616929499,3.04117858234319,35.6199417556526));
#66499=CARTESIAN_POINT('Ctrl Pts',(-1.30514082959193,3.5751659222856,35.8179088149073));
#66500=CARTESIAN_POINT('Ctrl Pts',(-3.08976124773103,1.55359860142908,35.9648527127807));
#66501=CARTESIAN_POINT('Ctrl Pts',(-3.22516278382668,0.245224791032393,
36.0458075909027));
#66502=CARTESIAN_POINT('Ctrl Pts',(-3.22294839772764,0.00289713149391371,
36.0607734492731));
#66503=CARTESIAN_POINT('Origin',(0.,0.,-2.31077344927314));
#66504=CARTESIAN_POINT('',(-3.21741785881761,-7.00034835067217E-5,33.3142265507269));
#66505=CARTESIAN_POINT('',(-3.21834786352283,-0.00162040783760142,33.5607734492731));
#66506=CARTESIAN_POINT('',(-3.22275,7.67147279210326E-13,-2.31077344927314));
#66507=CARTESIAN_POINT('Ctrl Pts',(-3.21741785881761,-7.00034835066088E-5,
33.3142265507269));
#66508=CARTESIAN_POINT('Ctrl Pts',(-3.21752104774941,-0.534900734659731,
33.3471143671513));
#66509=CARTESIAN_POINT('Ctrl Pts',(-2.83756055391816,-2.14770788379053,
33.4462976002423));
#66510=CARTESIAN_POINT('Ctrl Pts',(-0.286187673586392,-3.80112834136171,
33.61177625));
#66511=CARTESIAN_POINT('Ctrl Pts',(3.0432488488294,-2.29545561834177,33.8106625000001));
#66512=CARTESIAN_POINT('Ctrl Pts',(3.57621472747308,1.31953335496755,34.00954875));
#66513=CARTESIAN_POINT('Ctrl Pts',(0.822962489122625,3.72199043445967,34.208435));
#66514=CARTESIAN_POINT('Ctrl Pts',(-2.43959062434672,2.7758812439376,34.3933276002424));
#66515=CARTESIAN_POINT('Ctrl Pts',(-3.21559816731754,0.843588877853916,
34.5119247838179));
#66516=CARTESIAN_POINT('Ctrl Pts',(-3.22346981451293,-0.00292769470226783,
34.5642265507269));
#66517=CARTESIAN_POINT('Ctrl Pts',(-3.21834786352283,-0.00162040783760153,
33.5607734492731));
#66518=CARTESIAN_POINT('Ctrl Pts',(-3.22031869209415,-0.432251674099872,
33.5872726872174));
#66519=CARTESIAN_POINT('Ctrl Pts',(-2.93972437209767,-1.93278809414023,
33.6797609449134));
#66520=CARTESIAN_POINT('Ctrl Pts',(-0.666791331988793,-3.74707795879318,
33.8382382223608));
#66521=CARTESIAN_POINT('Ctrl Pts',(2.78006191089306,-2.59931908033378,34.0362052816155));
#66522=CARTESIAN_POINT('Ctrl Pts',(3.69387053796041,0.916801155928787,34.2341723408701));
#66523=CARTESIAN_POINT('Ctrl Pts',(1.24202070877136,3.59758091881176,34.4321394001247));
#66524=CARTESIAN_POINT('Ctrl Pts',(-2.23710626490338,3.01783076015345,34.6243397695924));
#66525=CARTESIAN_POINT('Ctrl Pts',(-3.22101033143359,0.970361477603226,
34.7505511193085));
#66526=CARTESIAN_POINT('Ctrl Pts',(-3.22696929196504,-0.00160766725764983,
34.8107734492731));
#66527=CARTESIAN_POINT('Origin',(0.,0.,-2.31077344927314));
#66528=CARTESIAN_POINT('',(-3.22321200919049,0.00295167801057836,32.0642265507269));
#66529=CARTESIAN_POINT('',(-3.22115050171122,0.00280629626111237,32.3107734492731));
#66530=CARTESIAN_POINT('',(-3.22275,7.67147279210326E-13,-2.31077344927314));
#66531=CARTESIAN_POINT('Ctrl Pts',(-3.22321200919049,0.00295167801057841,
32.0642265507269));
#66532=CARTESIAN_POINT('Ctrl Pts',(-3.21541685821078,-0.835323973416723,
32.1160085338179));
#66533=CARTESIAN_POINT('Ctrl Pts',(-2.45212244763611,-2.75940586074536,
32.2340859335757));
#66534=CARTESIAN_POINT('Ctrl Pts',(0.793763968866624,-3.72832654331965,
32.41845875));
#66535=CARTESIAN_POINT('Ctrl Pts',(3.56576227116223,-1.34752346081344,32.6173450000001));
#66536=CARTESIAN_POINT('Ctrl Pts',(3.06114731919247,2.27153189325784,32.81623125));
#66537=CARTESIAN_POINT('Ctrl Pts',(-0.256385353190344,3.80325473806034,
33.0151175000001));
#66538=CARTESIAN_POINT('Ctrl Pts',(-2.82869405418981,2.16475235003571,33.1811159335757));
#66539=CARTESIAN_POINT('Ctrl Pts',(-3.21731303901023,0.543213595337759,
33.2808189504846));
#66540=CARTESIAN_POINT('Ctrl Pts',(-3.21741785881761,-7.00034835066088E-5,
33.3142265507269));
#66541=CARTESIAN_POINT('Ctrl Pts',(-3.22115050171122,0.00280629626111247,
32.3107734492731));
#66542=CARTESIAN_POINT('Ctrl Pts',(-3.21469754736738,-0.763061078972069,
32.3580052353748));
#66543=CARTESIAN_POINT('Ctrl Pts',(-2.55869281488842,-2.60888204696492,
32.4712260412281));
#66544=CARTESIAN_POINT('Ctrl Pts',(0.518024667143807,-3.77052441367253,
32.650435866833));
#66545=CARTESIAN_POINT('Ctrl Pts',(3.44477432083465,-1.61825022428116,32.8484029260877));
#66546=CARTESIAN_POINT('Ctrl Pts',(3.23282874888886,2.00848753798692,33.0463699853423));
#66547=CARTESIAN_POINT('Ctrl Pts',(0.0753014887309373,3.80519823342296,
33.2443370445969));
#66548=CARTESIAN_POINT('Ctrl Pts',(-2.71899596473592,2.35840681143994,33.4158048659072));
#66549=CARTESIAN_POINT('Ctrl Pts',(-3.21541088886627,0.640116338696104,
33.5212836674659));
#66550=CARTESIAN_POINT('Ctrl Pts',(-3.21834786352283,-0.00162040783760153,
33.5607734492731));
#66551=CARTESIAN_POINT('Origin',(0.,0.,-2.31077344927314));
#66552=CARTESIAN_POINT('',(-3.22747527198257,-0.00128106685233335,30.8142265507269));
#66553=CARTESIAN_POINT('',(-3.22784895015315,-0.000584129469891059,31.0607734492731));
#66554=CARTESIAN_POINT('',(-3.22275,7.67147279210326E-13,-2.31077344927314));
#66555=CARTESIAN_POINT('Ctrl Pts',(-3.22747527198257,-0.00128106685233375,
30.8142265507269));
#66556=CARTESIAN_POINT('Ctrl Pts',(-3.22783152828137,-0.0719553879082988,
30.8186072838179));
#66557=CARTESIAN_POINT('Ctrl Pts',(-3.19363801753637,-1.21182193198418,
30.8892834335756));
#66558=CARTESIAN_POINT('Ctrl Pts',(-1.84430286171068,-3.33601963516042,
31.0262550000001));
#66559=CARTESIAN_POINT('Ctrl Pts',(1.80971425616015,-3.35490899473305,31.22514125));
#66560=CARTESIAN_POINT('Ctrl Pts',(3.8007675342582,-0.290940204197991,31.4240275000001));
#66561=CARTESIAN_POINT('Ctrl Pts',(2.29925896103701,3.04037633887334,31.62291375));
#66562=CARTESIAN_POINT('Ctrl Pts',(-1.31506079077929,3.57786181516915,31.8218000000001));
#66563=CARTESIAN_POINT('Ctrl Pts',(-3.09455949069686,1.54366917503357,31.968904266909));
#66564=CARTESIAN_POINT('Ctrl Pts',(-3.22539683099921,0.237903243377298,
32.0497131171513));
#66565=CARTESIAN_POINT('Ctrl Pts',(-3.22321200919049,0.00295167801057841,
32.0642265507269));
#66566=CARTESIAN_POINT('Ctrl Pts',(-3.22784895015315,-0.000584129469891211,
31.0607734492731));
#66567=CARTESIAN_POINT('Ctrl Pts',(-3.22792887150411,-0.0324419667226371,
31.0627487637807));
#66568=CARTESIAN_POINT('Ctrl Pts',(-3.21309758646861,-1.12849329993279,
31.1307130980398));
#66569=CARTESIAN_POINT('Ctrl Pts',(-1.9760576970998,-3.25275266314625,31.2646664520505));
#66570=CARTESIAN_POINT('Ctrl Pts',(1.65261824030163,-3.42841900322799,31.4626335113052));
#66571=CARTESIAN_POINT('Ctrl Pts',(3.77551629574763,-0.480292213570351,
31.6606005705598));
#66572=CARTESIAN_POINT('Ctrl Pts',(2.45836462134124,2.90545130718283,31.8585676298145));
#66573=CARTESIAN_POINT('Ctrl Pts',(-1.0987182013029,3.64390206015446,32.0565346890691));
#66574=CARTESIAN_POINT('Ctrl Pts',(-3.04488911002489,1.67817047252684,32.207269962222));
#66575=CARTESIAN_POINT('Ctrl Pts',(-3.22371317363936,0.306956413960427,
32.2920162156233));
#66576=CARTESIAN_POINT('Ctrl Pts',(-3.22115050171122,0.00280629626111247,
32.3107734492731));
#66577=CARTESIAN_POINT('Origin',(0.,0.,-2.31077344927314));
#66578=CARTESIAN_POINT('',(-3.21928386531128,-0.0023275571713062,29.5642265507269));
#66579=CARTESIAN_POINT('',(-3.21951987652482,-0.0023462889869294,29.8107734492731));
#66580=CARTESIAN_POINT('',(-3.22275,7.67147279210326E-13,-2.31077344927314));
#66581=CARTESIAN_POINT('Ctrl Pts',(-3.21928386531128,-0.00232755717130651,
29.5642265507269));
#66582=CARTESIAN_POINT('Ctrl Pts',(-3.22179663352806,-0.380281685711084,
29.5875014504846));
#66583=CARTESIAN_POINT('Ctrl Pts',(-2.98525657845807,-1.8317424676862,29.677071766909));
#66584=CARTESIAN_POINT('Ctrl Pts',(-0.832267516579828,-3.71992081000873,
29.8329375));
#66585=CARTESIAN_POINT('Ctrl Pts',(2.67974690370432,-2.71098443078842,30.03182375));
#66586=CARTESIAN_POINT('Ctrl Pts',(3.72931611451176,0.789101622057042,30.2307100000001));
#66587=CARTESIAN_POINT('Ctrl Pts',(1.35198087098079,3.56407460309012,30.42959625));
#66588=CARTESIAN_POINT('Ctrl Pts',(-2.18797427827443,3.07500027700796,30.624101766909));
#66589=CARTESIAN_POINT('Ctrl Pts',(-3.2224401567282,0.997587874520822,30.7523118671513));
#66590=CARTESIAN_POINT('Ctrl Pts',(-3.22747527198257,-0.00128106685233375,
30.8142265507269));
#66591=CARTESIAN_POINT('Ctrl Pts',(-3.21951987652482,-0.00234628898692951,
29.8107734492731));
#66592=CARTESIAN_POINT('Ctrl Pts',(-3.22202184511065,-0.371027753442167,
29.8334813119381));
#66593=CARTESIAN_POINT('Ctrl Pts',(-2.9935553562486,-1.80809092066496,29.9221781943546));
#66594=CARTESIAN_POINT('Ctrl Pts',(-0.879815326883564,-3.70285415597931,
30.0768640965227));
#66595=CARTESIAN_POINT('Ctrl Pts',(2.62699068395643,-2.75392880377806,30.2748311557773));
#66596=CARTESIAN_POINT('Ctrl Pts',(3.74022244301854,0.70423006653559,30.4727982150319));
#66597=CARTESIAN_POINT('Ctrl Pts',(1.44556235449795,3.52073193940277,30.6707652742866));
#66598=CARTESIAN_POINT('Ctrl Pts',(-2.13017897797683,3.1332354492707,30.8667570190336));
#66599=CARTESIAN_POINT('Ctrl Pts',(-3.22525895155626,1.03182777038991,30.9967597440292));
#66600=CARTESIAN_POINT('Ctrl Pts',(-3.22784895015315,-0.000584129469891211,
31.0607734492731));
#66601=CARTESIAN_POINT('Origin',(0.,0.,-2.31077344927314));
#66602=CARTESIAN_POINT('',(-3.21898880855509,0.00217568322875482,28.3142265507269));
#66603=CARTESIAN_POINT('',(-3.2195784941175,0.00237125681338005,28.5607734492731));
#66604=CARTESIAN_POINT('',(-3.22275,7.67147279210326E-13,-2.31077344927314));
#66605=CARTESIAN_POINT('Ctrl Pts',(-3.21898880855509,0.00217568322875492,
28.3142265507269));
#66606=CARTESIAN_POINT('Ctrl Pts',(-3.21475771426579,-0.682752752100061,
28.3563956171513));
#66607=CARTESIAN_POINT('Ctrl Pts',(-2.66484322282807,-2.45068470257344,
28.4648601002423));
#66608=CARTESIAN_POINT('Ctrl Pts',(0.246873732837376,-3.80388399033473,
28.63962));
#66609=CARTESIAN_POINT('Ctrl Pts',(3.33371099678845,-1.8484726240282,28.8385062500001));
#66610=CARTESIAN_POINT('Ctrl Pts',(3.35716915487184,1.80551801914775,29.0373925));
#66611=CARTESIAN_POINT('Ctrl Pts',(0.295692279952789,3.80040078511023,29.23627875));
#66612=CARTESIAN_POINT('Ctrl Pts',(-2.64742839616081,2.47828694492588,29.4118901002423));
#66613=CARTESIAN_POINT('Ctrl Pts',(-3.21463935175017,0.696269736346894,
29.5212060338179));
#66614=CARTESIAN_POINT('Ctrl Pts',(-3.21928386531128,-0.00232755717130651,
29.5642265507269));
#66615=CARTESIAN_POINT('Ctrl Pts',(-3.2195784941175,0.00237125681337987,
28.5607734492731));
#66616=CARTESIAN_POINT('Ctrl Pts',(-3.2147354374273,-0.702888423299994,
28.6042138600955));
#66617=CARTESIAN_POINT('Ctrl Pts',(-2.64000685660925,-2.48666699441575,
28.7136432906694));
#66618=CARTESIAN_POINT('Ctrl Pts',(0.301725028063924,-3.79396440643719,
28.8890617409948));
#66619=CARTESIAN_POINT('Ctrl Pts',(3.34667671285774,-1.8124455549031,29.0870288002495));
#66620=CARTESIAN_POINT('Ctrl Pts',(3.34231449720922,1.8204773307068,29.2849958595041));
#66621=CARTESIAN_POINT('Ctrl Pts',(0.292613000107598,3.79467805512411,29.4829629187588));
#66622=CARTESIAN_POINT('Ctrl Pts',(-2.64330314849576,2.48151312137492,29.6582221153484));
#66623=CARTESIAN_POINT('Ctrl Pts',(-3.21475112761232,0.700360108942837,
29.7674922921865));
#66624=CARTESIAN_POINT('Ctrl Pts',(-3.21951987652482,-0.00234628898692951,
29.8107734492731));
#66625=CARTESIAN_POINT('Origin',(0.,0.,-2.31077344927314));
#66626=CARTESIAN_POINT('',(-3.22723414919969,0.00150563849211922,27.0642265507269));
#66627=CARTESIAN_POINT('',(-3.22786891212035,0.000537718463040557,27.3107734492731));
#66628=CARTESIAN_POINT('',(-3.22275,7.67147279210326E-13,-2.31077344927314));
#66629=CARTESIAN_POINT('Ctrl Pts',(-3.22723414919969,0.00150563849211919,
27.0642265507269));
#66630=CARTESIAN_POINT('Ctrl Pts',(-3.22154002065253,-0.983821934168731,
27.1252897838179));
#66631=CARTESIAN_POINT('Ctrl Pts',(-2.21180709545868,-3.04899464970893,
27.2526484335756));
#66632=CARTESIAN_POINT('Ctrl Pts',(1.30610950143672,-3.58113920731194,27.4463025));
#66633=CARTESIAN_POINT('Ctrl Pts',(3.71887727353106,-0.836918082194489,
27.6451887500001));
#66634=CARTESIAN_POINT('Ctrl Pts',(2.71433294268781,2.67635511995881,27.8440750000001));
#66635=CARTESIAN_POINT('Ctrl Pts',(-0.784438041578219,3.73029985534876,
28.04296125));
#66636=CARTESIAN_POINT('Ctrl Pts',(-2.973385007322,1.85975711368115,28.1996784335757));
#66637=CARTESIAN_POINT('Ctrl Pts',(-3.22140956081232,0.394046424575874,
28.2901002004846));
#66638=CARTESIAN_POINT('Ctrl Pts',(-3.21898880855509,0.00217568322875492,
28.3142265507269));
#66639=CARTESIAN_POINT('Ctrl Pts',(-3.22786891212035,0.000537718463040756,
27.3107734492731));
#66640=CARTESIAN_POINT('Ctrl Pts',(-3.22546512944508,-1.03442543785973,
27.3749464082529));
#66641=CARTESIAN_POINT('Ctrl Pts',(-2.12555463795461,-3.1380341292707,27.5051083869842));
#66642=CARTESIAN_POINT('Ctrl Pts',(1.45401317967913,-3.51725028725448,27.701259385467));
#66643=CARTESIAN_POINT('Ctrl Pts',(3.74190285747308,-0.695245938576497,
27.8992264447217));
#66644=CARTESIAN_POINT('Ctrl Pts',(2.6203695833697,2.76022954777739,28.0971935039762));
#66645=CARTESIAN_POINT('Ctrl Pts',(-0.888705147656408,3.70073061305487,
28.295160563231));
#66646=CARTESIAN_POINT('Ctrl Pts',(-2.99571736444363,1.80285265676093,28.4496872116632));
#66647=CARTESIAN_POINT('Ctrl Pts',(-3.22209237898327,0.368450315904827,
28.5382248403439));
#66648=CARTESIAN_POINT('Ctrl Pts',(-3.2195784941175,0.00237125681337987,
28.5607734492731));
#66649=CARTESIAN_POINT('Origin',(0.,0.,-2.31077344927314));
#66650=CARTESIAN_POINT('',(-3.22363407567384,-0.00290863082020876,25.8142265507269));
#66651=CARTESIAN_POINT('',(-3.22107869366301,-0.00279461251546875,26.0607734492731));
#66652=CARTESIAN_POINT('',(-3.22275,7.67147279210326E-13,-2.31077344927314));
#66653=CARTESIAN_POINT('Ctrl Pts',(-3.22363407567384,-0.0029086308202092,
25.8142265507269));
#66654=CARTESIAN_POINT('Ctrl Pts',(-3.22568756323173,-0.22400215866507,
25.827888533818));
#66655=CARTESIAN_POINT('Ctrl Pts',(-3.10397607047467,-1.51571554300823,
25.9078459335757));
#66656=CARTESIAN_POINT('Ctrl Pts',(-1.36088934335066,-3.56068255353444,
26.05409875));
#66657=CARTESIAN_POINT('Ctrl Pts',(2.26003338720418,-3.06964641947774,26.252985));
#66658=CARTESIAN_POINT('Ctrl Pts',(3.80418969631625,0.242117340005657,26.4518712500001));
#66659=CARTESIAN_POINT('Ctrl Pts',(1.852639496472,3.33139714654406,26.6507575));
#66660=CARTESIAN_POINT('Ctrl Pts',(-1.80131895941629,3.35942406646398,26.8496437500001));
#66661=CARTESIAN_POINT('Ctrl Pts',(-3.18637259141522,1.23963008315624,26.987466766909));
#66662=CARTESIAN_POINT('Ctrl Pts',(-3.22772204878106,0.0859331160642886,
27.0589943671513));
#66663=CARTESIAN_POINT('Ctrl Pts',(-3.22723414919969,0.00150563849211919,
27.0642265507269));
#66664=CARTESIAN_POINT('Ctrl Pts',(-3.22107869366301,-0.00279461251546882,
26.0607734492731));
#66665=CARTESIAN_POINT('Ctrl Pts',(-3.22364795624573,-0.309544392334381,
26.0796899366587));
#66666=CARTESIAN_POINT('Ctrl Pts',(-3.04291136040896,-1.68340601974217,
26.1645954437958));
#66667=CARTESIAN_POINT('Ctrl Pts',(-1.08996424799818,-3.64653011066113,
26.3154899706845));
#66668=CARTESIAN_POINT('Ctrl Pts',(2.46533493731419,-2.89953919730883,26.5134570299392));
#66669=CARTESIAN_POINT('Ctrl Pts',(3.77435199303925,0.489357683614875,26.7114240891938));
#66670=CARTESIAN_POINT('Ctrl Pts',(1.64438016964158,3.43237785908865,26.9093911484484));
#66671=CARTESIAN_POINT('Ctrl Pts',(-1.98386344368891,3.24799780582855,27.1073582077031));
#66672=CARTESIAN_POINT('Ctrl Pts',(-3.21433376763909,1.12330283478777,27.2411523079779));
#66673=CARTESIAN_POINT('Ctrl Pts',(-3.22793693789772,0.0298266279716151,
27.3089573885013));
#66674=CARTESIAN_POINT('Ctrl Pts',(-3.22786891212035,0.000537718463040756,
27.3107734492731));
#66675=CARTESIAN_POINT('Origin',(0.,0.,-2.31077344927314));
#66676=CARTESIAN_POINT('',(-3.21742354549419,-0.000159280653085815,24.5642265507269));
#66677=CARTESIAN_POINT('',(-3.21838772674461,0.00165536655674689,24.8107734492731));
#66678=CARTESIAN_POINT('',(-3.22275,7.67147279210326E-13,-2.31077344927314));
#66679=CARTESIAN_POINT('Ctrl Pts',(-3.21742354549419,-0.000159280653085694,
24.5642265507269));
#66680=CARTESIAN_POINT('Ctrl Pts',(-3.21765598864656,-0.529594024909045,
24.5967827004846));
#66681=CARTESIAN_POINT('Ctrl Pts',(-2.84316955446559,-2.13682872494597,
24.695634266909));
#66682=CARTESIAN_POINT('Ctrl Pts',(-0.305195037191488,-3.79964946293255,
24.86078125));
#66683=CARTESIAN_POINT('Ctrl Pts',(3.03173030730948,-2.3106473975125,25.0596675000001));
#66684=CARTESIAN_POINT('Ctrl Pts',(3.58276950661523,1.30163079033885,25.25855375));
#66685=CARTESIAN_POINT('Ctrl Pts',(0.841567339384293,3.7178279230179,25.4574400000001));
#66686=CARTESIAN_POINT('Ctrl Pts',(-2.43153772899687,2.78638001033204,25.642664266909));
#66687=CARTESIAN_POINT('Ctrl Pts',(-3.21572291810203,0.848864602558081,
25.7615931171513));
#66688=CARTESIAN_POINT('Ctrl Pts',(-3.22363407567384,-0.0029086308202092,
25.8142265507269));
#66689=CARTESIAN_POINT('Ctrl Pts',(-3.21838772674461,0.00165536655674668,
24.8107734492731));
#66690=CARTESIAN_POINT('Ctrl Pts',(-3.21537305131233,-0.642649371821592,
24.8504224848161));
#66691=CARTESIAN_POINT('Ctrl Pts',(-2.71592291202178,-2.36359214900197,
24.9560605401106));
#66692=CARTESIAN_POINT('Ctrl Pts',(0.0844394074013012,-3.80500642527053,
25.1276876151567));
#66693=CARTESIAN_POINT('Ctrl Pts',(3.23764278439912,-2.00071814869078,25.3256546744113));
#66694=CARTESIAN_POINT('Ctrl Pts',(3.44087817996476,1.6265181402354,25.523621733666));
#66695=CARTESIAN_POINT('Ctrl Pts',(0.50896830631917,3.77175757081959,25.7215887929206));
#66696=CARTESIAN_POINT('Ctrl Pts',(-2.56221901458568,2.60376870483498,25.9006393647896));
#66697=CARTESIAN_POINT('Ctrl Pts',(-3.21468523944414,0.760533623030957,
26.0137009169071));
#66698=CARTESIAN_POINT('Ctrl Pts',(-3.22107869366301,-0.00279461251546882,
26.0607734492731));
#66699=CARTESIAN_POINT('Origin',(0.,0.,-2.31077344927314));
#66700=CARTESIAN_POINT('',(-3.22304749582146,0.00296322048342273,23.3142265507269));
#66701=CARTESIAN_POINT('',(-3.22701991158836,0.00156882509208339,23.5607734492731));
#66702=CARTESIAN_POINT('',(-3.22275,7.67147279210326E-13,-2.31077344927314));
#66703=CARTESIAN_POINT('Ctrl Pts',(-3.22304749582146,0.00296322048342276,
23.3142265507269));
#66704=CARTESIAN_POINT('Ctrl Pts',(-3.21531008847461,-0.830052111865801,
23.3656768671513));
#66705=CARTESIAN_POINT('Ctrl Pts',(-2.460062449872,-2.74887948098658,23.4834226002424));
#66706=CARTESIAN_POINT('Ctrl Pts',(0.775107208778419,-3.73224983981374,
23.66746375));
#66707=CARTESIAN_POINT('Ctrl Pts',(3.55897817735421,-1.36534039162637,23.8663500000001));
#66708=CARTESIAN_POINT('Ctrl Pts',(3.07246986072833,2.25619347725455,24.06523625));
#66709=CARTESIAN_POINT('Ctrl Pts',(-0.237360568651399,3.80448945488611,
24.2641225));
#66710=CARTESIAN_POINT('Ctrl Pts',(-2.82298770437097,2.17562469080033,24.4304526002423));
#66711=CARTESIAN_POINT('Ctrl Pts',(-3.21718265516725,0.548515555906512,
24.5304872838179));
#66712=CARTESIAN_POINT('Ctrl Pts',(-3.21742354549419,-0.000159280653085694,
24.5642265507269));
#66713=CARTESIAN_POINT('Ctrl Pts',(-3.22701991158836,0.00156882509208334,
23.5607734492731));
#66714=CARTESIAN_POINT('Ctrl Pts',(-3.2211640532689,-0.972930212896847,
23.6211550329735));
#66715=CARTESIAN_POINT('Ctrl Pts',(-2.2327364184039,-3.02272099417933,23.7475256364254));
#66716=CARTESIAN_POINT('Ctrl Pts',(1.25065667292649,-3.59458784790924,23.9398852596288));
#66717=CARTESIAN_POINT('Ctrl Pts',(3.6960615727801,-0.90792772845131,24.1378523188835));
#66718=CARTESIAN_POINT('Ctrl Pts',(2.77381166227548,2.60598786875474,24.3358193781381));
#66719=CARTESIAN_POINT('Ctrl Pts',(-0.675787969966405,3.74546586281613,
24.5337864373928));
#66720=CARTESIAN_POINT('Ctrl Pts',(-2.94207777719568,1.92755146848088,24.6921044611044));
#66721=CARTESIAN_POINT('Ctrl Pts',(-3.22039046154491,0.429685365319261,
24.7844334650645));
#66722=CARTESIAN_POINT('Ctrl Pts',(-3.21838772674461,0.00165536655674668,
24.8107734492731));
#66723=CARTESIAN_POINT('Origin',(0.,0.,-2.31077344927314));
#66724=CARTESIAN_POINT('',(-3.22755990945695,-0.0011906676974904,22.0642265507269));
#66725=CARTESIAN_POINT('',(-3.22287078059728,-0.00290075263836898,22.3107734492731));
#66726=CARTESIAN_POINT('',(-3.22275,7.67147279210326E-13,-2.31077344927314));
#66727=CARTESIAN_POINT('Ctrl Pts',(-3.22755990945695,-0.0011906676974902,
22.0642265507269));
#66728=CARTESIAN_POINT('Ctrl Pts',(-3.22786903641777,-0.0665096632917848,
22.0682756171513));
#66729=CARTESIAN_POINT('Ctrl Pts',(-3.19641732350679,-1.20099399831007,
22.1386201002423));
#66730=CARTESIAN_POINT('Ctrl Pts',(-1.86096454568552,-3.32675382491574,
22.27526));
#66731=CARTESIAN_POINT('Ctrl Pts',(1.79291239805955,-3.36391812991553,22.47414625));
#66732=CARTESIAN_POINT('Ctrl Pts',(3.79926489107751,-0.309945703818892,
22.6730325));
#66733=CARTESIAN_POINT('Ctrl Pts',(2.31443632605062,3.02883881125214,22.87191875));
#66734=CARTESIAN_POINT('Ctrl Pts',(-1.29715004429138,3.58439420467181,23.070805));
#66735=CARTESIAN_POINT('Ctrl Pts',(-3.09083529909138,1.5545607399339,23.2182409335757));
#66736=CARTESIAN_POINT('Ctrl Pts',(-3.22527999108412,0.243315408215143,
23.2993814504846));
#66737=CARTESIAN_POINT('Ctrl Pts',(-3.22304749582146,0.00296322048342276,
23.3142265507269));
#66738=CARTESIAN_POINT('Ctrl Pts',(-3.22287078059728,-0.00290075263836877,
22.3107734492731));
#66739=CARTESIAN_POINT('Ctrl Pts',(-3.22510637863034,-0.247822164486929,
22.3258985613793));
#66740=CARTESIAN_POINT('Ctrl Pts',(-3.08796074838616,-1.55882789172308,
22.4070126932371));
#66741=CARTESIAN_POINT('Ctrl Pts',(-1.29655136755524,-3.57828987942048,
22.5541158448463));
#66742=CARTESIAN_POINT('Ctrl Pts',(2.29562293209663,-3.03567443305511,22.752082904101));
#66743=CARTESIAN_POINT('Ctrl Pts',(3.79614765886846,0.272886170297954,22.9500499633556));
#66744=CARTESIAN_POINT('Ctrl Pts',(1.83782445454307,3.3328074027996,23.1480170226103));
#66745=CARTESIAN_POINT('Ctrl Pts',(-1.79502668798453,3.35605171284586,23.3459840818649));
#66746=CARTESIAN_POINT('Ctrl Pts',(-3.18314642283721,1.24702165210228,23.4835695574192));
#66747=CARTESIAN_POINT('Ctrl Pts',(-3.22756372559652,0.0920672966887587,
23.5551660132219));
#66748=CARTESIAN_POINT('Ctrl Pts',(-3.22701991158836,0.00156882509208334,
23.5607734492731));
#66749=CARTESIAN_POINT('Origin',(0.,0.,-2.31077344927314));
#66750=CARTESIAN_POINT('',(-3.2194044849354,-0.00238303041332784,20.8142265507269));
#66751=CARTESIAN_POINT('',(-3.21768849251173,0.000747963174234367,21.0607734492731));
#66752=CARTESIAN_POINT('',(-3.22275,7.67147279210326E-13,-2.31077344927314));
#66753=CARTESIAN_POINT('Ctrl Pts',(-3.2194044849354,-0.00238303041332839,
20.8142265507269));
#66754=CARTESIAN_POINT('Ctrl Pts',(-3.22194656271802,-0.374916247463388,
20.8371697838179));
#66755=CARTESIAN_POINT('Ctrl Pts',(-2.98981931580154,-1.82082982892955,
20.9264084335756));
#66756=CARTESIAN_POINT('Ctrl Pts',(-0.850861899417176,-3.7157117864563,
21.0819425));
#66757=CARTESIAN_POINT('Ctrl Pts',(2.6661546849312,-2.724352996201,21.28082875));
#66758=CARTESIAN_POINT('Ctrl Pts',(3.73321608039316,0.770439971045078,21.479715));
#66759=CARTESIAN_POINT('Ctrl Pts',(1.36978930534994,3.55726823712227,21.67860125));
#66760=CARTESIAN_POINT('Ctrl Pts',(-2.17860797484293,3.08510098167624,21.8734384335757));
#66761=CARTESIAN_POINT('Ctrl Pts',(-3.22280769671063,1.00295909204903,22.0019802004846));
#66762=CARTESIAN_POINT('Ctrl Pts',(-3.22755990945695,-0.0011906676974902,
22.0642265507269));
#66763=CARTESIAN_POINT('Ctrl Pts',(-3.21768849251173,0.000747963174234575,
21.0607734492731));
#66764=CARTESIAN_POINT('Ctrl Pts',(-3.21647214829413,-0.582263006821988,
21.0966311095367));
#66765=CARTESIAN_POINT('Ctrl Pts',(-2.7866028252762,-2.23986331067818,21.1984777895519));
#66766=CARTESIAN_POINT('Ctrl Pts',(-0.133122145626393,-3.80361438689783,
21.3663134893184));
#66767=CARTESIAN_POINT('Ctrl Pts',(3.11802883817059,-2.18245276563067,21.5642805485732));
#66768=CARTESIAN_POINT('Ctrl Pts',(3.52819770926901,1.42724378933009,21.7622476078277));
#66769=CARTESIAN_POINT('Ctrl Pts',(0.723660398246818,3.73651168041552,21.9602146670825));
#66770=CARTESIAN_POINT('Ctrl Pts',(-2.47558847099782,2.72494770381142,22.1430566142308));
#66771=CARTESIAN_POINT('Ctrl Pts',(-3.21535273702263,0.820740089503346,
22.2599095416278));
#66772=CARTESIAN_POINT('Ctrl Pts',(-3.22287078059728,-0.00290075263836877,
22.3107734492731));
#66773=CARTESIAN_POINT('Origin',(0.,0.,-2.31077344927314));
#66774=CARTESIAN_POINT('',(-3.21887978231881,0.00211299402852188,19.5642265507269));
#66775=CARTESIAN_POINT('',(-3.22557758161264,0.00235737622836907,19.8107734492731));
#66776=CARTESIAN_POINT('',(-3.22275,7.67147279210326E-13,-2.31077344927314));
#66777=CARTESIAN_POINT('Ctrl Pts',(-3.21887978231881,0.00211299402852177,
19.5642265507269));
#66778=CARTESIAN_POINT('Ctrl Pts',(-3.21481144448344,-0.677486100948278,
19.6060639504846));
#66779=CARTESIAN_POINT('Ctrl Pts',(-2.67155366980303,-2.43992188292104,
19.714196766909));
#66780=CARTESIAN_POINT('Ctrl Pts',(0.227845920122608,-3.80507112792566,
19.8886250000001));
#66781=CARTESIAN_POINT('Ctrl Pts',(3.32442436079109,-1.86512270943999,20.08751125));
#66782=CARTESIAN_POINT('Ctrl Pts',(3.366157274749,1.78870490957689,20.2863975000001));
#66783=CARTESIAN_POINT('Ctrl Pts',(0.314695885881992,3.7988743795102,20.48528375));
#66784=CARTESIAN_POINT('Ctrl Pts',(-2.64057130871506,2.48902761712003,20.661226766909));
#66785=CARTESIAN_POINT('Ctrl Pts',(-3.21460112429926,0.701533821648526,
20.7708743671513));
#66786=CARTESIAN_POINT('Ctrl Pts',(-3.2194044849354,-0.00238303041332839,
20.8142265507269));
#66787=CARTESIAN_POINT('Ctrl Pts',(-3.22557758161264,0.00235737622836879,
19.8107734492731));
#66788=CARTESIAN_POINT('Ctrl Pts',(-3.21805665506623,-0.912024844401449,
19.8673636576941));
#66789=CARTESIAN_POINT('Ctrl Pts',(-2.33391015726838,-2.90537649651881,
19.9899428858666));
#66790=CARTESIAN_POINT('Ctrl Pts',(1.04321325149407,-3.66017896034874,20.1785111337906));
#66791=CARTESIAN_POINT('Ctrl Pts',(3.63814224250802,-1.11764257844405,20.3764781930453));
#66792=CARTESIAN_POINT('Ctrl Pts',(2.91818943772608,2.44323030339269,20.5744452522999));
#66793=CARTESIAN_POINT('Ctrl Pts',(-0.460662442187536,3.77796162291654,
20.7724123115546));
#66794=CARTESIAN_POINT('Ctrl Pts',(-2.88379934488129,2.0521538463159,20.9345217105456));
#66795=CARTESIAN_POINT('Ctrl Pts',(-3.21871059224195,0.490654805763857,
21.0306420897851));
#66796=CARTESIAN_POINT('Ctrl Pts',(-3.21768849251173,0.000747963174234575,
21.0607734492731));
#66797=CARTESIAN_POINT('Origin',(0.,0.,-2.31077344927314));
#66798=CARTESIAN_POINT('',(-3.22713146099961,0.00158994899472997,18.3142265507269));
#66799=CARTESIAN_POINT('',(-3.22470148543098,-0.00263455512554606,18.5607734492731));
#66800=CARTESIAN_POINT('',(-3.22275,7.67147279210326E-13,-2.31077344927314));
#66801=CARTESIAN_POINT('Ctrl Pts',(-3.22713146099961,0.00158994899473025,
18.3142265507269));
#66802=CARTESIAN_POINT('Ctrl Pts',(-3.22120609028706,-0.978468238727024,
18.3749581171513));
#66803=CARTESIAN_POINT('Ctrl Pts',(-2.22100824016265,-3.03883590904923,
18.5019851002423));
#66804=CARTESIAN_POINT('Ctrl Pts',(1.28818247537154,-3.58762678689348,18.6953075));
#66805=CARTESIAN_POINT('Ctrl Pts',(3.71464500371619,-0.855507187729257,
18.89419375));
#66806=CARTESIAN_POINT('Ctrl Pts',(2.72768450257131,2.6627461963774,19.09308));
#66807=CARTESIAN_POINT('Ctrl Pts',(-0.76577152881775,3.73417648452,19.29196625));
#66808=CARTESIAN_POINT('Ctrl Pts',(-2.96869873438807,1.87066944191426,19.4490151002423));
#66809=CARTESIAN_POINT('Ctrl Pts',(-3.22125812026871,0.399404562159262,
19.5397685338179));
#66810=CARTESIAN_POINT('Ctrl Pts',(-3.21887978231881,0.00211299402852177,
19.5642265507269));
#66811=CARTESIAN_POINT('Ctrl Pts',(-3.22470148543098,-0.00263455512554578,
18.5607734492731));
#66812=CARTESIAN_POINT('Ctrl Pts',(-3.22632095927964,-0.185893923124646,
18.5721071860999));
#66813=CARTESIAN_POINT('Ctrl Pts',(-3.12886753636446,-1.43443236269005,
18.6494299426783));
#66814=CARTESIAN_POINT('Ctrl Pts',(-1.49890159705929,-3.49835645871106,
18.7927417190082));
#66815=CARTESIAN_POINT('Ctrl Pts',(2.1184092557461,-3.16188964624663,18.9907087782628));
#66816=CARTESIAN_POINT('Ctrl Pts',(3.80553821630163,0.0555229154508125,
19.1886758375175));
#66817=CARTESIAN_POINT('Ctrl Pts',(2.02526306905968,3.2223459483698,19.3866428967721));
#66818=CARTESIAN_POINT('Ctrl Pts',(-1.60032411708034,3.45313866361654,19.5846099560268));
#66819=CARTESIAN_POINT('Ctrl Pts',(-3.14819898127591,1.37103695231587,19.7259868068604));
#66820=CARTESIAN_POINT('Ctrl Pts',(-3.22682669822862,0.154222976577529,
19.8013746379425));
#66821=CARTESIAN_POINT('Ctrl Pts',(-3.22557758161264,0.00235737622836879,
19.8107734492731));
#66822=CARTESIAN_POINT('Origin',(0.,0.,-2.31077344927314));
#66823=CARTESIAN_POINT('',(-3.22379796809719,-0.00288664070778104,17.0642265507269));
#66824=CARTESIAN_POINT('',(-3.2175431274752,-0.000244872741176072,17.3107734492731));
#66825=CARTESIAN_POINT('',(-3.22275,7.67147279210326E-13,-2.31077344927314));
#66826=CARTESIAN_POINT('Ctrl Pts',(-3.22379796809719,-0.00288664070778058,
17.0642265507269));
#66827=CARTESIAN_POINT('Ctrl Pts',(-3.22579710476995,-0.218584582317807,
17.0775568671513));
#66828=CARTESIAN_POINT('Ctrl Pts',(-3.10758827702004,-1.50482958829351,
17.1571826002423));
#66829=CARTESIAN_POINT('Ctrl Pts',(-1.37868070132254,-3.55383167520506,
17.30310375));
#66830=CARTESIAN_POINT('Ctrl Pts',(2.24465260765735,-3.08091134614859,17.50199));
#66831=CARTESIAN_POINT('Ctrl Pts',(3.80535304148599,0.223088057823076,17.70087625));
#66832=CARTESIAN_POINT('Ctrl Pts',(1.8692779572903,3.32208969931257,17.8997625000001));
#66833=CARTESIAN_POINT('Ctrl Pts',(-1.78449462466053,3.36839115698396,18.09864875));
#66834=CARTESIAN_POINT('Ctrl Pts',(-3.18349141863527,1.25046640358126,18.2368034335757));
#66835=CARTESIAN_POINT('Ctrl Pts',(-3.2276743067916,0.09137681447932,18.3086627004846));
#66836=CARTESIAN_POINT('Ctrl Pts',(-3.22713146099961,0.00158994899473025,
18.3142265507269));
#66837=CARTESIAN_POINT('Ctrl Pts',(-3.2175431274752,-0.000244872741175725,
17.3107734492731));
#66838=CARTESIAN_POINT('Ctrl Pts',(-3.21789832634533,-0.521670563510979,
17.3428397342573));
#66839=CARTESIAN_POINT('Ctrl Pts',(-2.85221365971589,-2.11566531376391,
17.440895038993));
#66840=CARTESIAN_POINT('Ctrl Pts',(-0.350248680105062,-3.78979284024299,
17.6049393634804));
#66841=CARTESIAN_POINT('Ctrl Pts',(2.98822575042405,-2.3570555306091,17.8029064227349));
#66842=CARTESIAN_POINT('Ctrl Pts',(3.60398774105126,1.2233054697109,18.0008734819896));
#66843=CARTESIAN_POINT('Ctrl Pts',(0.935987701844621,3.68905556096245,18.1988405412443));
#66844=CARTESIAN_POINT('Ctrl Pts',(-2.38326531404954,2.84480349181404,18.3854738636721));
#66845=CARTESIAN_POINT('Ctrl Pts',(-3.21689181041029,0.881106858642543,
18.5061181663484));
#66846=CARTESIAN_POINT('Ctrl Pts',(-3.22470148543098,-0.00263455512554578,
18.5607734492731));
#66847=CARTESIAN_POINT('Origin',(0.,0.,-2.31077344927314));
#66848=CARTESIAN_POINT('',(-3.2174336584483,-0.000248419282747805,15.8142265507269));
#66849=CARTESIAN_POINT('',(-3.22381398336647,0.00281172170752172,16.0607734492731));
#66850=CARTESIAN_POINT('',(-3.22275,7.67147279210326E-13,-2.31077344927314));
#66851=CARTESIAN_POINT('Ctrl Pts',(-3.2174336584483,-0.000248419282747846,
15.8142265507269));
#66852=CARTESIAN_POINT('Ctrl Pts',(-3.21779255326727,-0.524285427231881,
15.8464510338179));
#66853=CARTESIAN_POINT('Ctrl Pts',(-2.84874083961618,-2.1259470999027,15.9449709335756));
#66854=CARTESIAN_POINT('Ctrl Pts',(-0.324194766610495,-3.79807553969012,
16.10978625));
#66855=CARTESIAN_POINT('Ctrl Pts',(3.02013592975928,-2.32578137787433,16.3086725));
#66856=CARTESIAN_POINT('Ctrl Pts',(3.58923466600481,1.2836956665189,16.5075587500001));
#66857=CARTESIAN_POINT('Ctrl Pts',(0.86015113855453,3.71357241355724,16.706445));
#66858=CARTESIAN_POINT('Ctrl Pts',(-2.4234406942069,2.79686770301245,16.8920009335757));
#66859=CARTESIAN_POINT('Ctrl Pts',(-3.21585483524874,0.854142010055347,
17.0112614504846));
#66860=CARTESIAN_POINT('Ctrl Pts',(-3.22379796809719,-0.00288664070778058,
17.0642265507269));
#66861=CARTESIAN_POINT('Ctrl Pts',(-3.22381398336647,0.00281172170752176,
16.0607734492731));
#66862=CARTESIAN_POINT('Ctrl Pts',(-3.21602073876447,-0.851519211745776,
16.1135722824147));
#66863=CARTESIAN_POINT('Ctrl Pts',(-2.42919148351035,-2.7862976707188,16.2323601353078));
#66864=CARTESIAN_POINT('Ctrl Pts',(0.832360802113325,-3.71380928494957,
16.4171370079525));
#66865=CARTESIAN_POINT('Ctrl Pts',(3.56833413631518,-1.32370517921483,16.6151040672071));
#66866=CARTESIAN_POINT('Ctrl Pts',(3.05303110985611,2.27248871331039,16.8130711264618));
#66867=CARTESIAN_POINT('Ctrl Pts',(-0.244031554753848,3.79811170322264,
17.0110381857164));
#66868=CARTESIAN_POINT('Ctrl Pts',(-2.82070996455941,2.17652677557168,17.1769389599869));
#66869=CARTESIAN_POINT('Ctrl Pts',(-3.21716736467427,0.551368306571193,
17.2768507145058));
#66870=CARTESIAN_POINT('Ctrl Pts',(-3.2175431274752,-0.000244872741175725,
17.3107734492731));
#66871=CARTESIAN_POINT('Origin',(0.,0.,-2.31077344927314));
#66872=CARTESIAN_POINT('',(-3.22288314929224,0.0029718364718792,14.5642265507269));
#66873=CARTESIAN_POINT('',(-3.2263403267092,-0.00200868097619572,14.8107734492731));
#66874=CARTESIAN_POINT('',(-3.22275,7.67147279210326E-13,-2.31077344927314));
#66875=CARTESIAN_POINT('Ctrl Pts',(-3.22288314929224,0.00297183647187928,
14.5642265507269));
#66876=CARTESIAN_POINT('Ctrl Pts',(-3.21521016001633,-0.824781581368616,
14.6153452004846));
#66877=CARTESIAN_POINT('Ctrl Pts',(-2.4679586424349,-2.73834265879665,14.732759266909));
#66878=CARTESIAN_POINT('Ctrl Pts',(0.756431060077252,-3.73607977741916,
14.91646875));
#66879=CARTESIAN_POINT('Ctrl Pts',(3.55210505889249,-1.38312316967087,15.115355));
#66880=CARTESIAN_POINT('Ctrl Pts',(3.08371554718117,2.24079862458972,15.31424125));
#66881=CARTESIAN_POINT('Ctrl Pts',(-0.21832984675111,3.80562900581595,15.5131275));
#66882=CARTESIAN_POINT('Ctrl Pts',(-2.81724322909883,2.18649418273475,15.679789266909));
#66883=CARTESIAN_POINT('Ctrl Pts',(-3.21705419909425,0.553815707628409,
15.7801556171513));
#66884=CARTESIAN_POINT('Ctrl Pts',(-3.2174336584483,-0.000248419282747846,
15.8142265507269));
#66885=CARTESIAN_POINT('Ctrl Pts',(-3.2263403267092,-0.00200868097619563,
14.8107734492731));
#66886=CARTESIAN_POINT('Ctrl Pts',(-3.22723124442984,-0.123802489841831,
14.8183158108205));
#66887=CARTESIAN_POINT('Ctrl Pts',(-3.16578983988483,-1.31027741920305,
14.8918471921195));
#66888=CARTESIAN_POINT('Ctrl Pts',(-1.696353693388,-3.4069910561669,15.03136759317));
#66889=CARTESIAN_POINT('Ctrl Pts',(1.93427300977863,-3.27777238891207,15.2293346524246));
#66890=CARTESIAN_POINT('Ctrl Pts',(3.80249297873402,-0.162021778014253,
15.4273017116793));
#66891=CARTESIAN_POINT('Ctrl Pts',(2.2060834984687,3.10135446340087,15.6252687709339));
#66892=CARTESIAN_POINT('Ctrl Pts',(-1.40039198296493,3.53894139594313,15.8232358301886));
#66893=CARTESIAN_POINT('Ctrl Pts',(-3.10934499764541,1.49531585790812,15.9684040563016));
#66894=CARTESIAN_POINT('Ctrl Pts',(-3.225760889093,0.216240386100458,16.0475832626631));
#66895=CARTESIAN_POINT('Ctrl Pts',(-3.22381398336647,0.00281172170752176,
16.0607734492731));
#66896=CARTESIAN_POINT('Origin',(0.,0.,-2.31077344927314));
#66897=CARTESIAN_POINT('',(-3.22763904405734,-0.00109877613235525,13.3142265507269));
#66898=CARTESIAN_POINT('',(-3.21796438773957,-0.00120981133772902,13.5607734492731));
#66899=CARTESIAN_POINT('',(-3.22275,7.67147279210326E-13,-2.31077344927314));
#66900=CARTESIAN_POINT('Ctrl Pts',(-3.22763904405734,-0.00109877613235536,
13.3142265507269));
#66901=CARTESIAN_POINT('Ctrl Pts',(-3.22790364316531,-0.0610634584561656,
13.3179439504846));
#66902=CARTESIAN_POINT('Ctrl Pts',(-3.19916828701905,-1.19016844739519,
13.387956766909));
#66903=CARTESIAN_POINT('Ctrl Pts',(-1.87757967929805,-3.31740479890186,
13.524265));
#66904=CARTESIAN_POINT('Ctrl Pts',(1.77606569186011,-3.37284311969702,13.72315125));
#66905=CARTESIAN_POINT('Ctrl Pts',(3.79766721268626,-0.32894345042547,13.9220375));
#66906=CARTESIAN_POINT('Ctrl Pts',(2.32955579751124,3.01722551993911,14.12092375));
#66907=CARTESIAN_POINT('Ctrl Pts',(-1.2792068507562,3.59083693376187,14.31981));
#66908=CARTESIAN_POINT('Ctrl Pts',(-3.08707946816032,1.56545378025357,14.4675776002423));
#66909=CARTESIAN_POINT('Ctrl Pts',(-3.22516120574105,0.248725993520245,
14.5490497838179));
#66910=CARTESIAN_POINT('Ctrl Pts',(-3.22288314929224,0.00297183647187928,
14.5642265507269));
#66911=CARTESIAN_POINT('Ctrl Pts',(-3.21796438773957,-0.00120981133772905,
13.5607734492731));
#66912=CARTESIAN_POINT('Ctrl Pts',(-3.21952342447733,-0.460834059410147,
13.5890483589779));
#66913=CARTESIAN_POINT('Ctrl Pts',(-2.91292585124894,-1.99116214018758,
13.6833122884343));
#66914=CARTESIAN_POINT('Ctrl Pts',(-0.566230666680783,-3.76358695156398,
13.8435652376421));
#66915=CARTESIAN_POINT('Ctrl Pts',(2.84865769364129,-2.52395587408549,14.0415322968968));
#66916=CARTESIAN_POINT('Ctrl Pts',(3.66800060750612,1.01536961408498,14.2394993561514));
#66917=CARTESIAN_POINT('Ctrl Pts',(1.14525637075743,3.62954429028107,14.4374664154061));
#66918=CARTESIAN_POINT('Ctrl Pts',(-2.28511410901714,2.96306899170226,14.6278911131133));
#66919=CARTESIAN_POINT('Ctrl Pts',(-3.21943649915082,0.941786054053766,
14.752326791069));
#66920=CARTESIAN_POINT('Ctrl Pts',(-3.2263403267092,-0.00200868097619563,
14.8107734492731));
#66921=CARTESIAN_POINT('Origin',(0.,0.,-2.31077344927314));
#66922=CARTESIAN_POINT('',(-3.21952816226103,-0.00243635184806505,12.0642265507269));
#66923=CARTESIAN_POINT('',(-3.2219754753083,0.00289434104541186,12.3107734492731));
#66924=CARTESIAN_POINT('',(-3.22275,7.67147279210326E-13,-2.31077344927314));
#66925=CARTESIAN_POINT('Ctrl Pts',(-3.21952816226103,-0.00243635184806499,
12.0642265507269));
#66926=CARTESIAN_POINT('Ctrl Pts',(-3.22209591491135,-0.369548780530837,
12.0868381171513));
#66927=CARTESIAN_POINT('Ctrl Pts',(-2.99434768393422,-1.80991726839579,
12.1757451002423));
#66928=CARTESIAN_POINT('Ctrl Pts',(-0.869434998705811,-3.71140981769939,
12.3309475));
#66929=CARTESIAN_POINT('Ctrl Pts',(2.65249577468504,-2.73765341436203,12.52983375));
#66930=CARTESIAN_POINT('Ctrl Pts',(3.73702266321591,0.751759048166815,12.72872));
#66931=CARTESIAN_POINT('Ctrl Pts',(1.38756347566574,3.55037288927353,12.92760625));
#66932=CARTESIAN_POINT('Ctrl Pts',(-2.16919521531468,3.09518493566959,13.1227751002423));
#66933=CARTESIAN_POINT('Ctrl Pts',(-3.22318483183059,1.00833554596791,13.2516485338179));
#66934=CARTESIAN_POINT('Ctrl Pts',(-3.22763904405734,-0.00109877613235536,
13.3142265507269));
#66935=CARTESIAN_POINT('Ctrl Pts',(-3.2219754753083,0.00289434104541197,
12.3107734492731));
#66936=CARTESIAN_POINT('Ctrl Pts',(-3.21492550593893,-0.791248393644031,
12.3597809071353));
#66937=CARTESIAN_POINT('Ctrl Pts',(-2.51870961379289,-2.66576186073892,
12.474777384749));
#66938=CARTESIAN_POINT('Ctrl Pts',(0.61878835158859,-3.75530356773067,12.6557628821143));
#66939=CARTESIAN_POINT('Ctrl Pts',(3.48686537418057,-1.52544215629862,12.853729941369));
#66940=CARTESIAN_POINT('Ctrl Pts',(3.17789604102199,2.09432105044312,13.0516970006236));
#66941=CARTESIAN_POINT('Ctrl Pts',(-0.0266032173364325,3.80585025699904,
13.2496640598783));
#66942=CARTESIAN_POINT('Ctrl Pts',(-2.75263818088242,2.30051682698361,13.4193562094281));
#66943=CARTESIAN_POINT('Ctrl Pts',(-3.21588488744377,0.611853843079764,
13.5230593392264));
#66944=CARTESIAN_POINT('Ctrl Pts',(-3.21796438773957,-0.00120981133772905,
13.5607734492731));
#66945=CARTESIAN_POINT('Origin',(0.,0.,-2.31077344927314));
#66946=CARTESIAN_POINT('',(-3.21877418690567,0.0020484167724553,10.8142265507269));
#66947=CARTESIAN_POINT('',(-3.22752742220963,-0.00108629272672134,11.0607734492731));
#66948=CARTESIAN_POINT('',(-3.22275,7.67147279210326E-13,-2.31077344927314));
#66949=CARTESIAN_POINT('Ctrl Pts',(-3.21877418690567,0.0020484167724549,
10.8142265507269));
#66950=CARTESIAN_POINT('Ctrl Pts',(-3.21486930714951,-0.672218600580391,
10.8557322838179));
#66951=CARTESIAN_POINT('Ctrl Pts',(-2.67822325513316,-2.42915317683481,
10.9635334335756));
#66952=CARTESIAN_POINT('Ctrl Pts',(0.208812408046019,-3.80616308506823,
11.13763));
#66953=CARTESIAN_POINT('Ctrl Pts',(3.31505456729397,-1.88172614047672,11.33651625));
#66954=CARTESIAN_POINT('Ctrl Pts',(3.37506119321498,1.77184705715372,11.5354025));
#66955=CARTESIAN_POINT('Ctrl Pts',(0.333691619975345,3.79725294846791,11.73428875));
#66956=CARTESIAN_POINT('Ctrl Pts',(-2.6336728682884,2.49976175320687,11.9105634335756));
#66957=CARTESIAN_POINT('Ctrl Pts',(-3.21456745674729,0.706797323328607,
12.0205427004846));
#66958=CARTESIAN_POINT('Ctrl Pts',(-3.21952816226103,-0.00243635184806499,
12.0642265507269));
#66959=CARTESIAN_POINT('Ctrl Pts',(-3.22752742220963,-0.0010862927267216,
11.0607734492731));
#66960=CARTESIAN_POINT('Ctrl Pts',(-3.22779342624244,-0.0615982436869706,
11.0645244355411));
#66961=CARTESIAN_POINT('Ctrl Pts',(-3.1988784036326,-1.18640415769286,11.1342644415607));
#66962=CARTESIAN_POINT('Ctrl Pts',(-1.88826241961219,-3.30449223702413,
11.2699934673318));
#66963=CARTESIAN_POINT('Ctrl Pts',(1.74381591738736,-3.38294397768258,11.4679605265865));
#66964=CARTESIAN_POINT('Ctrl Pts',(3.78702189743871,-0.379037014277084,
11.6659275858411));
#66965=CARTESIAN_POINT('Ctrl Pts',(2.37969485505221,2.97022832568649,11.8638946450958));
#66966=CARTESIAN_POINT('Ctrl Pts',(-1.1958836268722,3.61317952236688,12.0618617043504));
#66967=CARTESIAN_POINT('Ctrl Pts',(-3.0664299399447,1.61980912775541,12.2108213057429));
#66968=CARTESIAN_POINT('Ctrl Pts',(-3.2244183584201,0.278072540168287,12.2937918873838));
#66969=CARTESIAN_POINT('Ctrl Pts',(-3.2219754753083,0.00289434104541197,
12.3107734492731));
#66970=CARTESIAN_POINT('Origin',(0.,0.,-2.31077344927314));
#66971=CARTESIAN_POINT('',(-3.22702415133123,0.00167235368052675,9.56422655072689));
#66972=CARTESIAN_POINT('',(-3.21891511857495,-0.00203587595620058,9.8107734492731));
#66973=CARTESIAN_POINT('',(-3.22275,7.67147279210326E-13,-2.31077344927314));
#66974=CARTESIAN_POINT('Ctrl Pts',(-3.22702415133123,0.00167235368052666,
9.56422655072689));
#66975=CARTESIAN_POINT('Ctrl Pts',(-3.22088140544128,-0.973119137173498,
9.6246264504846));
#66976=CARTESIAN_POINT('Ctrl Pts',(-2.23016324609443,-3.02866137559854,
9.75132176690898));
#66977=CARTESIAN_POINT('Ctrl Pts',(1.27022322657475,-3.59402462520223,9.94431250000001));
#66978=CARTESIAN_POINT('Ctrl Pts',(3.71031981538147,-0.874074893517518,
10.14319875));
#66979=CARTESIAN_POINT('Ctrl Pts',(2.74096783186856,2.64907066658324,10.342085));
#66980=CARTESIAN_POINT('Ctrl Pts',(-0.747085860967871,3.73795970660893,
10.54097125));
#66981=CARTESIAN_POINT('Ctrl Pts',(-2.96397756792535,1.88158151294885,10.698351766909));
#66982=CARTESIAN_POINT('Ctrl Pts',(-3.22110641251276,0.404760638936827,
10.7894368671513));
#66983=CARTESIAN_POINT('Ctrl Pts',(-3.21877418690567,0.0020484167724549,
10.8142265507269));
#66984=CARTESIAN_POINT('Ctrl Pts',(-3.21891511857495,-0.00203587595620017,
9.8107734492731));
#66985=CARTESIAN_POINT('Ctrl Pts',(-3.22122774117535,-0.39973470628387,
9.83525698369852));
#66986=CARTESIAN_POINT('Ctrl Pts',(-2.96891139380953,-1.86649717402379,
9.92572953787549));
#66987=CARTESIAN_POINT('Ctrl Pts',(-0.780362316170466,-3.72508235685782,
10.082191111804));
#66988=CARTESIAN_POINT('Ctrl Pts',(2.6997807504167,-2.68260839660801,10.2801581710586));
#66989=CARTESIAN_POINT('Ctrl Pts',(3.72002712642615,0.80411571836772,10.4781252303133));
#66990=CARTESIAN_POINT('Ctrl Pts',(1.35078255368256,3.55817234019647,10.6760922895679));
#66991=CARTESIAN_POINT('Ctrl Pts',(-2.18101206117008,3.07945714130881,10.8703083625545));
#66992=CARTESIAN_POINT('Ctrl Pts',(-3.22311376491591,1.00295492760852,10.9985354157896));
#66993=CARTESIAN_POINT('Ctrl Pts',(-3.22752742220963,-0.0010862927267216,
11.0607734492731));
#66994=CARTESIAN_POINT('Origin',(0.,0.,-2.31077344927314));
#66995=CARTESIAN_POINT('',(-3.22396133703721,-0.00286173073963965,8.31422655072689));
#66996=CARTESIAN_POINT('',(-3.22027572892457,0.00261454196279293,8.5607734492731));
#66997=CARTESIAN_POINT('',(-3.22275,7.67147279210326E-13,-2.31077344927314));
#66998=CARTESIAN_POINT('Ctrl Pts',(-3.22396133703721,-0.00286173073963985,
8.31422655072689));
#66999=CARTESIAN_POINT('Ctrl Pts',(-3.22590450377897,-0.213165553777342,
8.32722520048459));
#67000=CARTESIAN_POINT('Ctrl Pts',(-3.11116933513409,-1.49394529920932,
8.40651926690897));
#67001=CARTESIAN_POINT('Ctrl Pts',(-1.39643757283078,-3.54689190095731,
8.55210875000002));
#67002=CARTESIAN_POINT('Ctrl Pts',(2.22921568013466,-3.09209920657986,8.75099500000001));
#67003=CARTESIAN_POINT('Ctrl Pts',(3.80642119915558,0.204053195292361,8.94988125000001));
#67004=CARTESIAN_POINT('Ctrl Pts',(1.88586965979368,3.3126991529808,9.14876750000002));
#67005=CARTESIAN_POINT('Ctrl Pts',(-1.76762565236893,3.37727399021419,9.34765375000001));
#67006=CARTESIAN_POINT('Ctrl Pts',(-3.18058147267209,1.26130503966291,9.4861401002423));
#67007=CARTESIAN_POINT('Ctrl Pts',(-3.22762373282734,0.0968198578997676,
9.55833103381793));
#67008=CARTESIAN_POINT('Ctrl Pts',(-3.22702415133123,0.00167235368052666,
9.56422655072689));
#67009=CARTESIAN_POINT('Ctrl Pts',(-3.22027572892457,0.00261454196279275,
8.5607734492731));
#67010=CARTESIAN_POINT('Ctrl Pts',(-3.21463452458948,-0.73107245854707,
8.60598953185591));
#67011=CARTESIAN_POINT('Ctrl Pts',(-2.60260549049518,-2.54402617904789,
8.71719463419026));
#67012=CARTESIAN_POINT('Ctrl Pts',(0.403193815184867,-3.78452621305085,
8.89438875627614));
#67013=CARTESIAN_POINT('Ctrl Pts',(3.39400218094999,-1.72219427056852,9.0923558155308));
#67014=CARTESIAN_POINT('Ctrl Pts',(3.29237619572427,1.90930953375835,9.29032287478543));
#67015=CARTESIAN_POINT('Ctrl Pts',(0.190912054474585,3.80115199608339,9.48828993404008));
#67016=CARTESIAN_POINT('Ctrl Pts',(-2.67941498037181,2.42394983134342,9.6617734588693));
#67017=CARTESIAN_POINT('Ctrl Pts',(-3.21499466649732,0.672159388484275,
9.76926796394697));
#67018=CARTESIAN_POINT('Ctrl Pts',(-3.21891511857495,-0.00203587595620017,
9.8107734492731));
#67019=CARTESIAN_POINT('Origin',(0.,0.,-2.31077344927314));
#67020=CARTESIAN_POINT('',(-3.21744819095025,-0.00033734180616485,7.06422655072688));
#67021=CARTESIAN_POINT('',(-3.22798100933232,1.20436113847002E-5,7.3107734492731));
#67022=CARTESIAN_POINT('',(-3.22275,7.67147279210326E-13,-2.31077344927314));
#67023=CARTESIAN_POINT('Ctrl Pts',(-3.21744819095025,-0.00033734180616498,
7.06422655072688));
#67024=CARTESIAN_POINT('Ctrl Pts',(-3.21793065745993,-0.518974922087274,
7.09611936715126));
#67025=CARTESIAN_POINT('Ctrl Pts',(-2.85427452458422,-2.11506311315496,
7.1943076002423));
#67026=CARTESIAN_POINT('Ctrl Pts',(-0.343186386587714,-3.79640661098804,
7.35879125000001));
#67027=CARTESIAN_POINT('Ctrl Pts',(3.00846600621214,-2.34085718089664,7.55767750000001));
#67028=CARTESIAN_POINT('Ctrl Pts',(3.5956100439019,1.26572843220077,7.75656375000002));
#67029=CARTESIAN_POINT('Ctrl Pts',(0.878713421813992,3.70922401240668,7.95545000000001));
#67030=CARTESIAN_POINT('Ctrl Pts',(-2.41529942916466,2.8073441425483,8.14133760024231));
#67031=CARTESIAN_POINT('Ctrl Pts',(-3.21599400913541,0.859421202136209,
8.26092978381793));
#67032=CARTESIAN_POINT('Ctrl Pts',(-3.22396133703721,-0.00286173073963985,
8.31422655072689));
#67033=CARTESIAN_POINT('Ctrl Pts',(-3.22798098720893,1.20435604489447E-5,
7.31077344927309));
#67034=CARTESIAN_POINT('Ctrl Pts',(-3.22792175517501,-1.0634891969682,7.37672208001329));
#67035=CARTESIAN_POINT('Ctrl Pts',(-2.07326176640397,-3.19125327047275,
7.50865973050503));
#67036=CARTESIAN_POINT('Ctrl Pts',(1.5476603571224,-3.4770607312591,7.70658640074832));
#67037=CARTESIAN_POINT('Ctrl Pts',(3.75917552904779,-0.594813627685692,
7.90455346000295));
#67038=CARTESIAN_POINT('Ctrl Pts',(2.54552980900885,2.82939603119107,8.1025205192576));
#67039=CARTESIAN_POINT('Ctrl Pts',(-0.987467344283091,3.67561044642204,
8.30048757851224));
#67040=CARTESIAN_POINT('Ctrl Pts',(-3.01929261435194,1.74445015182628,8.45323855518407));
#67041=CARTESIAN_POINT('Ctrl Pts',(-3.22286738164004,0.339681202596263,
8.54000051210436));
#67042=CARTESIAN_POINT('Ctrl Pts',(-3.22027572892457,0.00261454196279275,
8.5607734492731));
#67043=CARTESIAN_POINT('Origin',(0.,0.,-2.31077344927314));
#67044=CARTESIAN_POINT('',(-3.22271911507513,0.00297753179786089,5.81422655072688));
#67045=CARTESIAN_POINT('',(-3.22030921936247,-0.00262401028225973,6.0607734492731));
#67046=CARTESIAN_POINT('',(-3.22275,7.67147279210326E-13,-2.31077344927314));
#67047=CARTESIAN_POINT('Ctrl Pts',(-3.22271911507513,0.00297753179786076,
5.81422655072688));
#67048=CARTESIAN_POINT('Ctrl Pts',(-3.21511698107986,-0.819512286718065,
5.86501353381793));
#67049=CARTESIAN_POINT('Ctrl Pts',(-2.47581111925387,-2.72779556832849,
5.98209593357564));
#67050=CARTESIAN_POINT('Ctrl Pts',(0.737735989926837,-3.73981626035058,
6.16547375000001));
#67051=CARTESIAN_POINT('Ctrl Pts',(3.5451430877039,-1.4008713501182,6.36436000000001));
#67052=CARTESIAN_POINT('Ctrl Pts',(3.09488409724894,2.22534772034816,6.56324625000001));
#67053=CARTESIAN_POINT('Ctrl Pts',(-0.19929366352457,3.8066733623451,6.76213250000001));
#67054=CARTESIAN_POINT('Ctrl Pts',(-2.81146051372698,2.19736071579676,6.92912593357563));
#67055=CARTESIAN_POINT('Ctrl Pts',(-3.21692775706187,0.559114075328717,
7.02982395048459));
#67056=CARTESIAN_POINT('Ctrl Pts',(-3.21744819095025,-0.00033734180616498,
7.06422655072688));
#67057=CARTESIAN_POINT('Ctrl Pts',(-3.22030921936247,-0.00262401028225941,
6.0607734492731));
#67058=CARTESIAN_POINT('Ctrl Pts',(-3.22290205123769,-0.338371123515593,
6.08146560841913));
#67059=CARTESIAN_POINT('Ctrl Pts',(-3.02034206694596,-1.74179359390663,
6.16814678731671));
#67060=CARTESIAN_POINT('Ctrl Pts',(-0.991943885951175,-3.67440488202038,
6.32081698596584));
#67061=CARTESIAN_POINT('Ctrl Pts',(2.54208142306422,-2.83249465107694,6.51878404522046));
#67062=CARTESIAN_POINT('Ctrl Pts',(3.75989728477033,0.590234121215191,6.71675110447512));
#67063=CARTESIAN_POINT('Ctrl Pts',(1.55189462906941,3.47517294104057,6.91471816372975));
#67064=CARTESIAN_POINT('Ctrl Pts',(-2.07011190883012,3.19371892858329,7.1126852229844));
#67065=CARTESIAN_POINT('Ctrl Pts',(-3.22768646466942,1.06546721490889,7.24470365149884));
#67066=CARTESIAN_POINT('Ctrl Pts',(-3.22798102348448,0.000663365099614621,
7.31073306026174));
#67067=CARTESIAN_POINT('Ctrl Pts',(-3.22798098720893,1.20435604489447E-5,
7.31077344927309));
#67068=CARTESIAN_POINT('Origin',(0.,0.,-2.31077344927314));
#67069=CARTESIAN_POINT('',(-3.22771248049277,-0.0010054936160085,4.56422655072689));
#67070=CARTESIAN_POINT('',(-3.21888985043626,0.0020204358260266,4.81077344927309));
#67071=CARTESIAN_POINT('',(-3.22275,7.67147279210326E-13,-2.31077344927314));
#67072=CARTESIAN_POINT('Ctrl Pts',(-3.22771248049277,-0.00100549361600838,
4.56422655072689));
#67073=CARTESIAN_POINT('Ctrl Pts',(-3.22793533636644,-0.0556168128984164,
4.56761228381793));
#67074=CARTESIAN_POINT('Ctrl Pts',(-3.20189100109211,-1.17934529311488,
4.63729343357563));
#67075=CARTESIAN_POINT('Ctrl Pts',(-1.89414784662335,-3.30797278933611,
4.77327));
#67076=CARTESIAN_POINT('Ctrl Pts',(1.75917455880395,-3.38168374168425,4.97215625000001));
#67077=CARTESIAN_POINT('Ctrl Pts',(3.79597453913422,-0.347932968357942,
5.17104250000001));
#67078=CARTESIAN_POINT('Ctrl Pts',(2.34461699717418,3.0055367551961,5.36992875000001));
#67079=CARTESIAN_POINT('Ctrl Pts',(-1.26123165898331,3.59718984140266,5.56881500000001));
#67080=CARTESIAN_POINT('Ctrl Pts',(-3.0832918894214,1.576348251431,5.71691426690897));
#67081=CARTESIAN_POINT('Ctrl Pts',(-3.22504052073703,0.254134972951963,
5.79871811715126));
#67082=CARTESIAN_POINT('Ctrl Pts',(-3.22271911507513,0.00297753179786076,
5.81422655072688));
#67083=CARTESIAN_POINT('Ctrl Pts',(-3.21888985043626,0.00202043582602666,
4.81077344927309));
#67084=CARTESIAN_POINT('Ctrl Pts',(-3.21500861080956,-0.670875972885779,
4.85219815657651));
#67085=CARTESIAN_POINT('Ctrl Pts',(-2.68102990457166,-2.42132711321019,
4.95961188363147));
#67086=CARTESIAN_POINT('Ctrl Pts',(0.186281715928623,-3.80138172682447,
5.133014630438));
#67087=CARTESIAN_POINT('Ctrl Pts',(3.290048016384,-1.91331857244767,5.33098168969263));
#67088=CARTESIAN_POINT('Ctrl Pts',(3.39609747398096,1.71805874664089,5.52894874894727));
#67089=CARTESIAN_POINT('Ctrl Pts',(0.407803461009433,3.78403227353958,5.72691580820191));
#67090=CARTESIAN_POINT('Ctrl Pts',(-2.60087562294228,2.54663069375663,5.90419070831052));
#67091=CARTESIAN_POINT('Ctrl Pts',(-3.21463329433229,0.732354397698439,
6.01547658866758));
#67092=CARTESIAN_POINT('Ctrl Pts',(-3.22030921936247,-0.00262401028225941,
6.0607734492731));
#67093=CARTESIAN_POINT('Origin',(0.,0.,-2.31077344927314));
#67094=CARTESIAN_POINT('',(-3.21965480394772,-0.00248744593871922,3.31422655072688));
#67095=CARTESIAN_POINT('',(-3.22750875009338,0.00110830861146782,3.5607734492731));
#67096=CARTESIAN_POINT('',(-3.22275,7.67147279210326E-13,-2.31077344927314));
#67097=CARTESIAN_POINT('Ctrl Pts',(-3.21965480394772,-0.00248744593871947,
3.31422655072688));
#67098=CARTESIAN_POINT('Ctrl Pts',(-3.22224462500577,-0.364179297671712,
3.33650645048459));
#67099=CARTESIAN_POINT('Ctrl Pts',(-2.99884181667278,-1.7990049583156,3.42508176690897));
#67100=CARTESIAN_POINT('Ctrl Pts',(-0.887986334554333,-3.70701493094446,
3.5799525));
#67101=CARTESIAN_POINT('Ctrl Pts',(2.63877050663273,-2.75088539460193,3.77883875000001));
#67102=CARTESIAN_POINT('Ctrl Pts',(3.74073577194275,0.7330593426781,3.977725));
#67103=CARTESIAN_POINT('Ctrl Pts',(1.40530293513768,3.54338872054109,4.17661125000001));
#67104=CARTESIAN_POINT('Ctrl Pts',(-2.15973593176927,3.1052519319067,4.37211176690896));
#67105=CARTESIAN_POINT('Ctrl Pts',(-3.22357163651051,1.01371738125969,4.50131686715126));
#67106=CARTESIAN_POINT('Ctrl Pts',(-3.22771248049277,-0.00100549361600838,
4.56422655072689));
#67107=CARTESIAN_POINT('Ctrl Pts',(-3.22750875009338,0.0011083086114679,
3.5607734492731));
#67108=CARTESIAN_POINT('Ctrl Pts',(-3.22302278853548,-1.00164523556617,
3.6229307047339));
#67109=CARTESIAN_POINT('Ctrl Pts',(-2.18329284268058,-3.07699904328362,
3.75107697994624));
#67110=CARTESIAN_POINT('Ctrl Pts',(1.34644732705721,-3.55981509909713,3.94521227491016));
#67111=CARTESIAN_POINT('Ctrl Pts',(3.71904487139598,-0.808646497252913,
4.14317933416478));
#67112=CARTESIAN_POINT('Ctrl Pts',(2.70304644183217,2.67931779227495,4.34114639341943));
#67113=CARTESIAN_POINT('Ctrl Pts',(-0.775824200771678,3.72603015619545,
4.53911345267407));
#67114=CARTESIAN_POINT('Ctrl Pts',(-2.96776667705998,1.869154056941,4.69565580462529));
#67115=CARTESIAN_POINT('Ctrl Pts',(-3.22119137503552,0.401039251040587,
4.78620913682497));
#67116=CARTESIAN_POINT('Ctrl Pts',(-3.21888985043626,0.00202043582602666,
4.81077344927309));
#67117=CARTESIAN_POINT('Origin',(0.,0.,-2.31077344927314));
#67118=CARTESIAN_POINT('',(-3.21867136367194,0.00198586312807969,2.06422655072688));
#67119=CARTESIAN_POINT('',(-3.22201388411817,-0.00289643951356,2.31077344927309));
#67120=CARTESIAN_POINT('',(-3.22275,7.67147279210326E-13,-2.31077344927314));
#67121=CARTESIAN_POINT('Ctrl Pts',(-3.21867136367194,0.00198586312807971,
2.06422655072688));
#67122=CARTESIAN_POINT('Ctrl Pts',(-3.21493076087555,-0.666947841793965,
2.10540061715126));
#67123=CARTESIAN_POINT('Ctrl Pts',(-2.68485324646853,-2.41838481311705,
2.2128701002423));
#67124=CARTESIAN_POINT('Ctrl Pts',(0.189774422820439,-3.8071558930084,2.386635));
#67125=CARTESIAN_POINT('Ctrl Pts',(3.30560145857767,-1.89828456209197,2.58552125000001));
#67126=CARTESIAN_POINT('Ctrl Pts',(3.38388089250329,1.75494596051086,2.7844075));
#67127=CARTESIAN_POINT('Ctrl Pts',(0.35267889993612,3.79553596959835,2.98329375));
#67128=CARTESIAN_POINT('Ctrl Pts',(-2.62673293070242,2.5104894057472,3.1599001002423));
#67129=CARTESIAN_POINT('Ctrl Pts',(-3.2145384293764,0.712060374694048,3.27021103381792));
#67130=CARTESIAN_POINT('Ctrl Pts',(-3.21965480394772,-0.00248744593871947,
3.31422655072688));
#67131=CARTESIAN_POINT('Ctrl Pts',(-3.22201388411817,-0.00289643951355986,
2.3107734492731));
#67132=CARTESIAN_POINT('Ctrl Pts',(-3.22444943885979,-0.276757467136012,
2.32767423313974));
#67133=CARTESIAN_POINT('Ctrl Pts',(-3.0673879406931,-1.61715552525174,2.41056403675793));
#67134=CARTESIAN_POINT('Ctrl Pts',(-1.20028377732907,-3.61171960603965,
2.55944286012766));
#67135=CARTESIAN_POINT('Ctrl Pts',(2.37607494490469,-2.97312511164363,2.75740991938231));
#67136=CARTESIAN_POINT('Ctrl Pts',(3.78748084593007,0.374423891696219,2.95537697863694));
#67137=CARTESIAN_POINT('Ctrl Pts',(1.74793537283732,3.38081724446415,3.15334403789159));
#67138=CARTESIAN_POINT('Ctrl Pts',(-1.88423579077553,3.30678992389447,3.35131109714622));
#67139=CARTESIAN_POINT('Ctrl Pts',(-3.19821240522555,1.18904022922726,3.48712090094007));
#67140=CARTESIAN_POINT('Ctrl Pts',(-3.22778529298737,0.0629243459269913,
3.55694168498235));
#67141=CARTESIAN_POINT('Ctrl Pts',(-3.22750875009338,0.0011083086114679,
3.5607734492731));
#67142=CARTESIAN_POINT('Origin',(0.,0.,-2.31077344927314));
#67143=CARTESIAN_POINT('',(-3.22687103957968,0.00196979923060657,0.814226550726883));
#67144=CARTESIAN_POINT('',(-3.217941538466,0.00121291371900201,1.06077344927309));
#67145=CARTESIAN_POINT('',(-3.22275,7.67147279210326E-13,-2.31077344927314));
#67146=CARTESIAN_POINT('Ctrl Pts',(-3.22687103957968,0.00196979923060637,
0.814226550726882));
#67147=CARTESIAN_POINT('Ctrl Pts',(-3.2205120016493,-0.967490928436361,
0.874294783817922));
#67148=CARTESIAN_POINT('Ctrl Pts',(-2.23933917473902,-3.01882333308509,
1.00065843357563));
#67149=CARTESIAN_POINT('Ctrl Pts',(1.25226897486165,-3.60013934158935,1.1933175));
#67150=CARTESIAN_POINT('Ctrl Pts',(3.70588259587967,-0.892721732175661,
1.39220375));
#67151=CARTESIAN_POINT('Ctrl Pts',(2.75419264545516,2.63538166557444,1.59109));
#67152=CARTESIAN_POINT('Ctrl Pts',(-0.728386757290071,3.7416218310534,1.78997625));
#67153=CARTESIAN_POINT('Ctrl Pts',(-2.95922030312456,1.89249897579954,1.94768843357563));
#67154=CARTESIAN_POINT('Ctrl Pts',(-3.22095360103943,0.410119412946076,
2.03910520048459));
#67155=CARTESIAN_POINT('Ctrl Pts',(-3.21867136367194,0.00198586312807971,
2.06422655072688));
#67156=CARTESIAN_POINT('Ctrl Pts',(-3.217941538466,0.00121291371900208,
1.06077344927309));
#67157=CARTESIAN_POINT('Ctrl Pts',(-3.21590426000095,-0.610555186325359,
1.09840678129712));
#67158=CARTESIAN_POINT('Ctrl Pts',(-2.75415550932367,-2.29791887119263,
1.2020291330727));
#67159=CARTESIAN_POINT('Ctrl Pts',(-0.031229830088373,-3.80578923437654,
1.37164050459982));
#67160=CARTESIAN_POINT('Ctrl Pts',(3.17533772956661,-2.09820398373205,1.56960756385447));
#67161=CARTESIAN_POINT('Ctrl Pts',(3.48872347062518,1.52120070666785,1.7675746231091));
#67162=CARTESIAN_POINT('Ctrl Pts',(0.623360915472078,3.75454335133777,1.96554168236375));
#67163=CARTESIAN_POINT('Ctrl Pts',(-2.51686097994096,2.66834479637078,2.14660795775174));
#67164=CARTESIAN_POINT('Ctrl Pts',(-3.21493982846427,0.792531442985166,
2.26168521338819));
#67165=CARTESIAN_POINT('Ctrl Pts',(-3.22201388411817,-0.00289643951355986,
2.3107734492731));
#67166=CARTESIAN_POINT('Origin',(0.,0.,39.5));
#67167=CARTESIAN_POINT('',(-3.73150059045713,-0.00288452150806035,39.2732311074181));
#67168=CARTESIAN_POINT('',(-3.5,-4.28626379701574E-16,39.5));
#67169=CARTESIAN_POINT('',(-3.48038110743704,-1.8235874740856,39.067));
#67170=CARTESIAN_POINT('Origin',(0.,0.,39.067));
#67171=CARTESIAN_POINT('Ctrl Pts',(-3.17710367210747,0.540490350682819,
39.77725));
#67172=CARTESIAN_POINT('Ctrl Pts',(-3.1637561532367,0.643070260528315,39.7732046970049));
#67173=CARTESIAN_POINT('Ctrl Pts',(-3.14512387900806,0.744684739103562,
39.7691738072623));
#67174=CARTESIAN_POINT('Ctrl Pts',(-3.12151814966561,0.845073767043372,
39.765152624555));
#67175=CARTESIAN_POINT('Ctrl Pts',(-3.09733288315468,0.947927415845119,
39.7610327189993));
#67176=CARTESIAN_POINT('Ctrl Pts',(-3.06792673767774,1.04949536878747,39.7569230029586));
#67177=CARTESIAN_POINT('Ctrl Pts',(-3.0335800607437,1.1494940547227,39.7528184150135));
#67178=CARTESIAN_POINT('Ctrl Pts',(-3.01568867325577,1.20158396262813,39.7506803108369));
#67179=CARTESIAN_POINT('Ctrl Pts',(-2.99645584073005,1.25324793479459,39.748543598133));
#67180=CARTESIAN_POINT('Ctrl Pts',(-2.97591588140006,1.304444537542,39.7464075614997));
#67181=CARTESIAN_POINT('Ctrl Pts',(-2.95980998271904,1.34458908132685,39.7447326414553));
#67182=CARTESIAN_POINT('Ctrl Pts',(-2.9429003211764,1.38444624584374,39.7430581370943));
#67183=CARTESIAN_POINT('Ctrl Pts',(-2.92520201085857,1.42399545129445,39.7413837035064));
#67184=CARTESIAN_POINT('Ctrl Pts',(-2.91751988870009,1.44116216507032,39.7406568994705));
#67185=CARTESIAN_POINT('Ctrl Pts',(-2.90969226795577,1.45826383112552,39.739930405335));
#67186=CARTESIAN_POINT('Ctrl Pts',(-2.90172327003567,1.47529356600236,39.7392044208686));
#67187=CARTESIAN_POINT('Ctrl Pts',(-2.85583879382635,1.57334861290315,39.7350242946709));
#67188=CARTESIAN_POINT('Ctrl Pts',(-2.80524636043718,1.66907618183903,39.7308586839284));
#67189=CARTESIAN_POINT('Ctrl Pts',(-2.750243849884,1.76218023578936,39.7267023800362));
#67190=CARTESIAN_POINT('Ctrl Pts',(-2.69481297715921,1.85600938854582,39.7225137066514));
#67191=CARTESIAN_POINT('Ctrl Pts',(-2.63490262455043,1.94717477698571,39.7183344856458));
#67192=CARTESIAN_POINT('Ctrl Pts',(-2.57076808318315,2.03535422259479,39.7141593857696));
#67193=CARTESIAN_POINT('Ctrl Pts',(-2.52863418965378,2.09328468087148,39.7114165079084));
#67194=CARTESIAN_POINT('Ctrl Pts',(-2.48467614357889,2.1499259994421,39.7086754087175));
#67195=CARTESIAN_POINT('Ctrl Pts',(-2.43895623479167,2.20517989437012,39.7059345765588));
#67196=CARTESIAN_POINT('Ctrl Pts',(-2.42734309124643,2.21921473018352,39.7052383880025));
#67197=CARTESIAN_POINT('Ctrl Pts',(-2.41561528860901,2.2331610124895,39.7045421643251));
#67198=CARTESIAN_POINT('Ctrl Pts',(-2.4037857568947,2.24700338325728,39.7038465751243));
#67199=CARTESIAN_POINT('Ctrl Pts',(-2.32918331887211,2.33429970505841,39.6994598714493));
#67200=CARTESIAN_POINT('Ctrl Pts',(-2.25043676277322,2.41759162180438,39.695092178329));
#67201=CARTESIAN_POINT('Ctrl Pts',(-2.16787254687766,2.49653395502271,39.6907375286809));
#67202=CARTESIAN_POINT('Ctrl Pts',(-2.08896125763975,2.57198360620801,39.6865755438041));
#67203=CARTESIAN_POINT('Ctrl Pts',(-2.0065617522895,2.6434606176488,39.6824254737553));
#67204=CARTESIAN_POINT('Ctrl Pts',(-1.92091521567439,2.7106349143576,39.6782821089402));
#67205=CARTESIAN_POINT('Ctrl Pts',(-1.83647215399636,2.77686530153194,39.6741969652268));
#67206=CARTESIAN_POINT('Ctrl Pts',(-1.7488721079392,2.83891368138453,39.670118339632));
#67207=CARTESIAN_POINT('Ctrl Pts',(-1.65831288783304,2.8964261348381,39.6660412391006));
#67208=CARTESIAN_POINT('Ctrl Pts',(-1.60536482584606,2.93005245082131,39.6636574445912));
#67209=CARTESIAN_POINT('Ctrl Pts',(-1.55140458800842,2.96212741030792,39.6612741714238));
#67210=CARTESIAN_POINT('Ctrl Pts',(-1.49646745549095,2.99257286153937,39.6588904216258));
#67211=CARTESIAN_POINT('Ctrl Pts',(-1.47911222300954,3.00219090783902,39.6581373693636));
#67212=CARTESIAN_POINT('Ctrl Pts',(-1.46165947603105,3.01164628460064,39.6573842695339));
#67213=CARTESIAN_POINT('Ctrl Pts',(-1.44411027186853,3.02093639848886,39.6566310906727));
#67214=CARTESIAN_POINT('Ctrl Pts',(-1.43026822018143,3.02826403770424,39.6560370158287));
#67215=CARTESIAN_POINT('Ctrl Pts',(-1.4163660931799,3.03548881054269,39.6554428905506));
#67216=CARTESIAN_POINT('Ctrl Pts',(-1.40241741124474,3.04260302573126,39.6548492486502));
#67217=CARTESIAN_POINT('Ctrl Pts',(-1.37807141460219,3.05502016018889,39.6538131074733));
#67218=CARTESIAN_POINT('Ctrl Pts',(-1.35357391445438,3.06710568910055,39.6527780219686));
#67219=CARTESIAN_POINT('Ctrl Pts',(-1.32892886492452,3.07885484871252,39.6517439135451));
#67220=CARTESIAN_POINT('Ctrl Pts',(-1.23400338476844,3.12410915490678,39.647760832135));
#67221=CARTESIAN_POINT('Ctrl Pts',(-1.13689144605682,3.16437662481258,39.6437922463479));
#67222=CARTESIAN_POINT('Ctrl Pts',(-1.03799851206363,3.19978018187908,39.6398336653046));
#67223=CARTESIAN_POINT('Ctrl Pts',(-0.936477173525234,3.23612470476135,
39.6357698719678));
#67224=CARTESIAN_POINT('Ctrl Pts',(-0.833078244337451,3.26734351361957,
39.6317166222599));
#67225=CARTESIAN_POINT('Ctrl Pts',(-0.728211962825303,3.29352264453908,
39.6276690576209));
#67226=CARTESIAN_POINT('Ctrl Pts',(-0.617268825661175,3.32121881980685,
39.6233869422216));
#67227=CARTESIAN_POINT('Ctrl Pts',(-0.504682531853149,3.34327483273434,
39.6191111898655));
#67228=CARTESIAN_POINT('Ctrl Pts',(-0.390918860121393,3.35973481018611,
39.6148360474606));
#67229=CARTESIAN_POINT('Ctrl Pts',(-0.341147253738749,3.36693605032126,
39.6129656726584));
#67230=CARTESIAN_POINT('Ctrl Pts',(-0.291150118517647,3.37306540876564,
39.6110954146048));
#67231=CARTESIAN_POINT('Ctrl Pts',(-0.240966022436918,3.37812300320975,
39.6092247915343));
#67232=CARTESIAN_POINT('Ctrl Pts',(-0.221881410394732,3.38004636609502,
39.6085134084794));
#67233=CARTESIAN_POINT('Ctrl Pts',(-0.202769759382229,3.38181470580387,
39.607801972635));
#67234=CARTESIAN_POINT('Ctrl Pts',(-0.183633192552594,3.38342794592711,
39.6070904575048));
#67235=CARTESIAN_POINT('Ctrl Pts',(-0.167412090454507,3.38479540817783,
39.6064873420309));
#67236=CARTESIAN_POINT('Ctrl Pts',(-0.1511812000706,3.38605072283508,39.6058844713497));
#67237=CARTESIAN_POINT('Ctrl Pts',(-0.134946694431332,3.3871938790219,39.60528200838));
#67238=CARTESIAN_POINT('Ctrl Pts',(-0.023532027885713,3.39503916659603,
39.6011474069104));
#67239=CARTESIAN_POINT('Ctrl Pts',(0.0881235026197957,3.39761219426123,
39.5970293228263));
#67240=CARTESIAN_POINT('Ctrl Pts',(0.199587753616714,3.39501220725874,39.5929227595484));
#67241=CARTESIAN_POINT('Ctrl Pts',(0.312322033150521,3.39238259589096,39.5887694059094));
#67242=CARTESIAN_POINT('Ctrl Pts',(0.424861556474873,3.38446148342019,39.5846278371095));
#67243=CARTESIAN_POINT('Ctrl Pts',(0.5367716407479,3.37129955295751,39.5804928838223));
#67244=CARTESIAN_POINT('Ctrl Pts',(0.648325420202415,3.35817952809499,39.5763710956022));
#67245=CARTESIAN_POINT('Ctrl Pts',(0.759254700367378,3.33985196600234,39.5722558808363));
#67246=CARTESIAN_POINT('Ctrl Pts',(0.869127285875629,3.31631566032459,39.5681421194162));
#67247=CARTESIAN_POINT('Ctrl Pts',(0.917101131057039,3.30603896500971,39.5663459210964));
#67248=CARTESIAN_POINT('Ctrl Pts',(0.96487341532449,3.29476857839289,39.5645499998529));
#67249=CARTESIAN_POINT('Ctrl Pts',(1.01240736146384,3.28250133365881,39.5627539294746));
#67250=CARTESIAN_POINT('Ctrl Pts',(1.05037596096517,3.27270264997857,39.561319285764));
#67251=CARTESIAN_POINT('Ctrl Pts',(1.0881924854212,3.2622679046368,39.5598845469008));
#67252=CARTESIAN_POINT('Ctrl Pts',(1.12583783052174,3.25119462790972,39.5584494956716));
#67253=CARTESIAN_POINT('Ctrl Pts',(1.14120725447008,3.24667375330859,39.5578636088729));
#67254=CARTESIAN_POINT('Ctrl Pts',(1.15654804398256,3.24204639639838,39.557277672997));
#67255=CARTESIAN_POINT('Ctrl Pts',(1.1718450966984,3.23731682728628,39.5566922030335));
#67256=CARTESIAN_POINT('Ctrl Pts',(1.28064083705401,3.20367917285225,39.5525282219505));
#67257=CARTESIAN_POINT('Ctrl Pts',(1.38740105523547,3.16482439786729,39.5483810786623));
#67258=CARTESIAN_POINT('Ctrl Pts',(1.49169195653895,3.12080692440921,39.544245675923));
#67259=CARTESIAN_POINT('Ctrl Pts',(1.59451171588211,3.07741036755443,39.5401686077499));
#67260=CARTESIAN_POINT('Ctrl Pts',(1.69493222231264,3.02899558619786,39.5361029512343));
#67261=CARTESIAN_POINT('Ctrl Pts',(1.79252890400652,2.97556546513603,39.5320438218091));
#67262=CARTESIAN_POINT('Ctrl Pts',(1.83909299894021,2.95007356124892,39.530107181294));
#67263=CARTESIAN_POINT('Ctrl Pts',(1.88501408928233,2.92343929481397,39.5281720265499));
#67264=CARTESIAN_POINT('Ctrl Pts',(1.93024444536004,2.89565908134739,39.5262378270902));
#67265=CARTESIAN_POINT('Ctrl Pts',(2.02491559571945,2.83751262851842,39.5221893759224));
#67266=CARTESIAN_POINT('Ctrl Pts',(2.11656269895661,2.7743484543806,39.518145109875));
#67267=CARTESIAN_POINT('Ctrl Pts',(2.2050194472515,2.70653335041133,39.5141001644575));
#67268=CARTESIAN_POINT('Ctrl Pts',(2.23439457737638,2.68401299394413,39.5127569000907));
#67269=CARTESIAN_POINT('Ctrl Pts',(2.26341761501468,2.66097938867885,39.5114135608029));
#67270=CARTESIAN_POINT('Ctrl Pts',(2.29208165138664,2.63744501091331,39.5100699684447));
#67271=CARTESIAN_POINT('Ctrl Pts',(2.30984392701489,2.62286143659788,39.5092373830583));
#67272=CARTESIAN_POINT('Ctrl Pts',(2.32747273375478,2.60808165907506,39.5084044881281));
#67273=CARTESIAN_POINT('Ctrl Pts',(2.34494114478636,2.59313055702297,39.5075724507146));
#67274=CARTESIAN_POINT('Ctrl Pts',(2.42860008947105,2.52152739762347,39.5035876937827));
#67275=CARTESIAN_POINT('Ctrl Pts',(2.50867656926775,2.44592450086923,39.4996182495046));
#67276=CARTESIAN_POINT('Ctrl Pts',(2.58505343015526,2.36673301098922,39.4956596520215));
#67277=CARTESIAN_POINT('Ctrl Pts',(2.66404287809359,2.28483265537954,39.491565644672));
#67278=CARTESIAN_POINT('Ctrl Pts',(2.73907586413126,2.19909353515585,39.4874832388718));
#67279=CARTESIAN_POINT('Ctrl Pts',(2.80999341936694,2.10992299212625,39.4834074946224));
#67280=CARTESIAN_POINT('Ctrl Pts',(2.88141591562966,2.02011754472876,39.4793027306123));
#67281=CARTESIAN_POINT('Ctrl Pts',(2.94866468551847,1.9268309090439,39.4752047233529));
#67282=CARTESIAN_POINT('Ctrl Pts',(3.01153978421965,1.83044129240823,39.4711084265728));
#67283=CARTESIAN_POINT('Ctrl Pts',(3.05695665617376,1.76081571778681,39.4681495288503));
#67284=CARTESIAN_POINT('Ctrl Pts',(3.10009073166378,1.68957028004866,39.4651915236005));
#67285=CARTESIAN_POINT('Ctrl Pts',(3.14085224826706,1.61683864750778,39.4622325089297));
#67286=CARTESIAN_POINT('Ctrl Pts',(3.15014066515061,1.60026512964199,39.4615582317163));
#67287=CARTESIAN_POINT('Ctrl Pts',(3.15930583138579,1.58361441596945,39.460883902088));
#67288=CARTESIAN_POINT('Ctrl Pts',(3.16834658750349,1.56688804883568,39.4602094975408));
#67289=CARTESIAN_POINT('Ctrl Pts',(3.17596640872947,1.55279056344176,39.4596410891005));
#67290=CARTESIAN_POINT('Ctrl Pts',(3.18349742175009,1.53864001413125,39.4590726559032));
#67291=CARTESIAN_POINT('Ctrl Pts',(3.19093291715979,1.52444919435569,39.4585046558345));
#67292=CARTESIAN_POINT('Ctrl Pts',(3.24480482802561,1.42163337161112,39.454389361911));
#67293=CARTESIAN_POINT('Ctrl Pts',(3.29375336700856,1.31654588028642,39.4502903090187));
#67294=CARTESIAN_POINT('Ctrl Pts',(3.337618406022,1.20959613349929,39.4462025795514));
#67295=CARTESIAN_POINT('Ctrl Pts',(3.38158731501003,1.10239313565547,39.4421051705678));
#67296=CARTESIAN_POINT('Ctrl Pts',(3.42044909886932,0.993318270514273,39.4380191386991));
#67297=CARTESIAN_POINT('Ctrl Pts',(3.45400073695398,0.882753434042322,39.4339395313225));
#67298=CARTESIAN_POINT('Ctrl Pts',(3.48712274811758,0.773604374354528,39.4299121630989));
#67299=CARTESIAN_POINT('Ctrl Pts',(3.51507009480238,0.663002461925495,39.4258910558902));
#67300=CARTESIAN_POINT('Ctrl Pts',(3.53760075803832,0.551297307640023,39.421871444902));
#67301=CARTESIAN_POINT('Ctrl Pts',(3.55737395285894,0.453263452399072,39.4183437834949));
#67302=CARTESIAN_POINT('Ctrl Pts',(3.57297471641564,0.354379297415562,39.4148172744827));
#67303=CARTESIAN_POINT('Ctrl Pts',(3.58420575248062,0.254876789158337,39.4112886971468));
#67304=CARTESIAN_POINT('Ctrl Pts',(3.58611064610739,0.238000189997689,39.4106902158989));
#67305=CARTESIAN_POINT('Ctrl Pts',(3.58788977339785,0.221104894290164,39.41009164332));
#67306=CARTESIAN_POINT('Ctrl Pts',(3.58954066532436,0.204208596389713,39.4094935490786));
#67307=CARTESIAN_POINT('Ctrl Pts',(3.597623244341,0.121486244504585,39.4065653477299));
#67308=CARTESIAN_POINT('Ctrl Pts',(3.60264407172324,0.0386479560669887,
39.4036453351744));
#67309=CARTESIAN_POINT('Ctrl Pts',(3.60453308945048,-0.0441671508522866,
39.4007317406353));
#67310=CARTESIAN_POINT('Ctrl Pts',(3.60708676003424,-0.156120839470894,
39.3967929948202));
#67311=CARTESIAN_POINT('Ctrl Pts',(3.60391953796431,-0.268032156050148,
39.3928659779381));
#67312=CARTESIAN_POINT('Ctrl Pts',(3.59530311376501,-0.379576415454748,
39.3889463152684));
#67313=CARTESIAN_POINT('Ctrl Pts',(3.58648336471152,-0.493752824780849,
39.3849341589118));
#67314=CARTESIAN_POINT('Ctrl Pts',(3.57195407432147,-0.607545351900785,
39.3809297079427));
#67315=CARTESIAN_POINT('Ctrl Pts',(3.5519521505194,-0.720608855394466,39.3769282705794));
#67316=CARTESIAN_POINT('Ctrl Pts',(3.53166934722454,-0.835260067142061,
39.3728706425362));
#67317=CARTESIAN_POINT('Ctrl Pts',(3.5057588970992,-0.949162442548182,39.368816113331));
#67318=CARTESIAN_POINT('Ctrl Pts',(3.47441538262496,-1.06194768262354,39.3647597907387));
#67319=CARTESIAN_POINT('Ctrl Pts',(3.46820705446736,-1.0842874806158,39.3639563396201));
#67320=CARTESIAN_POINT('Ctrl Pts',(3.46178541358641,-1.10658340128134,39.3631528181411));
#67321=CARTESIAN_POINT('Ctrl Pts',(3.45515174516057,-1.12883250042167,39.362349188284));
#67322=CARTESIAN_POINT('Ctrl Pts',(3.44954948246457,-1.1476222996899,39.361670507156));
#67323=CARTESIAN_POINT('Ctrl Pts',(3.44379534080171,-1.16638049820138,39.3609916829215));
#67324=CARTESIAN_POINT('Ctrl Pts',(3.43789702831884,-1.18508405728282,39.3603134654124));
#67325=CARTESIAN_POINT('Ctrl Pts',(3.40264701388611,-1.29686191399661,39.3562602422147));
#67326=CARTESIAN_POINT('Ctrl Pts',(3.36220319088117,-1.40685763388892,39.352222584789));
#67327=CARTESIAN_POINT('Ctrl Pts',(3.31684309881894,-1.51472132228663,39.3481957972556));
#67328=CARTESIAN_POINT('Ctrl Pts',(3.27089782911227,-1.62397652944516,39.3441170612818));
#67329=CARTESIAN_POINT('Ctrl Pts',(3.21990833949425,-1.731045158171,39.3400494774681));
#67330=CARTESIAN_POINT('Ctrl Pts',(3.16410959867439,-1.83555588581314,39.3359881658396));
#67331=CARTESIAN_POINT('Ctrl Pts',(3.10833645140519,-1.94001867687889,39.3319287170378));
#67332=CARTESIAN_POINT('Ctrl Pts',(3.04775807017554,-2.04192673482197,39.3278755346686));
#67333=CARTESIAN_POINT('Ctrl Pts',(2.98256133574493,-2.14088927082937,39.323823745469));
#67334=CARTESIAN_POINT('Ctrl Pts',(2.94977635263049,-2.19065380428797,39.3217862532287));
#67335=CARTESIAN_POINT('Ctrl Pts',(2.91582280876458,-2.23967311081566,39.31974911328));
#67336=CARTESIAN_POINT('Ctrl Pts',(2.88072037422569,-2.28789457686111,39.3177117059431));
#67337=CARTESIAN_POINT('Ctrl Pts',(2.85183603436686,-2.32757402451322,39.3160352078107));
#67338=CARTESIAN_POINT('Ctrl Pts',(2.8221737329529,-2.36671322663747,39.3143585286308));
#67339=CARTESIAN_POINT('Ctrl Pts',(2.79174315327695,-2.40528161823562,39.3126813231461));
#67340=CARTESIAN_POINT('Ctrl Pts',(2.78149815302897,-2.41826635877277,39.3121166618485));
#67341=CARTESIAN_POINT('Ctrl Pts',(2.77116939361923,-2.4311821130314,39.3115521259553));
#67342=CARTESIAN_POINT('Ctrl Pts',(2.76076240551527,-2.44402178436742,39.3109879700884));
#67343=CARTESIAN_POINT('Ctrl Pts',(2.68526519417086,-2.53716682986623,39.3068953167401));
#67344=CARTESIAN_POINT('Ctrl Pts',(2.60557688951826,-2.62640866910907,39.3028183552394));
#67345=CARTESIAN_POINT('Ctrl Pts',(2.52193212892038,-2.71137579627139,39.2987522504735));
#67346=CARTESIAN_POINT('Ctrl Pts',(2.43957779259837,-2.79503209843094,39.2947488752827));
#67347=CARTESIAN_POINT('Ctrl Pts',(2.35338763072836,-2.87454528342,39.2907560244275));
#67348=CARTESIAN_POINT('Ctrl Pts',(2.2635436371301,-2.94953435524468,39.2867690831406));
#67349=CARTESIAN_POINT('Ctrl Pts',(2.17674187142619,-3.02198420505862,39.2829171445791));
#67350=CARTESIAN_POINT('Ctrl Pts',(2.08652901371786,-3.09021163609735,39.2790707221512));
#67351=CARTESIAN_POINT('Ctrl Pts',(1.99303729858505,-3.15383958599926,39.2752256541803));
#67352=CARTESIAN_POINT('Ctrl Pts',(1.92845210860628,-3.19779453138171,39.2725694354444));
#67353=CARTESIAN_POINT('Ctrl Pts',(1.86230145895038,-3.23955372097215,39.269913863084));
#67354=CARTESIAN_POINT('Ctrl Pts',(1.79470553509306,-3.27911298465084,39.267257565119));
#67355=CARTESIAN_POINT('Ctrl Pts',(1.76785526964496,-3.29482660568139,39.2662024378066));
#67356=CARTESIAN_POINT('Ctrl Pts',(1.74077691345468,-3.31019301738663,39.2651471960072));
#67357=CARTESIAN_POINT('Ctrl Pts',(1.71347781142213,-3.32521155260794,39.2640917537339));
#67358=CARTESIAN_POINT('Ctrl Pts',(1.6984525861858,-3.33347764407684,39.2635108460593));
#67359=CARTESIAN_POINT('Ctrl Pts',(1.68335889097543,-3.34163913394484,39.2629298175273));
#67360=CARTESIAN_POINT('Ctrl Pts',(1.66821300299088,-3.34968806573045,39.2623492279294));
#67361=CARTESIAN_POINT('Ctrl Pts',(1.56635622650103,-3.40381749324935,39.2584447368246));
#67362=CARTESIAN_POINT('Ctrl Pts',(1.46200047581987,-3.4529389048349,39.2545546017007));
#67363=CARTESIAN_POINT('Ctrl Pts',(1.35557680788105,-3.49711548633947,39.250674628782));
#67364=CARTESIAN_POINT('Ctrl Pts',(1.24647006549714,-3.54240581499447,39.2466968368689));
#67365=CARTESIAN_POINT('Ctrl Pts',(1.13518916887396,-3.58249910677392,39.2427297260242));
#67366=CARTESIAN_POINT('Ctrl Pts',(1.02216633766018,-3.61741968837196,39.2387687772176));
#67367=CARTESIAN_POINT('Ctrl Pts',(0.906950805093988,-3.65301774730511,
39.2347309839565));
#67368=CARTESIAN_POINT('Ctrl Pts',(0.789924298256552,-3.68324071202624,
39.2306995941463));
#67369=CARTESIAN_POINT('Ctrl Pts',(0.67152272960871,-3.7080653836123,39.2266698206061));
#67370=CARTESIAN_POINT('Ctrl Pts',(0.576455744207969,-3.7279976084823,39.2234342349067));
#67371=CARTESIAN_POINT('Ctrl Pts',(0.480501676067777,-3.74444874562505,
39.2201996911852));
#67372=CARTESIAN_POINT('Ctrl Pts',(0.383881660549383,-3.75738289050549,
39.2169637114682));
#67373=CARTESIAN_POINT('Ctrl Pts',(0.360003491635362,-3.76057936790777,
39.2161639882445));
#67374=CARTESIAN_POINT('Ctrl Pts',(0.336084644176059,-3.76356093900021,
39.2153641773165));
#67375=CARTESIAN_POINT('Ctrl Pts',(0.312128454159217,-3.76632685583852,
39.2145642412819));
#67376=CARTESIAN_POINT('Ctrl Pts',(0.295455119908527,-3.76825191386828,
39.214007491612));
#67377=CARTESIAN_POINT('Ctrl Pts',(0.278767856439627,-3.77007198551237,
39.2134508204112));
#67378=CARTESIAN_POINT('Ctrl Pts',(0.262077281879732,-3.77178610004875,
39.2128945301218));
#67379=CARTESIAN_POINT('Ctrl Pts',(0.140725660955248,-3.78424885719911,
39.2088499282968));
#67380=CARTESIAN_POINT('Ctrl Pts',(0.0190525560554103,-3.79113177091376,
39.2048205149704));
#67381=CARTESIAN_POINT('Ctrl Pts',(-0.102493915516963,-3.79245700593582,
39.2008016264731));
#67382=CARTESIAN_POINT('Ctrl Pts',(-0.224824502847876,-3.7937907902613,
39.1967568114823));
#67383=CARTESIAN_POINT('Ctrl Pts',(-0.347027710634442,-3.78949511138404,
39.1927226575533));
#67384=CARTESIAN_POINT('Ctrl Pts',(-0.468659616482366,-3.77954173808746,
39.1886944101745));
#67385=CARTESIAN_POINT('Ctrl Pts',(-0.588412174998118,-3.76974215540543,
39.1847284036684));
#67386=CARTESIAN_POINT('Ctrl Pts',(-0.707611816239328,-3.75445834537323,
39.1807681225972));
#67387=CARTESIAN_POINT('Ctrl Pts',(-0.825834241284718,-3.73361353038175,
39.1768090294491));
#67388=CARTESIAN_POINT('Ctrl Pts',(-0.893388812412217,-3.72170240153762,
39.1745467273556));
#67389=CARTESIAN_POINT('Ctrl Pts',(-0.960624222063593,-3.70797457901974,
39.1722848131428));
#67390=CARTESIAN_POINT('Ctrl Pts',(-1.02745956875379,-3.69240826157735,
39.1700224402025));
#67391=CARTESIAN_POINT('Ctrl Pts',(-1.07281224182272,-3.68184537620588,
39.1684872546248));
#67392=CARTESIAN_POINT('Ctrl Pts',(-1.11798067116172,-3.67043582154343,
39.1669518578207));
#67393=CARTESIAN_POINT('Ctrl Pts',(-1.16293901326242,-3.65817132387934,
39.1654159852618));
#67394=CARTESIAN_POINT('Ctrl Pts',(-1.1790118050335,-3.65378671564155,39.1648669045201));
#67395=CARTESIAN_POINT('Ctrl Pts',(-1.19505272668909,-3.64929415759008,
39.1643179339248));
#67396=CARTESIAN_POINT('Ctrl Pts',(-1.21105312608346,-3.64469570725446,
39.1637693198638));
#67397=CARTESIAN_POINT('Ctrl Pts',(-1.32870450504678,-3.61088317484544,
39.1597353455105));
#67398=CARTESIAN_POINT('Ctrl Pts',(-1.44428982539489,-3.57131572587835,
39.1557163867866));
#67399=CARTESIAN_POINT('Ctrl Pts',(-1.55737353629067,-3.52596630724087,
39.151707817502));
#67400=CARTESIAN_POINT('Ctrl Pts',(-1.57607785915361,-3.51846540228185,
39.1510447903204));
#67401=CARTESIAN_POINT('Ctrl Pts',(-1.59471373536467,-3.51080619901927,
39.1503820473728));
#67402=CARTESIAN_POINT('Ctrl Pts',(-1.61327917907095,-3.50298843728883,
39.1497195677254));
#67403=CARTESIAN_POINT('Ctrl Pts',(-1.72303348532684,-3.45677176567174,
39.1458031520841));
#67404=CARTESIAN_POINT('Ctrl Pts',(-1.83032763142738,-3.40501790318193,
39.1418959384702));
#67405=CARTESIAN_POINT('Ctrl Pts',(-1.93495936234765,-3.34811198930233,
39.1379936017654));
#67406=CARTESIAN_POINT('Ctrl Pts',(-2.04145748741211,-3.290191002237,39.1340216561732));
#67407=CARTESIAN_POINT('Ctrl Pts',(-2.14519796427287,-3.22693205012696,
39.130054763028));
#67408=CARTESIAN_POINT('Ctrl Pts',(-2.24594491117972,-3.15869129439345,
39.1260883616074));
#67409=CARTESIAN_POINT('Ctrl Pts',(-2.30893415621142,-3.11602564728435,
39.1236084787062));
#67410=CARTESIAN_POINT('Ctrl Pts',(-2.37075274135737,-3.07141163206597,
39.1211287880216));
#67411=CARTESIAN_POINT('Ctrl Pts',(-2.43133703585902,-3.02492794515153,
39.118648174907));
#67412=CARTESIAN_POINT('Ctrl Pts',(-2.45143233918592,-3.00950969532322,
39.1178253763025));
#67413=CARTESIAN_POINT('Ctrl Pts',(-2.4713918044241,-2.99388569828028,39.1170024762128));
#67414=CARTESIAN_POINT('Ctrl Pts',(-2.49121297840036,-2.9780586911772,39.1161794339618));
#67415=CARTESIAN_POINT('Ctrl Pts',(-2.50475852752239,-2.96724270709744,
39.1156169769017));
#67416=CARTESIAN_POINT('Ctrl Pts',(-2.51823242965907,-2.95633753125181,
39.1150547462552));
#67417=CARTESIAN_POINT('Ctrl Pts',(-2.53163147637706,-2.94534651348948,
39.1144928398804));
#67418=CARTESIAN_POINT('Ctrl Pts',(-2.62682518042585,-2.86726068290147,
39.1105007686334));
#67419=CARTESIAN_POINT('Ctrl Pts',(-2.71828589383797,-2.78481154788143,
39.1065232597069));
#67420=CARTESIAN_POINT('Ctrl Pts',(-2.80580464251908,-2.69840960417894,
39.1025558290962));
#67421=CARTESIAN_POINT('Ctrl Pts',(-2.8941871921868,-2.61115488223934,39.0985492403563));
#67422=CARTESIAN_POINT('Ctrl Pts',(-2.97855017848199,-2.51986833452101,
39.0945529298579));
#67423=CARTESIAN_POINT('Ctrl Pts',(-3.05865080393408,-2.4249258325775,39.0905622795115));
#67424=CARTESIAN_POINT('Ctrl Pts',(-3.13867770514644,-2.33007071526719,
39.0865753021409));
#67425=CARTESIAN_POINT('Ctrl Pts',(-3.21445065607165,-2.23156568836847,
39.082593974508));
#67426=CARTESIAN_POINT('Ctrl Pts',(-3.2856914392638,-2.1297488045123,39.0786136912629));
#67427=CARTESIAN_POINT('Ctrl Pts',(-3.35497275713127,-2.03073237630024,
39.0747428850147));
#67428=CARTESIAN_POINT('Ctrl Pts',(-3.41996814007489,-1.92858304432759,
39.0708730664931));
#67429=CARTESIAN_POINT('Ctrl Pts',(-3.48038110743704,-1.8235874740856,39.067));
#67430=CARTESIAN_POINT('',(-3.,-3.67394039744206E-16,40.));
#67431=CARTESIAN_POINT('',(-3.5,-4.28626379701574E-16,39.5));
#67432=CARTESIAN_POINT('Origin',(0.,0.,40.));
#67433=CARTESIAN_POINT('Ctrl Pts',(-3.7316481904409,-0.0029745009063645,
39.273231107418));
#67434=CARTESIAN_POINT('Ctrl Pts',(-3.72101327086788,-0.0904815696235971,
39.2843416389771));
#67435=CARTESIAN_POINT('Ctrl Pts',(-3.70706464015071,-0.177438020952757,
39.2954883497431));
#67436=CARTESIAN_POINT('Ctrl Pts',(-3.68971365463305,-0.263683313725708,
39.3066800800367));
#67437=CARTESIAN_POINT('Ctrl Pts',(-3.66688152549423,-0.377173331926843,
39.3214072568354));
#67438=CARTESIAN_POINT('Ctrl Pts',(-3.63815885390845,-0.489433325135786,
39.3362123889011));
#67439=CARTESIAN_POINT('Ctrl Pts',(-3.6037996984897,-0.600127780314454,
39.3511156197284));
#67440=CARTESIAN_POINT('Ctrl Pts',(-3.56942892658912,-0.710859660165304,
39.3660238891868));
#67441=CARTESIAN_POINT('Ctrl Pts',(-3.52941713446667,-0.820025621887105,
39.3810303237503));
#67442=CARTESIAN_POINT('Ctrl Pts',(-3.48398224124741,-0.927253069125431,
39.3961550873513));
#67443=CARTESIAN_POINT('Ctrl Pts',(-3.47074172660182,-0.958501004026838,
39.4005627053687));
#67444=CARTESIAN_POINT('Ctrl Pts',(-3.45704046334811,-0.989584038315067,
39.4049803723675));
#67445=CARTESIAN_POINT('Ctrl Pts',(-3.44288339940111,-1.0204922370478,39.4094085873714));
#67446=CARTESIAN_POINT('Ctrl Pts',(-3.43640392014665,-1.03463846349922,
39.4114353160321));
#67447=CARTESIAN_POINT('Ctrl Pts',(-3.4298278760645,-1.04875033886207,39.4134645832393));
#67448=CARTESIAN_POINT('Ctrl Pts',(-3.42315930771927,-1.06281936111123,
39.4154953499366));
#67449=CARTESIAN_POINT('Ctrl Pts',(-3.37490270913961,-1.16462879365192,
39.4301908420194));
#67450=CARTESIAN_POINT('Ctrl Pts',(-3.32190256625949,-1.26399452116724,
39.444935534266));
#67451=CARTESIAN_POINT('Ctrl Pts',(-3.26442900579869,-1.36062889855108,
39.4597506949289));
#67452=CARTESIAN_POINT('Ctrl Pts',(-3.20700756171027,-1.45717564897817,
39.4745524213722));
#67453=CARTESIAN_POINT('Ctrl Pts',(-3.14512006233126,-1.55099662208012,
39.4894244884898));
#67454=CARTESIAN_POINT('Ctrl Pts',(-3.07899866234672,-1.64176875367575,
39.5043881067291));
#67455=CARTESIAN_POINT('Ctrl Pts',(-3.01376226873766,-1.73132593950196,
39.5191514434024));
#67456=CARTESIAN_POINT('Ctrl Pts',(-2.9444038130544,-1.81791582497803,39.5340038968541));
#67457=CARTESIAN_POINT('Ctrl Pts',(-2.87112112190071,-1.90118490671918,
39.5489658372021));
#67458=CARTESIAN_POINT('Ctrl Pts',(-2.82601293849714,-1.95244007969242,
39.558175460084));
#67459=CARTESIAN_POINT('Ctrl Pts',(-2.7794174721576,-2.00243617037411,39.567426565951));
#67460=CARTESIAN_POINT('Ctrl Pts',(-2.73137782673631,-2.05108126664787,
39.5767239054783));
#67461=CARTESIAN_POINT('Ctrl Pts',(-2.70785849585012,-2.0748970151868,39.5812757126947));
#67462=CARTESIAN_POINT('Ctrl Pts',(-2.68399298220066,-2.09838882749915,
39.585838601668));
#67463=CARTESIAN_POINT('Ctrl Pts',(-2.65978622078055,-2.12154522361285,
39.59041312988));
#67464=CARTESIAN_POINT('Ctrl Pts',(-2.64944130372411,-2.13144126021869,
39.5923680842873));
#67465=CARTESIAN_POINT('Ctrl Pts',(-2.63903323298336,-2.14127680635578,
39.594325319609));
#67466=CARTESIAN_POINT('Ctrl Pts',(-2.62856497776732,-2.15104852675842,
39.5962843953922));
#67467=CARTESIAN_POINT('Ctrl Pts',(-2.54974767685836,-2.22462149679763,
39.6110346152064));
#67468=CARTESIAN_POINT('Ctrl Pts',(-2.4677942019439,-2.29432581076987,39.6258380873112));
#67469=CARTESIAN_POINT('Ctrl Pts',(-2.38291639940009,-2.35987680253582,
39.6407167938454));
#67470=CARTESIAN_POINT('Ctrl Pts',(-2.29950856647313,-2.4242925391071,39.6553378211526));
#67471=CARTESIAN_POINT('Ctrl Pts',(-2.21327611648925,-2.48469790320087,
39.6700314995361));
#67472=CARTESIAN_POINT('Ctrl Pts',(-2.12440130761369,-2.54077665854762,
39.684818688697));
#67473=CARTESIAN_POINT('Ctrl Pts',(-2.03317702032287,-2.59833790175464,
39.699996789323));
#67474=CARTESIAN_POINT('Ctrl Pts',(-1.93916819329382,-2.6513414739591,39.7152734101447));
#67475=CARTESIAN_POINT('Ctrl Pts',(-1.84256188381164,-2.69938792578526,
39.7306711093119));
#67476=CARTESIAN_POINT('Ctrl Pts',(-1.75241852072327,-2.74422007779779,
39.7450387049088));
#67477=CARTESIAN_POINT('Ctrl Pts',(-1.66001305141746,-2.78473593017921,
39.7595117205049));
#67478=CARTESIAN_POINT('Ctrl Pts',(-1.56549738334504,-2.82055985230118,
39.774108482969));
#67479=CARTESIAN_POINT('Ctrl Pts',(-1.55872095882304,-2.8231282952831,39.7751550169577));
#67480=CARTESIAN_POINT('Ctrl Pts',(-1.55193368901203,-2.82567259777892,
39.7762021870499));
#67481=CARTESIAN_POINT('Ctrl Pts',(-1.5451356309518,-2.82819261092012,39.77725));
#67482=CARTESIAN_POINT('Origin',(0.,0.,39.5));
#67483=CARTESIAN_POINT('Ctrl Pts',(-3.55517835629984,1.66474646536813,39.067));
#67484=CARTESIAN_POINT('Ctrl Pts',(-3.59346767298069,1.54867526405411,39.0814568953907));
#67485=CARTESIAN_POINT('Ctrl Pts',(-3.62650702796103,1.43121621681944,39.0959580292964));
#67486=CARTESIAN_POINT('Ctrl Pts',(-3.6541619006592,1.31275716621601,39.1105228138977));
#67487=CARTESIAN_POINT('Ctrl Pts',(-3.68131382207819,1.19645249656677,39.1248227129172));
#67488=CARTESIAN_POINT('Ctrl Pts',(-3.7032752972325,1.07918303068495,39.1391839684911));
#67489=CARTESIAN_POINT('Ctrl Pts',(-3.71986954241218,0.961317221364022,
39.153624952814));
#67490=CARTESIAN_POINT('Ctrl Pts',(-3.73616669269371,0.845561621349798,
39.1678073931224));
#67491=CARTESIAN_POINT('Ctrl Pts',(-3.74728703315826,0.729230135992343,
39.18206673289));
#67492=CARTESIAN_POINT('Ctrl Pts',(-3.75301552808992,0.612684385714019,
39.1964203750936));
#67493=CARTESIAN_POINT('Ctrl Pts',(-3.755542939032,0.561264421478854,39.2027531994736));
#67494=CARTESIAN_POINT('Ctrl Pts',(-3.7570201630815,0.509802978089015,39.2091043805096));
#67495=CARTESIAN_POINT('Ctrl Pts',(-3.75742574055319,0.458332442123154,
39.2154754128171));
#67496=CARTESIAN_POINT('Ctrl Pts',(-3.75764127879252,0.430979175550461,
39.2188612051307));
#67497=CARTESIAN_POINT('Ctrl Pts',(-3.75755412750489,0.403623356983449,
39.2222526039123));
#67498=CARTESIAN_POINT('Ctrl Pts',(-3.75716085210795,0.376269966068251,
39.2256498334886));
#67499=CARTESIAN_POINT('Ctrl Pts',(-3.75691574882173,0.359222355018006,
39.2277671084051));
#67500=CARTESIAN_POINT('Ctrl Pts',(-3.75655173700823,0.34217568862123,39.2298866481352));
#67501=CARTESIAN_POINT('Ctrl Pts',(-3.75606795588435,0.325131190221386,
39.2320085069836));
#67502=CARTESIAN_POINT('Ctrl Pts',(-3.75571123254104,0.312563171019651,
39.233573091762));
#67503=CARTESIAN_POINT('Ctrl Pts',(-3.75528936565693,0.299996514206195,
39.2351389152941));
#67504=CARTESIAN_POINT('Ctrl Pts',(-3.7548024159468,0.287440005344609,39.2367049633161));
#67505=CARTESIAN_POINT('Ctrl Pts',(-3.75102773997828,0.19010602760176,39.2488444588559));
#67506=CARTESIAN_POINT('Ctrl Pts',(-3.74334047216327,0.0932328369217743,
39.2610159266466));
#67507=CARTESIAN_POINT('Ctrl Pts',(-3.7316481904409,-0.0029745009063645,
39.273231107418));
#67508=CARTESIAN_POINT('Ctrl Pts',(2.28405859260867,-3.20180657528379,-0.410063028691932));
#67509=CARTESIAN_POINT('Ctrl Pts',(3.35101936364523,-2.44067349002037,-0.343767612025265));
#67510=CARTESIAN_POINT('Ctrl Pts',(4.64535438600488,0.219163159607182,-0.211176778691931));
#67511=CARTESIAN_POINT('Ctrl Pts',(2.32227978484365,4.03443500934324,-0.0122905286919314));
#67512=CARTESIAN_POINT('Ctrl Pts',(-2.13685955260049,4.13065816376694,0.18659572130807));
#67513=CARTESIAN_POINT('Ctrl Pts',(-4.63131485374691,0.437059737780703,
0.38548197130807));
#67514=CARTESIAN_POINT('Ctrl Pts',(-2.87058777509758,-3.6612002757226,0.58436822130807));
#67515=CARTESIAN_POINT('Ctrl Pts',(1.52825192091582,-4.39356078829283,0.78325447130807));
#67516=CARTESIAN_POINT('Ctrl Pts',(4.52260840884179,-1.08946538597355,0.982140721308071));
#67517=CARTESIAN_POINT('Ctrl Pts',(3.36117901623604,3.21618372219525,1.18102697130807));
#67518=CARTESIAN_POINT('Ctrl Pts',(-0.888913231377699,4.56622408239327,
1.37991322130807));
#67519=CARTESIAN_POINT('Ctrl Pts',(-4.32215201846994,1.72043564577458,1.57879947130807));
#67520=CARTESIAN_POINT('Ctrl Pts',(-3.78373551838476,-2.70633956790168,
1.77768572130807));
#67521=CARTESIAN_POINT('Ctrl Pts',(0.231598108743597,-4.64620095483734,
1.97657197130807));
#67522=CARTESIAN_POINT('Ctrl Pts',(4.03411078631178,-2.3166405035163,2.17545822130807));
#67523=CARTESIAN_POINT('Ctrl Pts',(4.12964193630134,2.14171203558755,2.37434447130808));
#67524=CARTESIAN_POINT('Ctrl Pts',(0.430404503435925,4.63202015931436,2.57323072130807));
#67525=CARTESIAN_POINT('Ctrl Pts',(-3.66433530838834,2.86592281387884,2.77211697130807));
#67526=CARTESIAN_POINT('Ctrl Pts',(-4.39188239410591,-1.53369983889943,
2.97100322130807));
#67527=CARTESIAN_POINT('Ctrl Pts',(-1.0836863715155,-4.52399029506003,3.16988947130807));
#67528=CARTESIAN_POINT('Ctrl Pts',(3.22031941745,-3.35714289255106,3.36877572130807));
#67529=CARTESIAN_POINT('Ctrl Pts',(4.56514274797943,0.89461559064575,3.56766197130807));
#67530=CARTESIAN_POINT('Ctrl Pts',(1.71501247192487,4.32430310693921,3.76654822130808));
#67531=CARTESIAN_POINT('Ctrl Pts',(-2.71105925393979,3.78034694695518,3.96543447130807));
#67532=CARTESIAN_POINT('Ctrl Pts',(-4.64591255536892,-0.237406415989334,
4.16432072130808));
#67533=CARTESIAN_POINT('Ctrl Pts',(-2.31159211256507,-4.03700472592018,
4.36320697130807));
#67534=CARTESIAN_POINT('Ctrl Pts',(2.14687255908044,-4.12696056350751,4.56209322130808));
#67535=CARTESIAN_POINT('Ctrl Pts',(4.63255538357458,-0.424612633481082,
4.76097947130807));
#67536=CARTESIAN_POINT('Ctrl Pts',(2.86133849969297,3.66791592838001,4.95986572130809));
#67537=CARTESIAN_POINT('Ctrl Pts',(-1.53918985797284,4.38996125862584,5.15875197130807));
#67538=CARTESIAN_POINT('Ctrl Pts',(-4.5253418479552,1.07802895555233,5.35763822130809));
#67539=CARTESIAN_POINT('Ctrl Pts',(-3.35311367917035,-3.22451452534221,
5.55652447130807));
#67540=CARTESIAN_POINT('Ctrl Pts',(0.900322906953032,-4.56402058861491,
5.75541072130808));
#67541=CARTESIAN_POINT('Ctrl Pts',(4.32644411261801,-1.70960422620876,5.95429697130808));
#67542=CARTESIAN_POINT('Ctrl Pts',(3.7769542019951,2.71578390633149,6.15318322130808));
#67543=CARTESIAN_POINT('Ctrl Pts',(-0.243215259837961,4.64561208101878,
6.35206947130807));
#67544=CARTESIAN_POINT('Ctrl Pts',(-4.039891879632,2.30654262279634,6.55095572130809));
#67545=CARTESIAN_POINT('Ctrl Pts',(-4.12427298672108,-2.1520310408764,6.74984197130808));
#67546=CARTESIAN_POINT('Ctrl Pts',(-0.41881997004075,-4.63308267815251,
6.94872822130808));
#67547=CARTESIAN_POINT('Ctrl Pts',(3.6714907462362,-2.85675007135706,7.14761447130808));
#67548=CARTESIAN_POINT('Ctrl Pts',(4.38803329537382,1.54467765847374,7.34650072130808));
#67549=CARTESIAN_POINT('Ctrl Pts',(1.0723698356974,4.52668622784753,7.54538697130808));
#67550=CARTESIAN_POINT('Ctrl Pts',(-3.22870458239833,3.34907927488996,7.74427322130807));
#67551=CARTESIAN_POINT('Ctrl Pts',(-4.56289129899062,-0.906028842528388,
7.94315947130809));
#67552=CARTESIAN_POINT('Ctrl Pts',(-1.70419330507885,-4.32857834038177,
8.14204572130808));
#67553=CARTESIAN_POINT('Ctrl Pts',(2.72050431152591,-3.77355555953089,8.34093197130808));
#67554=CARTESIAN_POINT('Ctrl Pts',(4.64530434451287,0.249023727278098,8.53981822130808));
#67555=CARTESIAN_POINT('Ctrl Pts',(2.30148952663657,4.04277271543675,8.73870447130808));
#67556=CARTESIAN_POINT('Ctrl Pts',(-2.15718615802268,4.12157896315634,8.93759072130809));
#67557=CARTESIAN_POINT('Ctrl Pts',(-4.63360272954349,0.413026651276645,
9.13647697130808));
#67558=CARTESIAN_POINT('Ctrl Pts',(-2.85215717676813,-3.67505982385426,
9.33536322130809));
#67559=CARTESIAN_POINT('Ctrl Pts',(1.55016304402113,-4.38609847208755,9.53424947130807));
#67560=CARTESIAN_POINT('Ctrl Pts',(4.52802353080303,-1.06670903923785,9.7331357213081));
#67561=CARTESIAN_POINT('Ctrl Pts',(3.34503963470285,3.23288959170657,9.93202197130807));
#67562=CARTESIAN_POINT('Ctrl Pts',(-0.911733361628194,4.56175487583362,
10.1309082213081));
#67563=CARTESIAN_POINT('Ctrl Pts',(-4.33070580091485,1.69877971962819,10.3297944713081));
#67564=CARTESIAN_POINT('Ctrl Pts',(-3.7701510175469,-2.72522046351992,10.5286807213081));
#67565=CARTESIAN_POINT('Ctrl Pts',(0.254831805397762,-4.64498934561268,
10.7275669713081));
#67566=CARTESIAN_POINT('Ctrl Pts',(4.04564723083314,-2.29643283236192,10.9264532213081));
#67567=CARTESIAN_POINT('Ctrl Pts',(4.11887849597835,2.16233790265648,11.1253394713081));
#67568=CARTESIAN_POINT('Ctrl Pts',(0.407232686793075,4.6341155368317,11.3242257213081));
#67569=CARTESIAN_POINT('Ctrl Pts',(-3.67862315594041,2.84755982316029,11.5231119713081));
#67570=CARTESIAN_POINT('Ctrl Pts',(-4.38415679164241,-1.55564600606735,
11.7219982213081));
#67571=CARTESIAN_POINT('Ctrl Pts',(-1.0610465751018,-4.52935375471627,11.9208844713081));
#67572=CARTESIAN_POINT('Ctrl Pts',(3.23706954676494,-3.34099476493225,12.1197707213081));
#67573=CARTESIAN_POINT('Ctrl Pts',(4.56061132089925,0.917436455338055,12.3186569713081));
#67574=CARTESIAN_POINT('Ctrl Pts',(1.69336347833148,4.33282649088915,12.5175432213081));
#67575=CARTESIAN_POINT('Ctrl Pts',(-2.72993235494621,3.7667405813668,12.7164294713081));
#67576=CARTESIAN_POINT('Ctrl Pts',(-4.64466708480763,-0.260639485117335,
12.9153157213081));
#67577=CARTESIAN_POINT('Ctrl Pts',(-2.2913725478795,-4.04851542132692,13.1142019713081));
#67578=CARTESIAN_POINT('Ctrl Pts',(2.1674862667245,-4.11617158940907,13.3130882213081));
#67579=CARTESIAN_POINT('Ctrl Pts',(4.63462109921499,-0.401438085648196,
13.5119744713081));
#67580=CARTESIAN_POINT('Ctrl Pts',(2.84295801772125,3.68218073692372,13.7108607213081));
#67581=CARTESIAN_POINT('Ctrl Pts',(-1.56112653604057,4.382208257074,13.9097469713081));
#67582=CARTESIAN_POINT('Ctrl Pts',(-4.53067689750755,1.05538245214185,14.1086332213081));
#67583=CARTESIAN_POINT('Ctrl Pts',(-3.33694467190181,-3.24124444103862,
14.3075194713081));
#67584=CARTESIAN_POINT('Ctrl Pts',(0.923138114741901,-4.55946063597531,
14.5064057213081));
#67585=CARTESIAN_POINT('Ctrl Pts',(4.33494040698919,-1.68794458965632,14.7052919713081));
#67586=CARTESIAN_POINT('Ctrl Pts',(3.76332425632244,2.73463997843825,14.9041782213081));
#67587=CARTESIAN_POINT('Ctrl Pts',(-0.266446757357151,4.64433756260153,
15.1030644713081));
#67588=CARTESIAN_POINT('Ctrl Pts',(-4.05137728243396,2.28630868110051,15.3019507213081));
#67589=CARTESIAN_POINT('Ctrl Pts',(-4.11345824768048,-2.17263124217781,
15.5008369713081));
#67590=CARTESIAN_POINT('Ctrl Pts',(-0.395642856901232,-4.63511941590297,
15.6997232213081));
#67591=CARTESIAN_POINT('Ctrl Pts',(3.68573256124231,-2.83835176764541,15.8986094713081));
#67592=CARTESIAN_POINT('Ctrl Pts',(4.38025287142865,1.56660462537257,16.0974957213081));
#67593=CARTESIAN_POINT('Ctrl Pts',(1.0497166792132,4.5319929571083,16.2963819713081));
#67594=CARTESIAN_POINT('Ctrl Pts',(-3.24541426800062,3.33288936194342,16.4952682213081));
#67595=CARTESIAN_POINT('Ctrl Pts',(-4.55830282286078,-0.928838330925807,
16.6941544713081));
#67596=CARTESIAN_POINT('Ctrl Pts',(-1.6825230620746,-4.33704754591008,16.8930407213081));
#67597=CARTESIAN_POINT('Ctrl Pts',(2.73934332663622,-3.75990204775488,17.0919269713081));
#67598=CARTESIAN_POINT('Ctrl Pts',(4.64400077950955,0.272253613038182,17.2908132213081));
#67599=CARTESIAN_POINT('Ctrl Pts',(2.28124123994172,4.05423280968013,17.4896994713081));
#67600=CARTESIAN_POINT('Ctrl Pts',(-2.1777728209729,4.11073847503455,17.6885857213081));
#67601=CARTESIAN_POINT('Ctrl Pts',(-4.63561048611658,0.389847009612274,
17.8874719713081));
#67602=CARTESIAN_POINT('Ctrl Pts',(-2.83374108013408,-3.68927862334333,
18.0863582213081));
#67603=CARTESIAN_POINT('Ctrl Pts',(1.57208026549899,-4.37829063776336,18.2852444713081));
#67604=CARTESIAN_POINT('Ctrl Pts',(4.53330193146099,-1.0440492651737,18.4841307213081));
#67605=CARTESIAN_POINT('Ctrl Pts',(3.32882884139711,3.24957902113188,18.6830169713081));
#67606=CARTESIAN_POINT('Ctrl Pts',(-0.934537094978153,4.55713788336577,
18.8819032213081));
#67607=CARTESIAN_POINT('Ctrl Pts',(-4.33914790435761,1.67709890406219,19.0807894713081));
#67608=CARTESIAN_POINT('Ctrl Pts',(-3.75647396101428,-2.744042392187,19.2796757213081));
#67609=CARTESIAN_POINT('Ctrl Pts',(0.278060043082108,-4.6436567360582,19.4785619713081));
#67610=CARTESIAN_POINT('Ctrl Pts',(4.05708199860109,-2.27617023232547,19.6774482213081));
#67611=CARTESIAN_POINT('Ctrl Pts',(4.10801227572337,2.18291099507144,19.8763344713081));
#67612=CARTESIAN_POINT('Ctrl Pts',(0.38405055284252,4.63609430908809,20.0752207213081));
#67613=CARTESIAN_POINT('Ctrl Pts',(-3.69281891768294,2.82912596239557,20.2741069713081));
#67614=CARTESIAN_POINT('Ctrl Pts',(-4.37632155914585,-1.57755344785935,
20.4729932213081));
#67615=CARTESIAN_POINT('Ctrl Pts',(-1.03838021888359,-4.5346038185192,20.6718794713081));
#67616=CARTESIAN_POINT('Ctrl Pts',(3.2537386939213,-3.324763116611,20.8707657213081));
#67617=CARTESIAN_POINT('Ctrl Pts',(4.55596581931151,0.940234397989585,21.0696519713081));
#67618=CARTESIAN_POINT('Ctrl Pts',(1.67167212409921,4.34124147904805,21.2685382213081));
#67619=CARTESIAN_POINT('Ctrl Pts',(-2.74873716774412,3.75304000146011,21.4674244713081));
#67620=CARTESIAN_POINT('Ctrl Pts',(-4.6433054327854,-0.283866038411237,
21.6663107213081));
#67621=CARTESIAN_POINT('Ctrl Pts',(-2.27109566617969,-4.0599248447425,21.8651969713081));
#67622=CARTESIAN_POINT('Ctrl Pts',(2.18804575644055,-4.10527965400899,22.0640832213081));
#67623=CARTESIAN_POINT('Ctrl Pts',(4.63657088406109,-0.378253495654039,
22.2629694713081));
#67624=CARTESIAN_POINT('Ctrl Pts',(2.82450642164506,3.69635343872626,22.4618557213081));
#67625=CARTESIAN_POINT('Ctrl Pts',(-1.58302416389686,4.37434563865457,22.6607419713081));
#67626=CARTESIAN_POINT('Ctrl Pts',(-4.53589861624757,1.03270954920589,22.8596282213081));
#67627=CARTESIAN_POINT('Ctrl Pts',(-3.32069219394143,-3.25789327986572,
23.0585144713081));
#67628=CARTESIAN_POINT('Ctrl Pts',(0.945930231053035,-4.55478663253039,
23.2574007213081));
#67629=CARTESIAN_POINT('Ctrl Pts',(4.34332826670835,-1.66624273066974,23.4562869713081));
#67630=CARTESIAN_POINT('Ctrl Pts',(3.74960017446099,2.75342764596779,23.6551732213081));
#67631=CARTESIAN_POINT('Ctrl Pts',(-0.289671589948523,4.64294687024033,
23.8540594713081));
#67632=CARTESIAN_POINT('Ctrl Pts',(-4.06276134365987,2.26601754943795,24.0529457213081));
#67633=CARTESIAN_POINT('Ctrl Pts',(-4.10254061416358,-2.19317709705255,
24.2518319713081));
#67634=CARTESIAN_POINT('Ctrl Pts',(-0.372455847109915,-4.63704021029053,
24.4507182213082));
#67635=CARTESIAN_POINT('Ctrl Pts',(3.6998821809475,-2.81988246510469,24.6496044713081));
#67636=CARTESIAN_POINT('Ctrl Pts',(4.37236287937863,1.58849240505882,24.8484907213081));
#67637=CARTESIAN_POINT('Ctrl Pts',(1.02703726500591,4.53718632262184,25.0473769713081));
#67638=CARTESIAN_POINT('Ctrl Pts',(-3.2620427724699,3.31661607975275,25.2462632213081));
#67639=CARTESIAN_POINT('Ctrl Pts',(-4.55360032486595,-0.951624585263666,
25.4451494713081));
#67640=CARTESIAN_POINT('Ctrl Pts',(-1.66081073226206,-4.34540826407608,
25.6440357213081));
#67641=CARTESIAN_POINT('Ctrl Pts',(2.75811381952511,-3.74615448539464,25.8429219713081));
#67642=CARTESIAN_POINT('Ctrl Pts',(4.64258104898355,0.295476688617761,26.0418082213081));
#67643=CARTESIAN_POINT('Ctrl Pts',(2.2609358900392,4.06559149091866,26.2406944713081));
#67644=CARTESIAN_POINT('Ctrl Pts',(-2.19830500888522,4.09979516046932,26.4395807213081));
#67645=CARTESIAN_POINT('Ctrl Pts',(-4.63750228704264,0.366657616274049,
26.6384669713081));
#67646=CARTESIAN_POINT('Ctrl Pts',(-2.81525410000349,-3.70340513882985,
26.8373532213081));
#67647=CARTESIAN_POINT('Ctrl Pts',(1.59395816279613,-4.37037328441786,27.0362394713081));
#67648=CARTESIAN_POINT('Ctrl Pts',(4.53846693562883,-1.02136337515174,27.2351257213081));
#67649=CARTESIAN_POINT('Ctrl Pts',(3.31253478041756,3.26618716524659,27.4340119713081));
#67650=CARTESIAN_POINT('Ctrl Pts',(-0.957317451719108,4.55240689817286,
27.6328982213081));
#67651=CARTESIAN_POINT('Ctrl Pts',(-4.34748146789946,1.65537613736835,27.8317844713081));
#67652=CARTESIAN_POINT('Ctrl Pts',(-3.74270293964795,-2.76279568108975,
28.0306707213081));
#67653=CARTESIAN_POINT('Ctrl Pts',(0.301281325343274,-4.64220796958699,
28.2295569713081));
#67654=CARTESIAN_POINT('Ctrl Pts',(4.06841528209427,-2.25585069592812,28.4284432213081));
#67655=CARTESIAN_POINT('Ctrl Pts',(4.09704329721841,2.2034294839217,28.6273294713081));
#67656=CARTESIAN_POINT('Ctrl Pts',(0.360858812211213,4.63795711359509,28.8262157213081));
#67657=CARTESIAN_POINT('Ctrl Pts',(-3.70692230686563,2.81062133357725,29.0251019713081));
#67658=CARTESIAN_POINT('Ctrl Pts',(-4.36837685688271,-1.5994214285638,29.2239882213081));
#67659=CARTESIAN_POINT('Ctrl Pts',(-1.0156878885138,-4.53974045326646,29.4228744713081));
#67660=CARTESIAN_POINT('Ctrl Pts',(3.27032645171657,-3.30844830231646,29.6217607213081));
#67661=CARTESIAN_POINT('Ctrl Pts',(4.55120635431684,0.96300882151919,29.8206469713082));
#67662=CARTESIAN_POINT('Ctrl Pts',(1.6499389544851,4.34954787493714,30.0195332213081));
#67663=CARTESIAN_POINT('Ctrl Pts',(-2.76747322334208,3.73924554261714,30.2184194713081));
#67664=CARTESIAN_POINT('Ctrl Pts',(-4.64182763263396,-0.307085491050202,
30.4173057213081));
#67665=CARTESIAN_POINT('Ctrl Pts',(-2.2507619750547,-4.07123271277209,30.6161919713081));
#67666=CARTESIAN_POINT('Ctrl Pts',(2.20855051415048,-4.09428502871299,30.8150782213081));
#67667=CARTESIAN_POINT('Ctrl Pts',(4.63840468923668,-0.355059443987292,
31.0139644713082));
#67668=CARTESIAN_POINT('Ctrl Pts',(2.80598417306898,3.71043367955604,31.2128507213081));
#67669=CARTESIAN_POINT('Ctrl Pts',(-1.60488219382066,4.36637359989451,31.4117369713082));
#67670=CARTESIAN_POINT('Ctrl Pts',(-4.54100687354372,1.01001081396483,31.6106232213081));
#67671=CARTESIAN_POINT('Ctrl Pts',(-3.3043566518382,-3.27446062540828,31.8095094713081));
#67672=CARTESIAN_POINT('Ctrl Pts',(0.968698685766213,-4.54999869517525,
32.0083957213081));
#67673=CARTESIAN_POINT('Ctrl Pts',(4.35160748195836,-1.64449919211191,32.2072819713081));
#67674=CARTESIAN_POINT('Ctrl Pts',(3.73578229970788,2.77214643896784,32.4061682213081));
#67675=CARTESIAN_POINT('Ctrl Pts',(-0.312889176665352,4.64144003872198,
32.6050544713081));
#67676=CARTESIAN_POINT('Ctrl Pts',(-4.07404377854549,2.245669735369,32.8039407213081));
#67677=CARTESIAN_POINT('Ctrl Pts',(-4.09152035926885,-2.21366809155445,
33.0028269713081));
#67678=CARTESIAN_POINT('Ctrl Pts',(-0.349259520662366,-4.63884501328854,
33.2017132213082));
#67679=CARTESIAN_POINT('Ctrl Pts',(3.71393925139909,-2.80134262568852,33.4005994713081));
#67680=CARTESIAN_POINT('Ctrl Pts',(4.36436351660891,1.61034044995361,33.5994857213082));
#67681=CARTESIAN_POINT('Ctrl Pts',(1.0043321603347,4.54226619462571,33.7983719713081));
#67682=CARTESIAN_POINT('Ctrl Pts',(-3.2785896797709,3.30025983510218,33.9972582213082));
#67683=CARTESIAN_POINT('Ctrl Pts',(-4.54878392280352,-0.974387035033758,
34.1961444713081));
#67684=CARTESIAN_POINT('Ctrl Pts',(-1.63905685843296,-4.35366028675904,
34.3950307213081));
#67685=CARTESIAN_POINT('Ctrl Pts',(2.77681532004856,-3.73231321439111,34.5939169713081));
#67686=CARTESIAN_POINT('Ctrl Pts',(4.64104518962864,0.318692369397484,34.7928032213081));
#67687=CARTESIAN_POINT('Ctrl Pts',(2.24057398259076,4.07684848213216,34.9916894713081));
#67688=CARTESIAN_POINT('Ctrl Pts',(-2.21878220384499,4.08874927960163,35.1905757213081));
#67689=CARTESIAN_POINT('Ctrl Pts',(-4.63927809326544,0.343459077334103,
35.3894619713081));
#67690=CARTESIAN_POINT('Ctrl Pts',(-2.79669668299912,-3.71743906671155,
35.5883482213081));
#67691=CARTESIAN_POINT('Ctrl Pts',(1.6157961584067,-4.3623465149027,35.7872344713082));
#67692=CARTESIAN_POINT('Ctrl Pts',(4.54351847197868,-0.998652118751192,
35.9861207213081));
#67693=CARTESIAN_POINT('Ctrl Pts',(3.29615774863631,3.28271395700534,36.1850069713081));
#67694=CARTESIAN_POINT('Ctrl Pts',(-0.980073650227081,4.54756137209857,
36.3838932213081));
#67695=CARTESIAN_POINT('Ctrl Pts',(-4.35570668825951,1.63361323797604,36.5827794713081));
#67696=CARTESIAN_POINT('Ctrl Pts',(-3.72883752278967,-2.78148230039399,
36.7816657213081));
#67697=CARTESIAN_POINT('Ctrl Pts',(0.324493588450696,-4.64063841596816,
36.9805519713081));
#67698=CARTESIAN_POINT('Ctrl Pts',(4.07964963465135,-2.23548365871144,37.1794382213081));
#67699=CARTESIAN_POINT('Ctrl Pts',(4.08596640779809,2.22390993440854,37.3783244713081));
#67700=CARTESIAN_POINT('Ctrl Pts',(0.337668427315605,4.63967123153578,37.5772107213081));
#67701=CARTESIAN_POINT('Ctrl Pts',(-3.72095283273302,2.79210890379928,37.7760969713081));
#67702=CARTESIAN_POINT('Ctrl Pts',(-4.3602848861238,-1.6213689767605,37.9749832213081));
#67703=CARTESIAN_POINT('Ctrl Pts',(-0.993042844038055,-4.54453476652035,
38.1738694713081));
#67704=CARTESIAN_POINT('Ctrl Pts',(3.28697147748708,-3.29248844184413,38.3727557213081));
#67705=CARTESIAN_POINT('Ctrl Pts',(4.54606692907903,0.986597164631765,38.5716419713082));
#67706=CARTESIAN_POINT('Ctrl Pts',(1.62867416074003,4.35613660157396,38.7705282213081));
#67707=CARTESIAN_POINT('Ctrl Pts',(-2.78711997617271,3.72848648678348,38.9694144713082));
#67708=CARTESIAN_POINT('Ctrl Pts',(-4.63831401868151,-0.336738661585157,
39.1683007213081));
#67709=CARTESIAN_POINT('Ctrl Pts',(-3.03582612181379,-2.82311487873352,
39.3008915546415));
#67710=CARTESIAN_POINT('Ctrl Pts',(-1.88566238042959,-3.45148756147731,
39.3671869713081));
#67711=CARTESIAN_POINT('Ctrl Pts',(2.14656790565208,-3.00907133330608,-0.273375352461288));
#67712=CARTESIAN_POINT('Ctrl Pts',(3.14930214159003,-2.29375524726366,-0.207079935794621));
#67713=CARTESIAN_POINT('Ctrl Pts',(4.36572365859917,0.205970462419992,-0.0744891024612875));
#67714=CARTESIAN_POINT('Ctrl Pts',(2.18248834343466,3.79157904990716,0.124397147538712));
#67715=CARTESIAN_POINT('Ctrl Pts',(-2.00822962656989,3.88200997656335,0.323283397538713));
#67716=CARTESIAN_POINT('Ctrl Pts',(-4.35252924692651,0.410750586262939,
0.522169647538713));
#67717=CARTESIAN_POINT('Ctrl Pts',(-2.69779050691701,-3.44081147193987,
0.721055897538714));
#67718=CARTESIAN_POINT('Ctrl Pts',(1.43625760556443,-4.129086972725,0.919942147538715));
#67719=CARTESIAN_POINT('Ctrl Pts',(4.25036647118775,-1.02388416804092,1.11882839753871));
#67720=CARTESIAN_POINT('Ctrl Pts',(3.15885022597575,3.02258303665498,1.31771464753872));
#67721=CARTESIAN_POINT('Ctrl Pts',(-0.835404406681822,4.29135666527998,
1.51660089753871));
#67722=CARTESIAN_POINT('Ctrl Pts',(-4.06197670945066,1.616872681336,1.71548714753872));
#67723=CARTESIAN_POINT('Ctrl Pts',(-3.55597061017793,-2.54342934855236,
1.91437339753872));
#67724=CARTESIAN_POINT('Ctrl Pts',(0.217656880102546,-4.36651926756103,
2.11325964753872));
#67725=CARTESIAN_POINT('Ctrl Pts',(3.79127434373374,-2.17718852304153,2.31214589753872));
#67726=CARTESIAN_POINT('Ctrl Pts',(3.88105492170199,2.01279001056198,2.51103214753871));
#67727=CARTESIAN_POINT('Ctrl Pts',(0.404495968935988,4.35319209607569,2.70991839753872));
#67728=CARTESIAN_POINT('Ctrl Pts',(-3.44375778887116,2.69340635667425,2.90880464753871));
#67729=CARTESIAN_POINT('Ctrl Pts',(-4.12750961078415,-1.44137758187943,
3.10769089753872));
#67730=CARTESIAN_POINT('Ctrl Pts',(-1.01845302586177,-4.25166517368817,
3.30657714753872));
#67731=CARTESIAN_POINT('Ctrl Pts',(3.02646978051091,-3.15505705990135,3.50546339753872));
#67732=CARTESIAN_POINT('Ctrl Pts',(4.29034042263387,0.840763507989867,3.70434964753872));
#67733=CARTESIAN_POINT('Ctrl Pts',(1.61177595966248,4.06399831147317,3.90323589753872));
#67734=CARTESIAN_POINT('Ctrl Pts',(-2.54786492941134,3.55278601644629,4.10212214753872));
#67735=CARTESIAN_POINT('Ctrl Pts',(-4.36624822852336,-0.223115551767193,
4.30100839753872));
#67736=CARTESIAN_POINT('Ctrl Pts',(-2.17244402391783,-3.79399408039216,
4.49989464753872));
#67737=CARTESIAN_POINT('Ctrl Pts',(2.01763989232161,-3.87853495623309,4.69878089753872));
#67738=CARTESIAN_POINT('Ctrl Pts',(4.35369510209446,-0.399052745106703,
4.89766714753871));
#67739=CARTESIAN_POINT('Ctrl Pts',(2.68909799885338,3.44712287065204,5.09655339753873));
#67740=CARTESIAN_POINT('Ctrl Pts',(-1.44653712497633,4.12570411955144,5.29543964753872));
#67741=CARTESIAN_POINT('Ctrl Pts',(-4.25293536880354,1.01313616246135,5.49432589753872));
#67742=CARTESIAN_POINT('Ctrl Pts',(-3.15127038816007,-3.03041236061429,
5.69321214753872));
#67743=CARTESIAN_POINT('Ctrl Pts',(0.846127267944299,-4.2892858125268,5.89209839753872));
#67744=CARTESIAN_POINT('Ctrl Pts',(4.06601043764664,-1.60669326751191,6.09098464753873));
#67745=CARTESIAN_POINT('Ctrl Pts',(3.54959750041304,2.55230517767038,6.28987089753872));
#67746=CARTESIAN_POINT('Ctrl Pts',(-0.228574727733499,4.36596584146089,
6.48875714753872));
#67747=CARTESIAN_POINT('Ctrl Pts',(-3.79670743963632,2.16769849212081,6.68764339753873));
#67748=CARTESIAN_POINT('Ctrl Pts',(-3.87600916022575,-2.02248785528584,
6.88652964753872));
#67749=CARTESIAN_POINT('Ctrl Pts',(-0.393608775556405,-4.35419065576435,
7.08541589753873));
#67750=CARTESIAN_POINT('Ctrl Pts',(3.45048249956151,-2.68478577453692,7.28430214753871));
#67751=CARTESIAN_POINT('Ctrl Pts',(4.12389221154984,1.45169458304942,7.48318839753873));
#67752=CARTESIAN_POINT('Ctrl Pts',(1.00781769773627,4.25419882270057,7.68207464753872));
#67753=CARTESIAN_POINT('Ctrl Pts',(-3.03435019392059,3.14747883798937,7.88096089753873));
#67754=CARTESIAN_POINT('Ctrl Pts',(-4.2882245013715,-0.851489730281045,
8.07984714753873));
#67755=CARTESIAN_POINT('Ctrl Pts',(-1.60160806099616,-4.06801619390695,
8.27873339753872));
#67756=CARTESIAN_POINT('Ctrl Pts',(2.5567414343955,-3.54640344188055,8.47761964753874));
#67757=CARTESIAN_POINT('Ctrl Pts',(4.36567662939378,0.234033549949525,8.67650589753872));
#67758=CARTESIAN_POINT('Ctrl Pts',(2.16294957102227,3.79941486128476,8.87539214753873));
#67759=CARTESIAN_POINT('Ctrl Pts',(-2.02733265613809,3.87347730550896,9.07427839753872));
#67760=CARTESIAN_POINT('Ctrl Pts',(-4.35467940225657,0.388164190130051,
9.27316464753873));
#67761=CARTESIAN_POINT('Ctrl Pts',(-2.68046935281703,-3.45383673377096,
9.47205089753873));
#67762=CARTESIAN_POINT('Ctrl Pts',(1.456849771539,-4.12207385645912,9.67093714753872));
#67763=CARTESIAN_POINT('Ctrl Pts',(4.25545562566251,-1.00249765733107,9.86982339753873));
#67764=CARTESIAN_POINT('Ctrl Pts',(3.14368236709142,3.03828328333213,10.0687096475387));
#67765=CARTESIAN_POINT('Ctrl Pts',(-0.856850861408087,4.28715648609206,
10.2675958975387));
#67766=CARTESIAN_POINT('Ctrl Pts',(-4.07001559029531,1.59652035054053,10.4664821475387));
#67767=CARTESIAN_POINT('Ctrl Pts',(-3.54320383895445,-2.56117369394491,
10.6653683975387));
#67768=CARTESIAN_POINT('Ctrl Pts',(0.239492006280512,-4.36538059209787,
10.8642546475387));
#67769=CARTESIAN_POINT('Ctrl Pts',(3.80211634298675,-2.15819726840019,11.0631408975387));
#67770=CARTESIAN_POINT('Ctrl Pts',(3.87093939505723,2.0321742874889,11.2620271475387));
#67771=CARTESIAN_POINT('Ctrl Pts',(0.382718997853834,4.35516134071043,11.4609133975387));
#67772=CARTESIAN_POINT('Ctrl Pts',(-3.45718556830527,2.67614874049235,11.6597996475387));
#67773=CARTESIAN_POINT('Ctrl Pts',(-4.12024905698152,-1.46200268241196,
11.8586858975387));
#67774=CARTESIAN_POINT('Ctrl Pts',(-0.997176049636473,-4.25670577571064,
12.0575721475387));
#67775=CARTESIAN_POINT('Ctrl Pts',(3.04221162273831,-3.13988098140884,12.2564583975387));
#67776=CARTESIAN_POINT('Ctrl Pts',(4.28608176833814,0.862210652947643,12.4553446475387));
#67777=CARTESIAN_POINT('Ctrl Pts',(1.59143014410956,4.07200862368394,12.6542308975387));
#67778=CARTESIAN_POINT('Ctrl Pts',(-2.5656019493948,3.53999869663798,12.8531171475387));
#67779=CARTESIAN_POINT('Ctrl Pts',(-4.36507773003311,-0.244950088193424,
13.0520033975387));
#67780=CARTESIAN_POINT('Ctrl Pts',(-2.15344159168568,-3.80481188051856,
13.2508896475387));
#67781=CARTESIAN_POINT('Ctrl Pts',(2.0370127417697,-3.86839543283839,13.4497758975388));
#67782=CARTESIAN_POINT('Ctrl Pts',(4.35563647037208,-0.377273207240618,
13.6486621475387));
#67783=CARTESIAN_POINT('Ctrl Pts',(2.67182394431791,3.46052899792885,13.8475483975387));
#67784=CARTESIAN_POINT('Ctrl Pts',(-1.46715330761245,4.11841781596996,14.0464346475388));
#67785=CARTESIAN_POINT('Ctrl Pts',(-4.25794927089048,0.991852882972159,
14.2453208975387));
#67786=CARTESIAN_POINT('Ctrl Pts',(-3.13607468688462,-3.04613520599768,
14.4442071475388));
#67787=CARTESIAN_POINT('Ctrl Pts',(0.867569096520351,-4.28500034978993,
14.6430933975387));
#67788=CARTESIAN_POINT('Ctrl Pts',(4.07399529095696,-1.58633744966117,14.8419796475388));
#67789=CARTESIAN_POINT('Ctrl Pts',(3.53678801994201,2.57002619382208,15.0408658975387));
#67790=CARTESIAN_POINT('Ctrl Pts',(-0.250407787155136,4.364768043673,15.2397521475388));
#67791=CARTESIAN_POINT('Ctrl Pts',(-3.80750146966602,2.14868254831374,15.4386383975387));
#67792=CARTESIAN_POINT('Ctrl Pts',(-3.86584542282966,-2.04184801141611,
15.6375246475387));
#67793=CARTESIAN_POINT('Ctrl Pts',(-0.371826826804321,-4.35610479049868,
15.8364108975387));
#67794=CARTESIAN_POINT('Ctrl Pts',(3.46386701741464,-2.66749497105505,16.0352971475387));
#67795=CARTESIAN_POINT('Ctrl Pts',(4.11658013628737,1.47230163908801,16.2341833975387));
#67796=CARTESIAN_POINT('Ctrl Pts',(0.986528165660311,4.25918610925795,16.4330696475388));
#67797=CARTESIAN_POINT('Ctrl Pts',(-3.05005402697614,3.13226348946949,16.6319558975387));
#67798=CARTESIAN_POINT('Ctrl Pts',(-4.28391223213811,-0.872926183748866,
16.8308421475388));
#67799=CARTESIAN_POINT('Ctrl Pts',(-1.58124227515725,-4.07597558900841,
17.0297283975387));
#67800=CARTESIAN_POINT('Ctrl Pts',(2.57444642030993,-3.53357181388611,17.2286146475388));
#67801=CARTESIAN_POINT('Ctrl Pts',(4.3644515335017,0.255865094633145,17.4275008975387));
#67802=CARTESIAN_POINT('Ctrl Pts',(2.14392014572458,3.81018510622428,17.6263871475388));
#67803=CARTESIAN_POINT('Ctrl Pts',(-2.04668008886878,3.86328936901768,17.8252733975387));
#67804=CARTESIAN_POINT('Ctrl Pts',(-4.3565663003581,0.366379865059645,18.0241596475388));
#67805=CARTESIAN_POINT('Ctrl Pts',(-2.66316182747159,-3.46719962154403,
18.2230458975387));
#67806=CARTESIAN_POINT('Ctrl Pts',(1.47744766878984,-4.11473602080673,18.4219321475387));
#67807=CARTESIAN_POINT('Ctrl Pts',(4.26041628887939,-0.98120190602555,18.6208183975388));
#67808=CARTESIAN_POINT('Ctrl Pts',(3.12844739512184,3.05396807954705,18.8197046475387));
#67809=CARTESIAN_POINT('Ctrl Pts',(-0.878281906258018,4.28281741708385,
19.0185908975388));
#67810=CARTESIAN_POINT('Ctrl Pts',(-4.07794951474237,1.57614462856346,19.2174771475387));
#67811=CARTESIAN_POINT('Ctrl Pts',(-3.53035008349838,-2.57886262194789,
19.4163633975388));
#67812=CARTESIAN_POINT('Ctrl Pts',(0.261322002095605,-4.36412820001402,
19.6152496475387));
#67813=CARTESIAN_POINT('Ctrl Pts',(3.81286278599776,-2.13915439136365,19.8141358975387));
#67814=CARTESIAN_POINT('Ctrl Pts',(3.86072727539858,2.05150896657326,20.0130221475387));
#67815=CARTESIAN_POINT('Ctrl Pts',(0.360932330522345,4.35702099922879,20.2119083975387));
#67816=CARTESIAN_POINT('Ctrl Pts',(-3.4705268051069,2.65882452034193,20.4107946475388));
#67817=CARTESIAN_POINT('Ctrl Pts',(-4.11288547241112,-1.48259138867275,
20.6096808975387));
#67818=CARTESIAN_POINT('Ctrl Pts',(-0.975874112394784,-4.26163980783156,
20.8085671475387));
#67819=CARTESIAN_POINT('Ctrl Pts',(3.05787735759126,-3.12462640980767,21.0074533975388));
#67820=CARTESIAN_POINT('Ctrl Pts',(4.28171590633873,0.883636255674747,21.2063396475387));
#67821=CARTESIAN_POINT('Ctrl Pts',(1.57104451784945,4.07991706507279,21.4052258975388));
#67822=CARTESIAN_POINT('Ctrl Pts',(-2.58327479183168,3.52712283381567,21.6041121475387));
#67823=CARTESIAN_POINT('Ctrl Pts',(-4.3637980437155,-0.266778501011266,
21.8029983975388));
#67824=CARTESIAN_POINT('Ctrl Pts',(-2.13438529268163,-3.81553450480025,
22.0018846475387));
#67825=CARTESIAN_POINT('Ctrl Pts',(2.05633463698022,-3.85815914597783,22.2007708975388));
#67826=CARTESIAN_POINT('Ctrl Pts',(4.3574688863999,-0.355484231708993,22.3996571475387));
#67827=CARTESIAN_POINT('Ctrl Pts',(2.65448305644691,3.47384856290156,22.5985433975388));
#67828=CARTESIAN_POINT('Ctrl Pts',(-1.48773279069503,4.11102849399365,22.7974296475387));
#67829=CARTESIAN_POINT('Ctrl Pts',(-4.26285666420163,0.970544793097504,
22.9963158975388));
#67830=CARTESIAN_POINT('Ctrl Pts',(-3.12080053950068,-3.06178185499708,
23.1952021475388));
#67831=CARTESIAN_POINT('Ctrl Pts',(0.888989223628163,-4.28060770162484,
23.3940883975387));
#67832=CARTESIAN_POINT('Ctrl Pts',(4.08187823692364,-1.56594195098862,23.5929746475388));
#67833=CARTESIAN_POINT('Ctrl Pts',(3.52389006988343,2.58768292306338,23.7918608975387));
#67834=CARTESIAN_POINT('Ctrl Pts',(-0.272234582849482,4.36346106512225,
23.9907471475388));
#67835=CARTESIAN_POINT('Ctrl Pts',(-3.81820025845479,2.12961285713456,24.1896333975387));
#67836=CARTESIAN_POINT('Ctrl Pts',(-3.85558498477047,-2.06115709254521,
24.3885196475388));
#67837=CARTESIAN_POINT('Ctrl Pts',(-0.350035577137102,-4.3579099611712,
24.5874058975388));
#67838=CARTESIAN_POINT('Ctrl Pts',(3.47716488973482,-2.65013744257396,24.7862921475387));
#67839=CARTESIAN_POINT('Ctrl Pts',(4.1091650884575,1.49287186681883,24.9851783975387));
#67840=CARTESIAN_POINT('Ctrl Pts',(0.965213956465368,4.2640668560872,25.1840646475388));
#67841=CARTESIAN_POINT('Ctrl Pts',(-3.06568156566023,3.11696979018211,25.3829508975388));
#67842=CARTESIAN_POINT('Ctrl Pts',(-4.27949280467476,-0.894340801749458,
25.5818371475387));
#67843=CARTESIAN_POINT('Ctrl Pts',(-1.56083693595826,-4.08383302722886,
25.7807233975388));
#67844=CARTESIAN_POINT('Ctrl Pts',(2.59208700875147,-3.52065179675568,25.9796096475387));
#67845=CARTESIAN_POINT('Ctrl Pts',(4.36311726476112,0.277690239080396,26.1784958975388));
#67846=CARTESIAN_POINT('Ctrl Pts',(2.12483709218347,3.82086004279379,26.3773821475388));
#67847=CARTESIAN_POINT('Ctrl Pts',(-2.06597632572891,3.85300479580088,26.5762683975387));
#67848=CARTESIAN_POINT('Ctrl Pts',(-4.35834422285313,0.344586375324983,
26.7751546475387));
#67849=CARTESIAN_POINT('Ctrl Pts',(-2.64578768551692,-3.48047578042199,
26.9740408975387));
#67850=CARTESIAN_POINT('Ctrl Pts',(1.49800860900966,-4.10729525871589,27.1729271475388));
#67851=CARTESIAN_POINT('Ctrl Pts',(4.26527038159624,-0.959881610832656,
27.3718133975387));
#67852=CARTESIAN_POINT('Ctrl Pts',(3.11313416784098,3.06957648348399,27.5706996475387));
#67853=CARTESIAN_POINT('Ctrl Pts',(-0.899690981672145,4.27837121723149,
27.7695858975388));
#67854=CARTESIAN_POINT('Ctrl Pts',(-4.08578143293244,1.55572948073937,27.9684721475387));
#67855=CARTESIAN_POINT('Ctrl Pts',(-3.517408019495,-2.59648704201063,28.1673583975388));
#67856=CARTESIAN_POINT('Ctrl Pts',(0.283145461174642,-4.36276664316957,
28.3662446475387));
#67857=CARTESIAN_POINT('Ctrl Pts',(3.82351385365899,-2.12005800529481,28.5651308975388));
#67858=CARTESIAN_POINT('Ctrl Pts',(3.85041858310289,2.07079232899705,28.7640171475388));
#67859=CARTESIAN_POINT('Ctrl Pts',(0.339136634791738,4.3587716707668,28.9629033975388));
#67860=CARTESIAN_POINT('Ctrl Pts',(-3.48378122978692,2.64143379207604,29.1617896475387));
#67861=CARTESIAN_POINT('Ctrl Pts',(-4.10541900769204,-1.5031430092369,29.3606758975388));
#67862=CARTESIAN_POINT('Ctrl Pts',(-0.954547764535808,-4.26646723884722,
29.5595621475387));
#67863=CARTESIAN_POINT('Ctrl Pts',(3.07346660237915,-3.10929367847378,29.7584483975388));
#67864=CARTESIAN_POINT('Ctrl Pts',(4.27724294104848,0.905039755031803,29.9573346475388));
#67865=CARTESIAN_POINT('Ctrl Pts',(1.55061959331699,4.08772345098814,30.1562208975387));
#67866=CARTESIAN_POINT('Ctrl Pts',(-2.60088301596186,3.51415874317283,30.3551071475388));
#67867=CARTESIAN_POINT('Ctrl Pts',(-4.36240920089582,-0.288600240603635,
30.5539933975387));
#67868=CARTESIAN_POINT('Ctrl Pts',(-2.11527560394003,-3.82616168690154,
30.7528796475387));
#67869=CARTESIAN_POINT('Ctrl Pts',(2.07560509482036,-3.84782635071967,30.9517658975388));
#67870=CARTESIAN_POINT('Ctrl Pts',(4.35919230424386,-0.333686364057531,
31.1506521475388));
#67871=CARTESIAN_POINT('Ctrl Pts',(2.63707576905832,3.48708123266181,31.3495383975388));
#67872=CARTESIAN_POINT('Ctrl Pts',(-1.50827505947353,4.10353633831938,31.5484246475388));
#67873=CARTESIAN_POINT('Ctrl Pts',(-4.26765742596897,0.949212425913485,
31.7473108975388));
#67874=CARTESIAN_POINT('Ctrl Pts',(-3.10544832808469,-3.07735191626373,
31.9461971475387));
#67875=CARTESIAN_POINT('Ctrl Pts',(0.91038711346635,-4.27610797789004,32.1450833975388));
#67876=CARTESIAN_POINT('Ctrl Pts',(4.08965907835965,-1.54550728167909,32.3439696475388));
#67877=CARTESIAN_POINT('Ctrl Pts',(3.51090397286941,2.60527492373118,32.5428558975387));
#67878=CARTESIAN_POINT('Ctrl Pts',(-0.29405456884035,4.36204493850143,32.7417421475388));
#67879=CARTESIAN_POINT('Ctrl Pts',(-3.82880353838003,2.11048989559061,32.9406283975388));
#67880=CARTESIAN_POINT('Ctrl Pts',(-3.84522810270724,-2.08041461566436,
33.1395146475387));
#67881=CARTESIAN_POINT('Ctrl Pts',(-0.328235571637042,-4.35960612264627,
33.3384008975388));
#67882=CARTESIAN_POINT('Ctrl Pts',(3.49037578387586,-2.6327136232396,33.5372871475387));
#67883=CARTESIAN_POINT('Ctrl Pts',(4.10164725356363,1.51340475162492,33.7361733975388));
#67884=CARTESIAN_POINT('Ctrl Pts',(0.943875603264011,4.26884094123703,33.9350596475387));
#67885=CARTESIAN_POINT('Ctrl Pts',(-3.0812324189812,3.10159812242476,34.1339458975388));
#67886=CARTESIAN_POINT('Ctrl Pts',(-4.27496632968791,-0.915733048116786,
34.3328321475387));
#67887=CARTESIAN_POINT('Ctrl Pts',(-1.54039255351717,-4.0915883129756,34.5317183975388));
#67888=CARTESIAN_POINT('Ctrl Pts',(2.60966275787677,-3.50764371184675,34.7306046475388));
#67889=CARTESIAN_POINT('Ctrl Pts',(4.36167385765697,0.299508433863526,34.9294908975388));
#67890=CARTESIAN_POINT('Ctrl Pts',(2.10570088562199,3.83143941064858,35.1283771475388));
#67891=CARTESIAN_POINT('Ctrl Pts',(-2.08522087998014,3.8426238303401,35.3272633975388));
#67892=CARTESIAN_POINT('Ctrl Pts',(-4.36001313303645,0.322784290515226,
35.5261496475388));
#67893=CARTESIAN_POINT('Ctrl Pts',(-2.628347346691,-3.49366492507817,35.7250358975388));
#67894=CARTESIAN_POINT('Ctrl Pts',(1.51853204945604,-4.09975166684699,35.9239221475388));
#67895=CARTESIAN_POINT('Ctrl Pts',(4.27001783677883,-0.938537476210095,
36.1228083975388));
#67896=CARTESIAN_POINT('Ctrl Pts',(3.09774296425047,3.08510843213345,36.3216946475388));
#67897=CARTESIAN_POINT('Ctrl Pts',(-0.921077353076951,4.27381737137538,
36.5205808975388));
#67898=CARTESIAN_POINT('Ctrl Pts',(-4.09351152974297,1.53527661603589,36.7194671475388));
#67899=CARTESIAN_POINT('Ctrl Pts',(-3.50437724220988,-2.61404880570331,
36.9183533975387));
#67900=CARTESIAN_POINT('Ctrl Pts',(0.304960444014917,-4.36129157005399,
37.1172396475388));
#67901=CARTESIAN_POINT('Ctrl Pts',(3.83407194560894,-2.10091697775549,37.3161258975387));
#67902=CARTESIAN_POINT('Ctrl Pts',(3.84000847567348,2.09003994280635,37.5150121475388));
#67903=CARTESIAN_POINT('Ctrl Pts',(0.31734221318727,4.36038260604223,37.7138983975388));
#67904=CARTESIAN_POINT('Ctrl Pts',(-3.49696717721569,2.62403573243536,37.9127846475388));
#67905=CARTESIAN_POINT('Ctrl Pts',(-4.09781413941906,-1.52376940766611,
38.1116708975388));
#67906=CARTESIAN_POINT('Ctrl Pts',(-0.933265856159647,-4.27097295467856,
38.3105571475387));
#67907=CARTESIAN_POINT('Ctrl Pts',(3.08910966785189,-3.09429453424015,38.5094433975388));
#67908=CARTESIAN_POINT('Ctrl Pts',(4.27241288751803,0.927208179448248,38.7083296475388));
#67909=CARTESIAN_POINT('Ctrl Pts',(1.53063485040313,4.09391556409043,38.9072158975388));
#67910=CARTESIAN_POINT('Ctrl Pts',(-2.61934711719507,3.50404733708965,39.1061021475388));
#67911=CARTESIAN_POINT('Ctrl Pts',(-4.35910709167342,-0.316468415429424,
39.3049883975388));
#67912=CARTESIAN_POINT('Ctrl Pts',(-2.85308220258183,-2.65317527854529,
39.4375792308721));
#67913=CARTESIAN_POINT('Ctrl Pts',(-1.7721534639367,-3.24372257795841,39.5038746475388));
#67914=CARTESIAN_POINT('Ctrl Pts',(2.0090772186955,-2.81633609132837,-0.136687676230644));
#67915=CARTESIAN_POINT('Ctrl Pts',(2.94758491953483,-2.14683700450694,-0.070392259563977));
#67916=CARTESIAN_POINT('Ctrl Pts',(4.08609293119346,0.192777765232804,0.0621985737693567));
#67917=CARTESIAN_POINT('Ctrl Pts',(2.04269690202567,3.54872309047107,0.261084823769356));
#67918=CARTESIAN_POINT('Ctrl Pts',(-1.87959970053929,3.63336178935976,0.459971073769358));
#67919=CARTESIAN_POINT('Ctrl Pts',(-4.07374364010612,0.384441434745174,
0.658857323769356));
#67920=CARTESIAN_POINT('Ctrl Pts',(-2.52499323873643,-3.22042266815715,
0.857743573769359));
#67921=CARTESIAN_POINT('Ctrl Pts',(1.34426329021304,-3.86461315715718,1.05662982376936));
#67922=CARTESIAN_POINT('Ctrl Pts',(3.97812453353371,-0.958302950108288,
1.25551607376936));
#67923=CARTESIAN_POINT('Ctrl Pts',(2.95652143571546,2.82898235111471,1.45440232376936));
#67924=CARTESIAN_POINT('Ctrl Pts',(-0.781895581985945,4.01648924816669,
1.65328857376936));
#67925=CARTESIAN_POINT('Ctrl Pts',(-3.80180140043137,1.51330971689742,1.85217482376936));
#67926=CARTESIAN_POINT('Ctrl Pts',(-3.3282057019711,-2.38051912920303,2.05106107376936));
#67927=CARTESIAN_POINT('Ctrl Pts',(0.203715651461493,-4.08683758028472,
2.24994732376936));
#67928=CARTESIAN_POINT('Ctrl Pts',(3.54843790115571,-2.03773654256675,2.44883357376936));
#67929=CARTESIAN_POINT('Ctrl Pts',(3.63246790710264,1.88386798553642,2.64771982376936));
#67930=CARTESIAN_POINT('Ctrl Pts',(0.378587434436055,4.07436403283702,2.84660607376937));
#67931=CARTESIAN_POINT('Ctrl Pts',(-3.22318026935398,2.52088989946966,3.04549232376936));
#67932=CARTESIAN_POINT('Ctrl Pts',(-3.86313682746238,-1.34905532485943,
3.24437857376936));
#67933=CARTESIAN_POINT('Ctrl Pts',(-0.953219680208054,-3.97934005231632,
3.44326482376936));
#67934=CARTESIAN_POINT('Ctrl Pts',(2.83262014357182,-2.95297122725163,3.64215107376936));
#67935=CARTESIAN_POINT('Ctrl Pts',(4.01553809728831,0.786911425333983,3.84103732376936));
#67936=CARTESIAN_POINT('Ctrl Pts',(1.50853944740008,3.80369351600713,4.03992357376936));
#67937=CARTESIAN_POINT('Ctrl Pts',(-2.38467060488288,3.32522508593738,4.23880982376937));
#67938=CARTESIAN_POINT('Ctrl Pts',(-4.0865839016778,-0.208824687545051,
4.43769607376936));
#67939=CARTESIAN_POINT('Ctrl Pts',(-2.0332959352706,-3.55098343486414,4.63658232376937));
#67940=CARTESIAN_POINT('Ctrl Pts',(1.88840722556278,-3.63010934895867,4.83546857376936));
#67941=CARTESIAN_POINT('Ctrl Pts',(4.07483482061434,-0.373492856732322,
5.03435482376936));
#67942=CARTESIAN_POINT('Ctrl Pts',(2.51685749801378,3.22632981292407,5.23324107376936));
#67943=CARTESIAN_POINT('Ctrl Pts',(-1.35388439197982,3.86144698047705,5.43212732376937));
#67944=CARTESIAN_POINT('Ctrl Pts',(-3.9805288896519,0.948243369370376,5.63101357376936));
#67945=CARTESIAN_POINT('Ctrl Pts',(-2.94942709714979,-2.83631019588636,
5.82989982376937));
#67946=CARTESIAN_POINT('Ctrl Pts',(0.791931628935568,-4.01455103643869,
6.02878607376936));
#67947=CARTESIAN_POINT('Ctrl Pts',(3.80557676267527,-1.50378230881505,6.22767232376937));
#67948=CARTESIAN_POINT('Ctrl Pts',(3.32224079883099,2.38882644900927,6.42655857376937));
#67949=CARTESIAN_POINT('Ctrl Pts',(-0.213934195629035,4.08631960190299,
6.62544482376937));
#67950=CARTESIAN_POINT('Ctrl Pts',(-3.55352299964065,2.02885436144528,6.82433107376937));
#67951=CARTESIAN_POINT('Ctrl Pts',(-3.62774533373042,-1.89294466969528,
7.02321732376936));
#67952=CARTESIAN_POINT('Ctrl Pts',(-0.368397581072059,-4.07529863337619,
7.22210357376937));
#67953=CARTESIAN_POINT('Ctrl Pts',(3.22947425288682,-2.51282147771678,7.42098982376937));
#67954=CARTESIAN_POINT('Ctrl Pts',(3.85975112772587,1.35871150762509,7.61987607376937));
#67955=CARTESIAN_POINT('Ctrl Pts',(0.943265559775128,3.98171141755363,7.81876232376937));
#67956=CARTESIAN_POINT('Ctrl Pts',(-2.83999580544285,2.94587840108877,8.01764857376936));
#67957=CARTESIAN_POINT('Ctrl Pts',(-4.01355770375238,-0.796950618033701,
8.21653482376938));
#67958=CARTESIAN_POINT('Ctrl Pts',(-1.49902281691347,-3.80745404743213,
8.41542107376936));
#67959=CARTESIAN_POINT('Ctrl Pts',(2.39297855726508,-3.3192513242302,8.61430732376938));
#67960=CARTESIAN_POINT('Ctrl Pts',(4.08604891427468,0.219043372620942,8.81319357376936));
#67961=CARTESIAN_POINT('Ctrl Pts',(2.02440961540798,3.55605700713278,9.01207982376937));
#67962=CARTESIAN_POINT('Ctrl Pts',(-1.89747915425351,3.62537564786158,9.21096607376936));
#67963=CARTESIAN_POINT('Ctrl Pts',(-4.07575607496965,0.363301728983464,
9.40985232376938));
#67964=CARTESIAN_POINT('Ctrl Pts',(-2.50878152886593,-3.23261364368766,
9.60873857376937));
#67965=CARTESIAN_POINT('Ctrl Pts',(1.36353649905687,-3.85804924083067,9.80762482376936));
#67966=CARTESIAN_POINT('Ctrl Pts',(3.98288772052199,-0.938286275424292,
10.0065110737694));
#67967=CARTESIAN_POINT('Ctrl Pts',(2.94232509947999,2.84367697495768,10.2053973237694));
#67968=CARTESIAN_POINT('Ctrl Pts',(-0.80196836118798,4.01255809635049,10.4042835737694));
#67969=CARTESIAN_POINT('Ctrl Pts',(-3.80932537967576,1.49426098145287,10.6031698237694));
#67970=CARTESIAN_POINT('Ctrl Pts',(-3.316256660362,-2.3971269243699,10.8020560737694));
#67971=CARTESIAN_POINT('Ctrl Pts',(0.224152207163268,-4.08577183858305,
11.0009423237694));
#67972=CARTESIAN_POINT('Ctrl Pts',(3.55858545514036,-2.01996170443845,11.1998285737694));
#67973=CARTESIAN_POINT('Ctrl Pts',(3.6230002941361,1.90201067232131,11.3987148237694));
#67974=CARTESIAN_POINT('Ctrl Pts',(0.358205308914588,4.07620714458917,11.5976010737694));
#67975=CARTESIAN_POINT('Ctrl Pts',(-3.23574798067012,2.50473765782441,11.7964873237694));
#67976=CARTESIAN_POINT('Ctrl Pts',(-3.85634132232064,-1.36835935875657,
11.9953735737694));
#67977=CARTESIAN_POINT('Ctrl Pts',(-0.93330552417114,-3.98405779670502,
12.1942598237694));
#67978=CARTESIAN_POINT('Ctrl Pts',(2.84735369871167,-2.93876719788543,12.3931460737694));
#67979=CARTESIAN_POINT('Ctrl Pts',(4.01155221577702,0.80698485055723,12.5920323237694));
#67980=CARTESIAN_POINT('Ctrl Pts',(1.48949680988765,3.81119075647874,12.7909185737694));
#67981=CARTESIAN_POINT('Ctrl Pts',(-2.40127154384339,3.31325681190915,12.9898048237694));
#67982=CARTESIAN_POINT('Ctrl Pts',(-4.08548837525859,-0.229260691269513,
13.1886910737694));
#67983=CARTESIAN_POINT('Ctrl Pts',(-2.01551063549186,-3.56110833971021,
13.3875773237694));
#67984=CARTESIAN_POINT('Ctrl Pts',(1.9065392168149,-3.6206192762677,13.5864635737694));
#67985=CARTESIAN_POINT('Ctrl Pts',(4.07665184152917,-0.353108328833043,
13.7853498237694));
#67986=CARTESIAN_POINT('Ctrl Pts',(2.50068987091457,3.23887725893398,13.9842360737694));
#67987=CARTESIAN_POINT('Ctrl Pts',(-1.37318007918433,3.85462737486591,14.1831223237694));
#67988=CARTESIAN_POINT('Ctrl Pts',(-3.9852216442734,0.928323313802475,14.3820085737694));
#67989=CARTESIAN_POINT('Ctrl Pts',(-2.93520470186743,-2.85102597095673,
14.5808948237694));
#67990=CARTESIAN_POINT('Ctrl Pts',(0.812000078298801,-4.01054006360455,
14.7797810737693));
#67991=CARTESIAN_POINT('Ctrl Pts',(3.81305017492473,-1.48473030966602,14.9786673237694));
#67992=CARTESIAN_POINT('Ctrl Pts',(3.31025178356159,2.4054124092059,15.1775535737694));
#67993=CARTESIAN_POINT('Ctrl Pts',(-0.234368816953125,4.08519852474447,
15.3764398237694));
#67994=CARTESIAN_POINT('Ctrl Pts',(-3.56362565689806,2.01105641552697,15.5753260737694));
#67995=CARTESIAN_POINT('Ctrl Pts',(-3.61823259797885,-1.9110647806544,15.7742123237694));
#67996=CARTESIAN_POINT('Ctrl Pts',(-0.348010796707407,-4.0770901650944,
15.9730985737694));
#67997=CARTESIAN_POINT('Ctrl Pts',(3.24200147358696,-2.49663817446469,16.1719848237694));
#67998=CARTESIAN_POINT('Ctrl Pts',(3.85290740114609,1.37799865280346,16.3708710737694));
#67999=CARTESIAN_POINT('Ctrl Pts',(0.923339652107423,3.9863792614076,16.5697573237694));
#68000=CARTESIAN_POINT('Ctrl Pts',(-2.85469378595166,2.93163761699557,16.7686435737694));
#68001=CARTESIAN_POINT('Ctrl Pts',(-4.00952164141544,-0.817014036571931,
16.9675298237694));
#68002=CARTESIAN_POINT('Ctrl Pts',(-1.47996148823989,-3.81490363210673,
17.1664160737694));
#68003=CARTESIAN_POINT('Ctrl Pts',(2.40954951398363,-3.30724158001736,17.3653023237694));
#68004=CARTESIAN_POINT('Ctrl Pts',(4.08490228749385,0.239476576228112,17.5641885737694));
#68005=CARTESIAN_POINT('Ctrl Pts',(2.00659905150743,3.56613740276842,17.7630748237694));
#68006=CARTESIAN_POINT('Ctrl Pts',(-1.91558735676465,3.61584026300082,17.9619610737694));
#68007=CARTESIAN_POINT('Ctrl Pts',(-4.07752211459962,0.342912720507015,
18.1608473237694));
#68008=CARTESIAN_POINT('Ctrl Pts',(-2.4925825748091,-3.24512061974472,18.3597335737694));
#68009=CARTESIAN_POINT('Ctrl Pts',(1.38281507208069,-3.85118140385011,18.5586198237694));
#68010=CARTESIAN_POINT('Ctrl Pts',(3.98753064629779,-0.918354546877404,
18.7575060737694));
#68011=CARTESIAN_POINT('Ctrl Pts',(2.92806594884658,2.85835713796223,18.9563923237694));
#68012=CARTESIAN_POINT('Ctrl Pts',(-0.822026717537881,4.00849695080192,
19.1552785737694));
#68013=CARTESIAN_POINT('Ctrl Pts',(-3.81675112512713,1.47519035306472,19.3541648237694));
#68014=CARTESIAN_POINT('Ctrl Pts',(-3.30422620598249,-2.41368285170877,
19.5530510737694));
#68015=CARTESIAN_POINT('Ctrl Pts',(0.244583961109105,-4.08459966396984,
19.7519373237694));
#68016=CARTESIAN_POINT('Ctrl Pts',(3.56864357339442,-2.00213855040182,19.9508235737694));
#68017=CARTESIAN_POINT('Ctrl Pts',(3.61344227507378,1.92010693807507,20.1497098237694));
#68018=CARTESIAN_POINT('Ctrl Pts',(0.33781410820217,4.07794768936949,20.3485960737694));
#68019=CARTESIAN_POINT('Ctrl Pts',(-3.24823469253086,2.48852307828828,20.5474823237694));
#68020=CARTESIAN_POINT('Ctrl Pts',(-3.84944938567638,-1.38762932948615,
20.7463685737694));
#68021=CARTESIAN_POINT('Ctrl Pts',(-0.913368005905981,-3.98867579714393,
20.9452548237694));
#68022=CARTESIAN_POINT('Ctrl Pts',(2.86201602126123,-2.92448970300433,21.1441410737694));
#68023=CARTESIAN_POINT('Ctrl Pts',(4.00746599336594,0.827038113359913,21.3430273237694));
#68024=CARTESIAN_POINT('Ctrl Pts',(1.4704169115997,3.81859265109753,21.5419135737694));
#68025=CARTESIAN_POINT('Ctrl Pts',(-2.41781241591925,3.30120566617125,21.7407998237694));
#68026=CARTESIAN_POINT('Ctrl Pts',(-4.08429065464559,-0.249690963611301,
21.9396860737694));
#68027=CARTESIAN_POINT('Ctrl Pts',(-1.99767491918358,-3.57114416485799,
22.1385723237693));
#68028=CARTESIAN_POINT('Ctrl Pts',(1.92462351751989,-3.61103863794668,22.3374585737694));
#68029=CARTESIAN_POINT('Ctrl Pts',(4.0783668887387,-0.332714967763942,22.5363448237694));
#68030=CARTESIAN_POINT('Ctrl Pts',(2.48445969124877,3.25134368707685,22.7352310737694));
#68031=CARTESIAN_POINT('Ctrl Pts',(-1.39244141749321,3.84771134933273,22.9341173237694));
#68032=CARTESIAN_POINT('Ctrl Pts',(-3.9898147121557,0.908380036989118,23.1330035737694));
#68033=CARTESIAN_POINT('Ctrl Pts',(-2.92090888505992,-2.86567043012844,
23.3318898237694));
#68034=CARTESIAN_POINT('Ctrl Pts',(0.83204821620329,-4.00642877071929,23.5307760737694));
#68035=CARTESIAN_POINT('Ctrl Pts',(3.82042820713893,-1.46564117130749,23.7296623237694));
#68036=CARTESIAN_POINT('Ctrl Pts',(3.29817996530588,2.42193820015896,23.9285485737694));
#68037=CARTESIAN_POINT('Ctrl Pts',(-0.254797575750441,4.08397526000418,
24.1274348237694));
#68038=CARTESIAN_POINT('Ctrl Pts',(-3.57363917324971,1.99320816483117,24.3263210737694));
#68039=CARTESIAN_POINT('Ctrl Pts',(-3.60862935537735,-1.92913708803787,
24.5252073237694));
#68040=CARTESIAN_POINT('Ctrl Pts',(-0.327615307164295,-4.07877971205188,
24.7240935737694));
#68041=CARTESIAN_POINT('Ctrl Pts',(3.25444759852215,-2.48039242004323,24.9229798237694));
#68042=CARTESIAN_POINT('Ctrl Pts',(3.84596729753637,1.39725132857884,25.1218660737694));
#68043=CARTESIAN_POINT('Ctrl Pts',(0.903390647924833,3.99094738955255,25.3207523237694));
#68044=CARTESIAN_POINT('Ctrl Pts',(-2.86932035885057,2.91732350061147,25.5196385737694));
#68045=CARTESIAN_POINT('Ctrl Pts',(-4.00538528448356,-0.837057018235249,
25.7185248237694));
#68046=CARTESIAN_POINT('Ctrl Pts',(-1.46086313965446,-3.82225779038165,
25.9174110737694));
#68047=CARTESIAN_POINT('Ctrl Pts',(2.42606019797783,-3.29514910811671,26.1162973237694));
#68048=CARTESIAN_POINT('Ctrl Pts',(4.08365348053868,0.259903789543027,26.3151835737694));
#68049=CARTESIAN_POINT('Ctrl Pts',(1.98873829432774,3.57612859466892,26.5140698237694));
#68050=CARTESIAN_POINT('Ctrl Pts',(-1.9336476425726,3.60621443113243,26.7129560737694));
#68051=CARTESIAN_POINT('Ctrl Pts',(-4.07918615866362,0.322515134375918,
26.9118423237694));
#68052=CARTESIAN_POINT('Ctrl Pts',(-2.47632127103036,-3.25754642201413,
27.1107285737694));
#68053=CARTESIAN_POINT('Ctrl Pts',(1.40205905522319,-3.84421723301392,27.3096148237694));
#68054=CARTESIAN_POINT('Ctrl Pts',(3.99207382756366,-0.898399846513567,
27.5085010737694));
#68055=CARTESIAN_POINT('Ctrl Pts',(2.91373355526439,2.87296580172139,27.7073873237694));
#68056=CARTESIAN_POINT('Ctrl Pts',(-0.842064511625181,4.00433553629013,
27.9062735737694));
#68057=CARTESIAN_POINT('Ctrl Pts',(-3.82408139796542,1.4560828241104,28.1051598237694));
#68058=CARTESIAN_POINT('Ctrl Pts',(-3.29211309934206,-2.43017840293152,
28.3040460737694));
#68059=CARTESIAN_POINT('Ctrl Pts',(0.265009597006007,-4.08332531675215,
28.5029323237694));
#68060=CARTESIAN_POINT('Ctrl Pts',(3.57861242522373,-1.98426531466151,28.7018185737694));
#68061=CARTESIAN_POINT('Ctrl Pts',(3.60379386898736,1.9381551740724,28.9007048237694));
#68062=CARTESIAN_POINT('Ctrl Pts',(0.317414457372265,4.07958622793851,29.0995910737694));
#68063=CARTESIAN_POINT('Ctrl Pts',(-3.26064015270821,2.47224625057484,29.2984773237694));
#68064=CARTESIAN_POINT('Ctrl Pts',(-3.84246115850137,-1.40686458991001,
29.4973635737694));
#68065=CARTESIAN_POINT('Ctrl Pts',(-0.893407640557818,-3.99319402442797,
29.6962498237694));
#68066=CARTESIAN_POINT('Ctrl Pts',(2.87660675304174,-2.9101390546311,29.8951360737694));
#68067=CARTESIAN_POINT('Ctrl Pts',(4.00327952778012,0.847070688544426,30.0940223237694));
#68068=CARTESIAN_POINT('Ctrl Pts',(1.45130023214889,3.82589902703912,30.2929085737694));
#68069=CARTESIAN_POINT('Ctrl Pts',(-2.43429280858163,3.28907194372852,30.4917948237694));
#68070=CARTESIAN_POINT('Ctrl Pts',(-4.08299076915769,-0.270114990157072,
30.6906810737694));
#68071=CARTESIAN_POINT('Ctrl Pts',(-1.97978923282535,-3.58109066103098,
30.8895673237694));
#68072=CARTESIAN_POINT('Ctrl Pts',(1.94265967549026,-3.60136767272636,31.0884535737694));
#68073=CARTESIAN_POINT('Ctrl Pts',(4.07997991925103,-0.312313284127758,
31.2873398237694));
#68074=CARTESIAN_POINT('Ctrl Pts',(2.46816736504766,3.26372878576757,31.4862260737694));
#68075=CARTESIAN_POINT('Ctrl Pts',(-1.41166792512641,3.84069907674427,31.6851123237694));
#68076=CARTESIAN_POINT('Ctrl Pts',(-3.9943079783942,0.888414037862129,31.8839985737694));
#68077=CARTESIAN_POINT('Ctrl Pts',(-2.90654000433118,-2.88024320711916,
32.0828848237694));
#68078=CARTESIAN_POINT('Ctrl Pts',(0.852075541166488,-4.00221726060484,
32.2817710737694));
#68079=CARTESIAN_POINT('Ctrl Pts',(3.82771067476094,-1.44651537124626,32.4806573237694));
#68080=CARTESIAN_POINT('Ctrl Pts',(3.28602564603094,2.43840340849451,32.6795435737694));
#68081=CARTESIAN_POINT('Ctrl Pts',(-0.275219961015347,4.08264983828088,
32.8784298237694));
#68082=CARTESIAN_POINT('Ctrl Pts',(-3.58356329821457,1.97531005581222,33.0773160737694));
#68083=CARTESIAN_POINT('Ctrl Pts',(-3.59893584614564,-1.94716113977428,
33.2762023237694));
#68084=CARTESIAN_POINT('Ctrl Pts',(-0.307211622611714,-4.08036723200399,
33.4750885737694));
#68085=CARTESIAN_POINT('Ctrl Pts',(3.26681231635263,-2.46408462079069,33.6739748237694));
#68086=CARTESIAN_POINT('Ctrl Pts',(3.83893099051835,1.41646905329624,33.8728610737694));
#68087=CARTESIAN_POINT('Ctrl Pts',(0.883419046193318,3.99541568784834,34.0717473237694));
#68088=CARTESIAN_POINT('Ctrl Pts',(-2.88387515819149,2.90293640974734,34.2706335737694));
#68089=CARTESIAN_POINT('Ctrl Pts',(-4.00114873657231,-0.857079061199814,
34.4695198237694));
#68090=CARTESIAN_POINT('Ctrl Pts',(-1.44172824860138,-3.82951633919216,
34.6684060737694));
#68091=CARTESIAN_POINT('Ctrl Pts',(2.44251019570497,-3.28297420930239,34.8672923237694));
#68092=CARTESIAN_POINT('Ctrl Pts',(4.08230252568531,0.280324498329562,35.0661785737694));
#68093=CARTESIAN_POINT('Ctrl Pts',(1.97082778865322,3.58603033916501,35.2650648237694));
#68094=CARTESIAN_POINT('Ctrl Pts',(-1.95165955611527,3.59649838107857,35.4639510737694));
#68095=CARTESIAN_POINT('Ctrl Pts',(-4.08074817280747,0.302109503696352,
35.6628373237694));
#68096=CARTESIAN_POINT('Ctrl Pts',(-2.45999801038286,-3.26989078344478,
35.8617235737694));
#68097=CARTESIAN_POINT('Ctrl Pts',(1.42126794050536,-3.83715681879127,36.0606098237695));
#68098=CARTESIAN_POINT('Ctrl Pts',(3.99651720157898,-0.878422833668996,
36.2594960737694));
#68099=CARTESIAN_POINT('Ctrl Pts',(2.89932817986464,2.88750290726155,36.4583823237694));
#68100=CARTESIAN_POINT('Ctrl Pts',(-0.862081055926817,4.00007337065221,
36.6572685737694));
#68101=CARTESIAN_POINT('Ctrl Pts',(-3.83131637122645,1.43693999409573,36.8561548237694));
#68102=CARTESIAN_POINT('Ctrl Pts',(-3.27991696163009,-2.44661531101263,
37.0550410737694));
#68103=CARTESIAN_POINT('Ctrl Pts',(0.285427299579139,-4.08194472413982,
37.2539273237694));
#68104=CARTESIAN_POINT('Ctrl Pts',(3.58849425656653,-1.96635029679954,37.4528135737694));
#68105=CARTESIAN_POINT('Ctrl Pts',(3.59405054354887,1.95616995120416,37.6516998237694));
#68106=CARTESIAN_POINT('Ctrl Pts',(0.297015999058931,4.08109398054869,37.8505860737695));
#68107=CARTESIAN_POINT('Ctrl Pts',(-3.27298152169835,2.45596256107144,38.0494723237694));
#68108=CARTESIAN_POINT('Ctrl Pts',(-3.83534339271433,-1.42616983857172,
38.2483585737694));
#68109=CARTESIAN_POINT('Ctrl Pts',(-0.873488868281231,-3.99741114283678,
38.4472448237694));
#68110=CARTESIAN_POINT('Ctrl Pts',(2.89124785821669,-2.89610062663618,38.6461310737694));
#68111=CARTESIAN_POINT('Ctrl Pts',(3.99875884595704,0.86781919426473,38.8450173237695));
#68112=CARTESIAN_POINT('Ctrl Pts',(1.43259554006624,3.8316945266069,39.0439035737694));
#68113=CARTESIAN_POINT('Ctrl Pts',(-2.45157425821743,3.27960818739581,39.2427898237695));
#68114=CARTESIAN_POINT('Ctrl Pts',(-4.07990016466532,-0.296198169273691,
39.4416760737694));
#68115=CARTESIAN_POINT('Ctrl Pts',(-2.67033828334988,-2.48323567835706,
39.5742669071028));
#68116=CARTESIAN_POINT('Ctrl Pts',(-1.65864454744381,-3.03595759443951,
39.6405623237694));
#68117=CARTESIAN_POINT('Ctrl Pts',(1.87158653173891,-2.62360084935066,0.));
#68118=CARTESIAN_POINT('Ctrl Pts',(2.74586769747962,-1.99991876175022,0.0662954166666667));
#68119=CARTESIAN_POINT('Ctrl Pts',(3.80646220378775,0.179585068045613,0.19888625));
#68120=CARTESIAN_POINT('Ctrl Pts',(1.90290546061669,3.30586713103499,0.3977725));
#68121=CARTESIAN_POINT('Ctrl Pts',(-1.75096977450869,3.38471360215616,0.596658750000001));
#68122=CARTESIAN_POINT('Ctrl Pts',(-3.79495803328573,0.358132283227411,
0.795545000000001));
#68123=CARTESIAN_POINT('Ctrl Pts',(-2.35219597055587,-3.00003386437442,
0.994431250000001));
#68124=CARTESIAN_POINT('Ctrl Pts',(1.25226897486165,-3.60013934158935,1.1933175));
#68125=CARTESIAN_POINT('Ctrl Pts',(3.70588259587967,-0.892721732175661,
1.39220375));
#68126=CARTESIAN_POINT('Ctrl Pts',(2.75419264545516,2.63538166557444,1.59109));
#68127=CARTESIAN_POINT('Ctrl Pts',(-0.728386757290071,3.7416218310534,1.78997625));
#68128=CARTESIAN_POINT('Ctrl Pts',(-3.54162609141209,1.40974675245884,1.9888625));
#68129=CARTESIAN_POINT('Ctrl Pts',(-3.10044079376427,-2.21760890985371,
2.18774875));
#68130=CARTESIAN_POINT('Ctrl Pts',(0.189774422820439,-3.8071558930084,2.386635));
#68131=CARTESIAN_POINT('Ctrl Pts',(3.30560145857767,-1.89828456209197,2.58552125000001));
#68132=CARTESIAN_POINT('Ctrl Pts',(3.38388089250329,1.75494596051086,2.7844075));
#68133=CARTESIAN_POINT('Ctrl Pts',(0.35267889993612,3.79553596959835,2.98329375));
#68134=CARTESIAN_POINT('Ctrl Pts',(-3.0026027498368,2.34837344226508,3.18218));
#68135=CARTESIAN_POINT('Ctrl Pts',(-3.59876404414062,-1.25673306783944,
3.38106625000001));
#68136=CARTESIAN_POINT('Ctrl Pts',(-0.887986334554333,-3.70701493094446,
3.5799525));
#68137=CARTESIAN_POINT('Ctrl Pts',(2.63877050663273,-2.75088539460193,3.77883875000001));
#68138=CARTESIAN_POINT('Ctrl Pts',(3.74073577194275,0.7330593426781,3.977725));
#68139=CARTESIAN_POINT('Ctrl Pts',(1.40530293513768,3.54338872054109,4.17661125000001));
#68140=CARTESIAN_POINT('Ctrl Pts',(-2.22147628035442,3.09766415542848,4.37549750000001));
#68141=CARTESIAN_POINT('Ctrl Pts',(-3.80691957483225,-0.194533823322909,
4.57438375000001));
#68142=CARTESIAN_POINT('Ctrl Pts',(-1.89414784662335,-3.30797278933611,
4.77327));
#68143=CARTESIAN_POINT('Ctrl Pts',(1.75917455880395,-3.38168374168425,4.97215625000001));
#68144=CARTESIAN_POINT('Ctrl Pts',(3.79597453913422,-0.347932968357942,
5.17104250000001));
#68145=CARTESIAN_POINT('Ctrl Pts',(2.34461699717418,3.0055367551961,5.36992875000001));
#68146=CARTESIAN_POINT('Ctrl Pts',(-1.26123165898331,3.59718984140266,5.56881500000001));
#68147=CARTESIAN_POINT('Ctrl Pts',(-3.70812241050024,0.883350576279402,
5.76770125000001));
#68148=CARTESIAN_POINT('Ctrl Pts',(-2.74758380613951,-2.64220803115844,
5.96658750000001));
#68149=CARTESIAN_POINT('Ctrl Pts',(0.737735989926837,-3.73981626035058,
6.16547375000001));
#68150=CARTESIAN_POINT('Ctrl Pts',(3.5451430877039,-1.4008713501182,6.36436000000001));
#68151=CARTESIAN_POINT('Ctrl Pts',(3.09488409724894,2.22534772034816,6.56324625000001));
#68152=CARTESIAN_POINT('Ctrl Pts',(-0.19929366352457,3.8066733623451,6.76213250000001));
#68153=CARTESIAN_POINT('Ctrl Pts',(-3.31033855964498,1.89001023076976,6.96101875000001));
#68154=CARTESIAN_POINT('Ctrl Pts',(-3.3794815072351,-1.76340148410472,7.15990500000001));
#68155=CARTESIAN_POINT('Ctrl Pts',(-0.343186386587714,-3.79640661098804,
7.35879125000001));
#68156=CARTESIAN_POINT('Ctrl Pts',(3.00846600621214,-2.34085718089664,7.55767750000001));
#68157=CARTESIAN_POINT('Ctrl Pts',(3.5956100439019,1.26572843220077,7.75656375000002));
#68158=CARTESIAN_POINT('Ctrl Pts',(0.878713421813992,3.70922401240668,7.95545000000001));
#68159=CARTESIAN_POINT('Ctrl Pts',(-2.6456414169651,2.74427796418817,8.15433625000002));
#68160=CARTESIAN_POINT('Ctrl Pts',(-3.73889090613327,-0.742411505786354,
8.35322250000001));
#68161=CARTESIAN_POINT('Ctrl Pts',(-1.39643757283078,-3.54689190095731,
8.55210875000002));
#68162=CARTESIAN_POINT('Ctrl Pts',(2.22921568013466,-3.09209920657986,8.75099500000001));
#68163=CARTESIAN_POINT('Ctrl Pts',(3.80642119915558,0.204053195292361,8.94988125000001));
#68164=CARTESIAN_POINT('Ctrl Pts',(1.88586965979368,3.3126991529808,9.14876750000002));
#68165=CARTESIAN_POINT('Ctrl Pts',(-1.76762565236893,3.37727399021419,9.34765375000001));
#68166=CARTESIAN_POINT('Ctrl Pts',(-3.79683274768274,0.338439267836879,
9.54654000000001));
#68167=CARTESIAN_POINT('Ctrl Pts',(-2.33709370491482,-3.01139055360436,
9.74542625000002));
#68168=CARTESIAN_POINT('Ctrl Pts',(1.27022322657475,-3.59402462520223,9.94431250000001));
#68169=CARTESIAN_POINT('Ctrl Pts',(3.71031981538147,-0.874074893517518,
10.14319875));
#68170=CARTESIAN_POINT('Ctrl Pts',(2.74096783186856,2.64907066658324,10.342085));
#68171=CARTESIAN_POINT('Ctrl Pts',(-0.747085860967871,3.73795970660893,
10.54097125));
#68172=CARTESIAN_POINT('Ctrl Pts',(-3.54863516905622,1.39200161236521,10.7398575));
#68173=CARTESIAN_POINT('Ctrl Pts',(-3.08930948176955,-2.23308015479489,
10.93874375));
#68174=CARTESIAN_POINT('Ctrl Pts',(0.208812408046019,-3.80616308506823,
11.13763));
#68175=CARTESIAN_POINT('Ctrl Pts',(3.31505456729397,-1.88172614047672,11.33651625));
#68176=CARTESIAN_POINT('Ctrl Pts',(3.37506119321498,1.77184705715372,11.5354025));
#68177=CARTESIAN_POINT('Ctrl Pts',(0.333691619975345,3.79725294846791,11.73428875));
#68178=CARTESIAN_POINT('Ctrl Pts',(-3.01431039303498,2.33332657515646,11.933175));
#68179=CARTESIAN_POINT('Ctrl Pts',(-3.59243358765975,-1.27471603510118,
12.13206125));
#68180=CARTESIAN_POINT('Ctrl Pts',(-0.869434998705811,-3.71140981769939,
12.3309475));
#68181=CARTESIAN_POINT('Ctrl Pts',(2.65249577468504,-2.73765341436203,12.52983375));
#68182=CARTESIAN_POINT('Ctrl Pts',(3.73702266321591,0.751759048166815,12.72872));
#68183=CARTESIAN_POINT('Ctrl Pts',(1.38756347566574,3.55037288927353,12.92760625));
#68184=CARTESIAN_POINT('Ctrl Pts',(-2.23694113829198,3.08651492718033,13.1264925));
#68185=CARTESIAN_POINT('Ctrl Pts',(-3.80589902048407,-0.2135712943456,13.32537875));
#68186=CARTESIAN_POINT('Ctrl Pts',(-1.87757967929805,-3.31740479890186,
13.524265));
#68187=CARTESIAN_POINT('Ctrl Pts',(1.77606569186011,-3.37284311969702,13.72315125));
#68188=CARTESIAN_POINT('Ctrl Pts',(3.79766721268626,-0.32894345042547,13.9220375));
#68189=CARTESIAN_POINT('Ctrl Pts',(2.32955579751124,3.01722551993911,14.12092375));
#68190=CARTESIAN_POINT('Ctrl Pts',(-1.2792068507562,3.59083693376187,14.31981));
#68191=CARTESIAN_POINT('Ctrl Pts',(-3.71249401765632,0.864793744632787,
14.51869625));
#68192=CARTESIAN_POINT('Ctrl Pts',(-2.73433471685024,-2.65591673591578,
14.7175825));
#68193=CARTESIAN_POINT('Ctrl Pts',(0.756431060077252,-3.73607977741916,
14.91646875));
#68194=CARTESIAN_POINT('Ctrl Pts',(3.55210505889249,-1.38312316967087,15.115355));
#68195=CARTESIAN_POINT('Ctrl Pts',(3.08371554718117,2.24079862458972,15.31424125));
#68196=CARTESIAN_POINT('Ctrl Pts',(-0.21832984675111,3.80562900581595,15.5131275));
#68197=CARTESIAN_POINT('Ctrl Pts',(-3.31974984413011,1.8734302827402,15.71201375));
#68198=CARTESIAN_POINT('Ctrl Pts',(-3.37061977312804,-1.78028154989269,
15.9109));
#68199=CARTESIAN_POINT('Ctrl Pts',(-0.324194766610495,-3.79807553969012,
16.10978625));
#68200=CARTESIAN_POINT('Ctrl Pts',(3.02013592975928,-2.32578137787433,16.3086725));
#68201=CARTESIAN_POINT('Ctrl Pts',(3.58923466600481,1.2836956665189,16.5075587500001));
#68202=CARTESIAN_POINT('Ctrl Pts',(0.86015113855453,3.71357241355724,16.706445));
#68203=CARTESIAN_POINT('Ctrl Pts',(-2.65933354492717,2.73101174452164,16.9053312500001));
#68204=CARTESIAN_POINT('Ctrl Pts',(-3.73513105069278,-0.761101889394991,
17.1042175));
#68205=CARTESIAN_POINT('Ctrl Pts',(-1.37868070132254,-3.55383167520506,
17.30310375));
#68206=CARTESIAN_POINT('Ctrl Pts',(2.24465260765735,-3.08091134614859,17.50199));
#68207=CARTESIAN_POINT('Ctrl Pts',(3.80535304148599,0.223088057823076,17.70087625));
#68208=CARTESIAN_POINT('Ctrl Pts',(1.8692779572903,3.32208969931257,17.8997625000001));
#68209=CARTESIAN_POINT('Ctrl Pts',(-1.78449462466053,3.36839115698396,18.09864875));
#68210=CARTESIAN_POINT('Ctrl Pts',(-3.79847792884113,0.319445575954385,
18.297535));
#68211=CARTESIAN_POINT('Ctrl Pts',(-2.32200332214661,-3.02304161794542,
18.49642125));
#68212=CARTESIAN_POINT('Ctrl Pts',(1.28818247537154,-3.58762678689348,18.6953075));
#68213=CARTESIAN_POINT('Ctrl Pts',(3.71464500371619,-0.855507187729257,
18.89419375));
#68214=CARTESIAN_POINT('Ctrl Pts',(2.72768450257131,2.6627461963774,19.09308));
#68215=CARTESIAN_POINT('Ctrl Pts',(-0.76577152881775,3.73417648452,19.29196625));
#68216=CARTESIAN_POINT('Ctrl Pts',(-3.55555273551189,1.37423607756599,19.4908525));
#68217=CARTESIAN_POINT('Ctrl Pts',(-3.0781023284666,-2.24850308146965,19.68973875));
#68218=CARTESIAN_POINT('Ctrl Pts',(0.227845920122608,-3.80507112792566,
19.8886250000001));
#68219=CARTESIAN_POINT('Ctrl Pts',(3.32442436079109,-1.86512270943999,20.08751125));
#68220=CARTESIAN_POINT('Ctrl Pts',(3.366157274749,1.78870490957689,20.2863975000001));
#68221=CARTESIAN_POINT('Ctrl Pts',(0.314695885881992,3.7988743795102,20.48528375));
#68222=CARTESIAN_POINT('Ctrl Pts',(-3.02594257995482,2.31822163623464,20.6841700000001));
#68223=CARTESIAN_POINT('Ctrl Pts',(-3.58601329894164,-1.29266727029954,
20.88305625));
#68224=CARTESIAN_POINT('Ctrl Pts',(-0.850861899417176,-3.7157117864563,
21.0819425));
#68225=CARTESIAN_POINT('Ctrl Pts',(2.6661546849312,-2.724352996201,21.28082875));
#68226=CARTESIAN_POINT('Ctrl Pts',(3.73321608039316,0.770439971045078,21.479715));
#68227=CARTESIAN_POINT('Ctrl Pts',(1.36978930534994,3.55726823712227,21.67860125));
#68228=CARTESIAN_POINT('Ctrl Pts',(-2.25235004000682,3.07528849852681,21.8774875));
#68229=CARTESIAN_POINT('Ctrl Pts',(-3.80478326557569,-0.232603426211332,
22.07637375));
#68230=CARTESIAN_POINT('Ctrl Pts',(-1.86096454568552,-3.32675382491574,
22.27526));
#68231=CARTESIAN_POINT('Ctrl Pts',(1.79291239805955,-3.36391812991553,22.47414625));
#68232=CARTESIAN_POINT('Ctrl Pts',(3.79926489107751,-0.309945703818892,
22.6730325));
#68233=CARTESIAN_POINT('Ctrl Pts',(2.31443632605062,3.02883881125214,22.87191875));
#68234=CARTESIAN_POINT('Ctrl Pts',(-1.29715004429138,3.58439420467181,23.070805));
#68235=CARTESIAN_POINT('Ctrl Pts',(-3.71677276010977,0.846215280880731,
23.26969125));
#68236=CARTESIAN_POINT('Ctrl Pts',(-2.72101723061917,-2.6695590052598,23.4685775000001));
#68237=CARTESIAN_POINT('Ctrl Pts',(0.775107208778419,-3.73224983981374,
23.66746375));
#68238=CARTESIAN_POINT('Ctrl Pts',(3.55897817735421,-1.36534039162637,23.8663500000001));
#68239=CARTESIAN_POINT('Ctrl Pts',(3.07246986072833,2.25619347725455,24.06523625));
#68240=CARTESIAN_POINT('Ctrl Pts',(-0.237360568651399,3.80448945488611,
24.2641225));
#68241=CARTESIAN_POINT('Ctrl Pts',(-3.32907808804463,1.85680347252778,24.46300875));
#68242=CARTESIAN_POINT('Ctrl Pts',(-3.36167372598423,-1.79711708353053,
24.6618950000001));
#68243=CARTESIAN_POINT('Ctrl Pts',(-0.305195037191488,-3.79964946293255,
24.86078125));
#68244=CARTESIAN_POINT('Ctrl Pts',(3.03173030730948,-2.3106473975125,25.0596675000001));
#68245=CARTESIAN_POINT('Ctrl Pts',(3.58276950661523,1.30163079033885,25.25855375));
#68246=CARTESIAN_POINT('Ctrl Pts',(0.841567339384293,3.7178279230179,25.4574400000001));
#68247=CARTESIAN_POINT('Ctrl Pts',(-2.67295915204091,2.71767721104084,25.65632625));
#68248=CARTESIAN_POINT('Ctrl Pts',(-3.73127776429237,-0.77977323472104,
25.8552125000001));
#68249=CARTESIAN_POINT('Ctrl Pts',(-1.36088934335066,-3.56068255353444,
26.05409875));
#68250=CARTESIAN_POINT('Ctrl Pts',(2.26003338720418,-3.06964641947774,26.252985));
#68251=CARTESIAN_POINT('Ctrl Pts',(3.80418969631625,0.242117340005657,26.4518712500001));
#68252=CARTESIAN_POINT('Ctrl Pts',(1.852639496472,3.33139714654406,26.6507575));
#68253=CARTESIAN_POINT('Ctrl Pts',(-1.80131895941629,3.35942406646398,26.8496437500001));
#68254=CARTESIAN_POINT('Ctrl Pts',(-3.8000280944741,0.300443893426859,27.0485300000001));
#68255=CARTESIAN_POINT('Ctrl Pts',(-2.3068548565438,-3.03461706360628,27.24741625));
#68256=CARTESIAN_POINT('Ctrl Pts',(1.30610950143672,-3.58113920731194,27.4463025));
#68257=CARTESIAN_POINT('Ctrl Pts',(3.71887727353106,-0.836918082194489,
27.6451887500001));
#68258=CARTESIAN_POINT('Ctrl Pts',(2.71433294268781,2.67635511995881,27.8440750000001));
#68259=CARTESIAN_POINT('Ctrl Pts',(-0.784438041578219,3.73029985534876,
28.04296125));
#68260=CARTESIAN_POINT('Ctrl Pts',(-3.56238136299841,1.35643616748143,28.2418475));
#68261=CARTESIAN_POINT('Ctrl Pts',(-3.06681817918912,-2.2638697638524,28.44073375));
#68262=CARTESIAN_POINT('Ctrl Pts',(0.246873732837376,-3.80388399033473,
28.63962));
#68263=CARTESIAN_POINT('Ctrl Pts',(3.33371099678845,-1.8484726240282,28.8385062500001));
#68264=CARTESIAN_POINT('Ctrl Pts',(3.35716915487184,1.80551801914775,29.0373925));
#68265=CARTESIAN_POINT('Ctrl Pts',(0.295692279952789,3.80040078511023,29.23627875));
#68266=CARTESIAN_POINT('Ctrl Pts',(-3.0374990756295,2.30305870907363,29.435165));
#68267=CARTESIAN_POINT('Ctrl Pts',(-3.5795033093107,-1.31058617058311,29.6340512500001));
#68268=CARTESIAN_POINT('Ctrl Pts',(-0.832267516579828,-3.71992081000873,
29.8329375));
#68269=CARTESIAN_POINT('Ctrl Pts',(2.67974690370432,-2.71098443078842,30.03182375));
#68270=CARTESIAN_POINT('Ctrl Pts',(3.72931611451176,0.789101622057042,30.2307100000001));
#68271=CARTESIAN_POINT('Ctrl Pts',(1.35198087098079,3.56407460309012,30.42959625));
#68272=CARTESIAN_POINT('Ctrl Pts',(-2.26770260120141,3.06398514428421,30.6284825000001));
#68273=CARTESIAN_POINT('Ctrl Pts',(-3.80357233741956,-0.251629739710501,
30.82736875));
#68274=CARTESIAN_POINT('Ctrl Pts',(-1.84430286171068,-3.33601963516042,
31.0262550000001));
#68275=CARTESIAN_POINT('Ctrl Pts',(1.80971425616015,-3.35490899473305,31.22514125));
#68276=CARTESIAN_POINT('Ctrl Pts',(3.8007675342582,-0.290940204197991,31.4240275000001));
#68277=CARTESIAN_POINT('Ctrl Pts',(2.29925896103701,3.04037633887334,31.62291375));
#68278=CARTESIAN_POINT('Ctrl Pts',(-1.31506079077929,3.57786181516915,31.8218000000001));
#68279=CARTESIAN_POINT('Ctrl Pts',(-3.72095853081945,0.827615649810777,
32.02068625));
#68280=CARTESIAN_POINT('Ctrl Pts',(-2.70763168057768,-2.6831344979746,32.2195725000001));
#68281=CARTESIAN_POINT('Ctrl Pts',(0.793763968866624,-3.72832654331965,
32.41845875));
#68282=CARTESIAN_POINT('Ctrl Pts',(3.56576227116223,-1.34752346081344,32.6173450000001));
#68283=CARTESIAN_POINT('Ctrl Pts',(3.06114731919247,2.27153189325784,32.81623125));
#68284=CARTESIAN_POINT('Ctrl Pts',(-0.256385353190344,3.80325473806034,
33.0151175000001));
#68285=CARTESIAN_POINT('Ctrl Pts',(-3.33832305804911,1.84013021603382,33.21400375));
#68286=CARTESIAN_POINT('Ctrl Pts',(-3.35264358958403,-1.81390766388419,
33.4128900000001));
#68287=CARTESIAN_POINT('Ctrl Pts',(-0.286187673586392,-3.80112834136171,
33.61177625));
#68288=CARTESIAN_POINT('Ctrl Pts',(3.0432488488294,-2.29545561834177,33.8106625000001));
#68289=CARTESIAN_POINT('Ctrl Pts',(3.57621472747308,1.31953335496755,34.00954875));
#68290=CARTESIAN_POINT('Ctrl Pts',(0.822962489122625,3.72199043445967,34.208435));
#68291=CARTESIAN_POINT('Ctrl Pts',(-2.68651789740178,2.70427469706992,34.4073212500001));
#68292=CARTESIAN_POINT('Ctrl Pts',(-3.72733114345669,-0.798425074282841,
34.6062075));
#68293=CARTESIAN_POINT('Ctrl Pts',(-1.34306394368559,-3.56744436540872,
34.8050937500001));
#68294=CARTESIAN_POINT('Ctrl Pts',(2.27535763353318,-3.05830470675803,35.00398));
#68295=CARTESIAN_POINT('Ctrl Pts',(3.80293119371364,0.261140562795601,35.2028662500001));
#68296=CARTESIAN_POINT('Ctrl Pts',(1.83595469168445,3.34062126768144,35.4017525000001));
#68297=CARTESIAN_POINT('Ctrl Pts',(-1.81809823225042,3.35037293181705,35.6006387500001));
#68298=CARTESIAN_POINT('Ctrl Pts',(-3.80148321257848,0.281434716877477,
35.7995250000001));
#68299=CARTESIAN_POINT('Ctrl Pts',(-2.29164867407474,-3.0461166418114,35.9984112500001));
#68300=CARTESIAN_POINT('Ctrl Pts',(1.32400383155469,-3.57456197073556,36.1972975000001));
#68301=CARTESIAN_POINT('Ctrl Pts',(3.72301656637914,-0.818308191127896,
36.39618375));
#68302=CARTESIAN_POINT('Ctrl Pts',(2.7009133954788,2.68989738238965,36.5950700000001));
#68303=CARTESIAN_POINT('Ctrl Pts',(-0.803084758776685,3.72632936992902,
36.79395625));
#68304=CARTESIAN_POINT('Ctrl Pts',(-3.56912121270992,1.33860337215557,36.9928425000001));
#68305=CARTESIAN_POINT('Ctrl Pts',(-3.0554566810503,-2.27918181632194,37.19172875));
#68306=CARTESIAN_POINT('Ctrl Pts',(0.265894155143361,-3.80259787822564,
37.3906150000001));
#68307=CARTESIAN_POINT('Ctrl Pts',(3.34291656752411,-1.83178361584359,37.58950125));
#68308=CARTESIAN_POINT('Ctrl Pts',(3.34809261142426,1.82229995960197,37.7883875000001));
#68309=CARTESIAN_POINT('Ctrl Pts',(0.276689784930593,3.80180535505515,37.98727375));
#68310=CARTESIAN_POINT('Ctrl Pts',(-3.04899586618102,2.28788938970751,38.1861600000001));
#68311=CARTESIAN_POINT('Ctrl Pts',(-3.57287264600958,-1.32857026947732,
38.3850462500001));
#68312=CARTESIAN_POINT('Ctrl Pts',(-0.813711880402819,-3.723849330995,38.5839325000001));
#68313=CARTESIAN_POINT('Ctrl Pts',(2.6933860485815,-2.69790671903219,38.7828187500001));
#68314=CARTESIAN_POINT('Ctrl Pts',(3.72510480439603,0.808430209081211,38.9817050000001));
#68315=CARTESIAN_POINT('Ctrl Pts',(1.33455622972935,3.56947348912338,39.1805912500001));
#68316=CARTESIAN_POINT('Ctrl Pts',(-2.28380139923979,3.05516903770198,39.3794775000001));
#68317=CARTESIAN_POINT('Ctrl Pts',(-3.80069323765723,-0.275927923117959,
39.5783637500001));
#68318=CARTESIAN_POINT('Ctrl Pts',(-2.48759436411792,-2.31329607816883,
39.7109545833334));
#68319=CARTESIAN_POINT('Ctrl Pts',(-1.54513563095092,-2.82819261092061,
39.7772500000001));
#68320=CARTESIAN_POINT('',(1.87158653173903,-2.62360084935058,0.));
#68321=CARTESIAN_POINT('Ctrl Pts',(1.87158653173891,-2.62360084935066,0.));
#68322=CARTESIAN_POINT('Ctrl Pts',(2.74586769747962,-1.99991876175022,0.0662954166666667));
#68323=CARTESIAN_POINT('Ctrl Pts',(3.80646220378775,0.179585068045613,0.19888625));
#68324=CARTESIAN_POINT('Ctrl Pts',(1.90290546061669,3.30586713103499,0.3977725));
#68325=CARTESIAN_POINT('Ctrl Pts',(-1.75096977450869,3.38471360215616,0.596658750000001));
#68326=CARTESIAN_POINT('Ctrl Pts',(-3.17762645222587,1.27222962346284,0.735476766908961));
#68327=CARTESIAN_POINT('Ctrl Pts',(-3.22753027149843,0.102472337925121,
0.807999367151255));
#68328=CARTESIAN_POINT('Ctrl Pts',(-3.22687103957968,0.00196979923060637,
0.814226550726882));
#68329=CARTESIAN_POINT('Ctrl Pts',(1.75279216821278,3.52834843496255,-3.81639164714898E-17));
#68330=CARTESIAN_POINT('Ctrl Pts',(1.82191691638292,3.48650815550269,-1.21318433738122E-17));
#68331=CARTESIAN_POINT('Ctrl Pts',(1.88956902721166,3.44243155654609,4.31313297381532E-16));
#68332=CARTESIAN_POINT('Ctrl Pts',(1.95562633572894,3.39611167515613,3.72965547335014E-16));
#68333=CARTESIAN_POINT('Ctrl Pts',(2.055090558922,3.3263666140227,2.9513505280704E-16));
#68334=CARTESIAN_POINT('Ctrl Pts',(2.15094102353959,3.25153686259763,1.54341957985257E-16));
#68335=CARTESIAN_POINT('Ctrl Pts',(2.24299353637915,3.17203260947581,3.98986399474666E-16));
#68336=CARTESIAN_POINT('Ctrl Pts',(2.29704328498386,3.12535072365125,5.42632348424371E-16));
#68337=CARTESIAN_POINT('Ctrl Pts',(2.34978291432432,3.07705656763921,-1.94225233284913E-16));
#68338=CARTESIAN_POINT('Ctrl Pts',(2.40116830603661,3.02722856075797,-2.77555756156289E-16));
#68339=CARTESIAN_POINT('Ctrl Pts',(2.44043366591505,2.98915325263982,-3.41231498626496E-16));
#68340=CARTESIAN_POINT('Ctrl Pts',(2.47890818299915,2.95018225395627,-3.92682644174071E-16));
#68341=CARTESIAN_POINT('Ctrl Pts',(2.51657001727904,2.91034961927201,-4.16333634234434E-16));
#68342=CARTESIAN_POINT('Ctrl Pts',(2.53154412234642,2.89451241781124,-4.25737117014365E-16));
#68343=CARTESIAN_POINT('Ctrl Pts',(2.54639039078509,2.8785381668224,-5.91306110935837E-16));
#68344=CARTESIAN_POINT('Ctrl Pts',(2.56109596980966,2.86244180656298,-5.82867087928207E-16));
#68345=CARTESIAN_POINT('Ctrl Pts',(2.64412181623707,2.77156378450707,-5.35221427253556E-16));
#68346=CARTESIAN_POINT('Ctrl Pts',(2.72275487583107,2.67670423124671,-4.57210367042411E-16));
#68347=CARTESIAN_POINT('Ctrl Pts',(2.79680001326638,2.57828733731509,-3.46944695195361E-16));
#68348=CARTESIAN_POINT('Ctrl Pts',(2.86158950852228,2.49217255512492,-2.50462232329193E-16));
#68349=CARTESIAN_POINT('Ctrl Pts',(2.92286585232168,2.40333323665222,-1.40877212777496E-16));
#68350=CARTESIAN_POINT('Ctrl Pts',(2.98046656758873,2.31203951151562,-3.46944695195361E-16));
#68351=CARTESIAN_POINT('Ctrl Pts',(3.00570269469217,2.27204174342171,-4.37227344535292E-16));
#68352=CARTESIAN_POINT('Ctrl Pts',(3.03023288080839,2.23157272966444,1.66108317954742E-16));
#68353=CARTESIAN_POINT('Ctrl Pts',(3.05404152003192,2.19065478651688,1.94289029309402E-16));
#68354=CARTESIAN_POINT('Ctrl Pts',(3.06875072432013,2.16537529115556,2.11699341440679E-16));
#68355=CARTESIAN_POINT('Ctrl Pts',(3.08318449857401,2.13992444111478,-1.8109813009777E-16));
#68356=CARTESIAN_POINT('Ctrl Pts',(3.09733892594653,2.11430748080091,-2.22044604925031E-16));
#68357=CARTESIAN_POINT('Ctrl Pts',(3.10819488190479,2.0946601587558,-2.53449134099686E-16));
#68358=CARTESIAN_POINT('Ctrl Pts',(3.11888791824441,2.07491228675552,3.6193208763267E-17));
#68359=CARTESIAN_POINT('Ctrl Pts',(3.12940472621869,2.05508840908837,4.16333634234434E-17));
#68360=CARTESIAN_POINT('Ctrl Pts',(3.18512455295535,1.95005815356189,7.04562225862981E-17));
#68361=CARTESIAN_POINT('Ctrl Pts',(3.23597068553496,1.84277396746319,-5.60205083633985E-16));
#68362=CARTESIAN_POINT('Ctrl Pts',(3.28176671572766,1.73361210949876,-3.88578058618805E-16));
#68363=CARTESIAN_POINT('Ctrl Pts',(3.32722141767324,1.62526385973302,-2.18230208924308E-16));
#68364=CARTESIAN_POINT('Ctrl Pts',(3.36770124739318,1.5150649596808,4.5624040228757E-16));
#68365=CARTESIAN_POINT('Ctrl Pts',(3.40298410185854,1.40337142666729,4.71844785465692E-16));
#68366=CARTESIAN_POINT('Ctrl Pts',(3.43722346004176,1.29498124844761,4.8698766641906E-16));
#68367=CARTESIAN_POINT('Ctrl Pts',(3.46656871523125,1.185182805433,1.09754022917521E-16));
#68368=CARTESIAN_POINT('Ctrl Pts',(3.49076850390209,1.0743018781408,1.38777878078145E-16));
#68369=CARTESIAN_POINT('Ctrl Pts',(3.50694458616008,1.00018474327172,1.58178554460402E-16));
#68370=CARTESIAN_POINT('Ctrl Pts',(3.52082063196777,0.925583967821042,-1.4797628498031E-16));
#68371=CARTESIAN_POINT('Ctrl Pts',(3.53230884331038,0.850599325135752,-1.66533453693773E-16));
#68372=CARTESIAN_POINT('Ctrl Pts',(3.53784704101621,0.814450984571062,-1.75479430237078E-16));
#68373=CARTESIAN_POINT('Ctrl Pts',(3.54283015535757,0.778213475278794,4.31890150927375E-16));
#68374=CARTESIAN_POINT('Ctrl Pts',(3.54724746220084,0.741898253802422,4.44089209850063E-16));
#68375=CARTESIAN_POINT('Ctrl Pts',(3.54901842299873,0.727338967820404,4.48979985132335E-16));
#68376=CARTESIAN_POINT('Ctrl Pts',(3.55069805246863,0.712770036790904,-2.35249698187168E-16));
#68377=CARTESIAN_POINT('Ctrl Pts',(3.55228494128731,0.698200529246289,-2.22044604925031E-16));
#68378=CARTESIAN_POINT('Ctrl Pts',(3.56439573637877,0.587009172687399,-1.21266165516057E-16));
#68379=CARTESIAN_POINT('Ctrl Pts',(3.57112662647173,0.475642010642433,9.69433660681012E-16));
#68380=CARTESIAN_POINT('Ctrl Pts',(3.57228049049218,0.36441484357905,9.15933995315754E-16));
#68381=CARTESIAN_POINT('Ctrl Pts',(3.57294515040949,0.300344694623918,8.85116600433724E-16));
#68382=CARTESIAN_POINT('Ctrl Pts',(3.571758367986,0.23632098770379,1.62886379851061E-17));
#68383=CARTESIAN_POINT('Ctrl Pts',(3.56867460787407,0.172404957758522,2.77555756156289E-17));
#68384=CARTESIAN_POINT('Ctrl Pts',(3.56321882594294,0.0593248514506371,
4.55069473993787E-17));
#68385=CARTESIAN_POINT('Ctrl Pts',(3.55182795116294,-0.0534195019686971,
1.49200393472243E-16));
#68386=CARTESIAN_POINT('Ctrl Pts',(3.53471671103057,-0.16547091062102,8.32667268468867E-17));
#68387=CARTESIAN_POINT('Ctrl Pts',(3.517527935569,-0.278030052365175,1.70342982085031E-17));
#68388=CARTESIAN_POINT('Ctrl Pts',(3.49456629931175,-0.389890758654236,
2.39344739634145E-16));
#68389=CARTESIAN_POINT('Ctrl Pts',(3.46600457670592,-0.500664418693534,
2.77555756156289E-16));
#68390=CARTESIAN_POINT('Ctrl Pts',(3.45748853890934,-0.533692982438768,
2.88948852624566E-16));
#68391=CARTESIAN_POINT('Ctrl Pts',(3.44847437625935,-0.566624683524517,
6.71135571663658E-16));
#68392=CARTESIAN_POINT('Ctrl Pts',(3.43896601048078,-0.599448603535327,
7.21644966006352E-16));
#68393=CARTESIAN_POINT('Ctrl Pts',(3.43357461779711,-0.618060281537303,
7.50284585627391E-16));
#68394=CARTESIAN_POINT('Ctrl Pts',(3.42802355322236,-0.636639519647583,
-2.81216459416121E-16));
#68395=CARTESIAN_POINT('Ctrl Pts',(3.42232058208389,-0.655162173638946,
-2.77555756156289E-16));
#68396=CARTESIAN_POINT('Ctrl Pts',(3.38955314817876,-0.761587373008277,
-2.56522535191234E-16));
#68397=CARTESIAN_POINT('Ctrl Pts',(3.35173052613294,-0.866304866514825,
6.67536084978692E-16));
#68398=CARTESIAN_POINT('Ctrl Pts',(3.30908814868757,-0.968988090554606,
6.10622663543836E-16));
#68399=CARTESIAN_POINT('Ctrl Pts',(3.26640839035216,-1.07176132810998,5.53659351027008E-16));
#68400=CARTESIAN_POINT('Ctrl Pts',(3.2188998368367,-1.17249747840183,6.13910005376698E-16));
#68401=CARTESIAN_POINT('Ctrl Pts',(3.16675391650558,-1.27084201273691,7.21644966006352E-16));
#68402=CARTESIAN_POINT('Ctrl Pts',(3.11525182214775,-1.36797232426924,8.28049763788275E-16));
#68403=CARTESIAN_POINT('Ctrl Pts',(3.05922554692867,-1.46277033444214,5.31873682911928E-16));
#68404=CARTESIAN_POINT('Ctrl Pts',(2.99882509127823,-1.55485796594408,5.55111512312578E-16));
#68405=CARTESIAN_POINT('Ctrl Pts',(2.96292040398227,-1.60959890419193,5.68925100125488E-16));
#68406=CARTESIAN_POINT('Ctrl Pts',(2.92546942856268,-1.66338135170384,1.04307937839355E-15));
#68407=CARTESIAN_POINT('Ctrl Pts',(2.88649912210471,-1.71611830455392,1.0547118733939E-15));
#68408=CARTESIAN_POINT('Ctrl Pts',(2.86752122028498,-1.74180033798982,1.06037670818993E-15));
#68409=CARTESIAN_POINT('Ctrl Pts',(2.84818295875648,-1.76723433683073,1.01183881774261E-16));
#68410=CARTESIAN_POINT('Ctrl Pts',(2.82848721210062,-1.79240969940257,5.55111512312578E-17));
#68411=CARTESIAN_POINT('Ctrl Pts',(2.81866883519823,-1.8049596779692,3.27431856157449E-17));
#68412=CARTESIAN_POINT('Ctrl Pts',(2.80876707620499,-1.8174383783565,6.6984022778227E-16));
#68413=CARTESIAN_POINT('Ctrl Pts',(2.79878466697198,-1.82984214211003,6.66133814775094E-16));
#68414=CARTESIAN_POINT('Ctrl Pts',(2.73138918440726,-1.91358521698056,6.41110247079955E-16));
#68415=CARTESIAN_POINT('Ctrl Pts',(2.66028938173251,-1.99395520150624,3.65443711379627E-16));
#68416=CARTESIAN_POINT('Ctrl Pts',(2.58565989502056,-2.07063137270062,4.44089209850063E-16));
#68417=CARTESIAN_POINT('Ctrl Pts',(2.51208403758381,-2.14622501924906,5.21624380443388E-16));
#68418=CARTESIAN_POINT('Ctrl Pts',(2.43507686945386,-2.21822892513453,4.26467580169761E-16));
#68419=CARTESIAN_POINT('Ctrl Pts',(2.35477741768754,-2.28629489482386,4.44089209850063E-16));
#68420=CARTESIAN_POINT('Ctrl Pts',(2.27694831596886,-2.35226686800677,4.61168723827668E-16));
#68421=CARTESIAN_POINT('Ctrl Pts',(2.19602584295567,-2.41453975900013,1.30997556575806E-17));
#68422=CARTESIAN_POINT('Ctrl Pts',(2.11211808775947,-2.47275230421329,1.11022302462516E-16));
#68423=CARTESIAN_POINT('Ctrl Pts',(2.03447218398791,-2.52662057507036,2.01637104735594E-16));
#68424=CARTESIAN_POINT('Ctrl Pts',(1.95426950129378,-2.57701176798281,3.53086456726948E-16));
#68425=CARTESIAN_POINT('Ctrl Pts',(1.87158653173892,-2.62360084935066,3.33066907387547E-16));
#68426=CARTESIAN_POINT('Origin',(0.,0.,-2.31077344927314));
#68427=CARTESIAN_POINT('',(-1.87158653173914,-2.6236008493505,0.));
#68428=CARTESIAN_POINT('Ctrl Pts',(-1.87556985610733,-2.62720998907029,
2.71430013881746E-15));
#68429=CARTESIAN_POINT('Ctrl Pts',(-1.0677081740626,-3.19754239838391,0.0612793830239955));
#68430=CARTESIAN_POINT('Ctrl Pts',(1.20136616512241,-3.56759303705228,0.188547785799535));
#68431=CARTESIAN_POINT('Ctrl Pts',(3.66652278292836,-1.02049903436673,0.381805208326622));
#68432=CARTESIAN_POINT('Ctrl Pts',(2.851854515205,2.52082984529409,0.579772267581261));
#68433=CARTESIAN_POINT('Ctrl Pts',(-0.561710868652114,3.76409318953525,
0.777739326835903));
#68434=CARTESIAN_POINT('Ctrl Pts',(-2.91166705408581,1.99385906338734,0.938073054066512));
#68435=CARTESIAN_POINT('Ctrl Pts',(-3.21947657214126,0.462163466687255,
1.03241776154558));
#68436=CARTESIAN_POINT('Ctrl Pts',(-3.217941538466,0.00121291371900208,
1.06077344927309));
#68437=CARTESIAN_POINT('Origin',(0.,0.,0.));
#68438=CARTESIAN_POINT('Ctrl Pts',(-1.43290239521288,2.88667772504885,-0.41006302869194));
#68439=CARTESIAN_POINT('Ctrl Pts',(-2.39040471195644,2.41138831148588,-0.344074008940393));
#68440=CARTESIAN_POINT('Ctrl Pts',(-3.77909242612025,0.441642854121313,
-0.212095969437299));
#68441=CARTESIAN_POINT('Ctrl Pts',(-2.42543897582905,-2.93619362552599,
-0.014128910182659));
#68442=CARTESIAN_POINT('Ctrl Pts',(1.14129089352572,-3.6296651029358,0.183838149071981));
#68443=CARTESIAN_POINT('Ctrl Pts',(3.66652278292836,-1.02049903436673,0.381805208326622));
#68444=CARTESIAN_POINT('Ctrl Pts',(2.851854515205,2.52082984529409,0.579772267581261));
#68445=CARTESIAN_POINT('Ctrl Pts',(-0.561710868652114,3.76409318953525,
0.777739326835903));
#68446=CARTESIAN_POINT('Ctrl Pts',(-3.46324583227481,1.57835192224933,0.975706386090541));
#68447=CARTESIAN_POINT('Ctrl Pts',(-3.20937516570907,-2.04583258259621,
1.17367344534518));
#68448=CARTESIAN_POINT('Ctrl Pts',(-0.031229830088373,-3.80578923437654,
1.37164050459982));
#68449=CARTESIAN_POINT('Ctrl Pts',(3.17533772956661,-2.09820398373205,1.56960756385447));
#68450=CARTESIAN_POINT('Ctrl Pts',(3.48872347062518,1.52120070666785,1.7675746231091));
#68451=CARTESIAN_POINT('Ctrl Pts',(0.623360915472078,3.75454335133777,1.96554168236375));
#68452=CARTESIAN_POINT('Ctrl Pts',(-2.80997029272685,2.56695867698206,2.16350874161838));
#68453=CARTESIAN_POINT('Ctrl Pts',(-3.68300839979145,-0.95950905902386,
2.36147580087303));
#68454=CARTESIAN_POINT('Ctrl Pts',(-1.20028377732907,-3.61171960603965,
2.55944286012766));
#68455=CARTESIAN_POINT('Ctrl Pts',(2.37607494490469,-2.97312511164363,2.75740991938231));
#68456=CARTESIAN_POINT('Ctrl Pts',(3.78748084593007,0.374423891696219,2.95537697863694));
#68457=CARTESIAN_POINT('Ctrl Pts',(1.74793537283732,3.38081724446415,3.15334403789159));
#68458=CARTESIAN_POINT('Ctrl Pts',(-1.88423579077553,3.30678992389447,3.35131109714622));
#68459=CARTESIAN_POINT('Ctrl Pts',(-3.79959152376013,0.219791286247465,
3.54927815640087));
#68460=CARTESIAN_POINT('Ctrl Pts',(-2.25296143303411,-3.06746941436165,
3.7472452156555));
#68461=CARTESIAN_POINT('Ctrl Pts',(1.34644732705721,-3.55981509909713,3.94521227491016));
#68462=CARTESIAN_POINT('Ctrl Pts',(3.71904487139598,-0.808646497252913,
4.14317933416478));
#68463=CARTESIAN_POINT('Ctrl Pts',(2.70304644183217,2.67931779227495,4.34114639341943));
#68464=CARTESIAN_POINT('Ctrl Pts',(-0.775824200771678,3.72603015619545,
4.53911345267407));
#68465=CARTESIAN_POINT('Ctrl Pts',(-3.54780507800637,1.37778192696114,4.73708051192871));
#68466=CARTESIAN_POINT('Ctrl Pts',(-3.08721458058898,-2.22582794524067,
4.93504757118334));
#68467=CARTESIAN_POINT('Ctrl Pts',(0.186281715928623,-3.80138172682447,
5.133014630438));
#68468=CARTESIAN_POINT('Ctrl Pts',(3.290048016384,-1.91331857244767,5.33098168969263));
#68469=CARTESIAN_POINT('Ctrl Pts',(3.39609747398096,1.71805874664089,5.52894874894727));
#68470=CARTESIAN_POINT('Ctrl Pts',(0.407803461009433,3.78403227353958,5.72691580820191));
#68471=CARTESIAN_POINT('Ctrl Pts',(-2.95205938548467,2.40219676430168,5.92488286745655));
#68472=CARTESIAN_POINT('Ctrl Pts',(-3.62216266107621,-1.16839272787695,
6.12284992671119));
#68473=CARTESIAN_POINT('Ctrl Pts',(-0.991943885951175,-3.67440488202038,
6.32081698596584));
#68474=CARTESIAN_POINT('Ctrl Pts',(2.54208142306422,-2.83249465107694,6.51878404522046));
#68475=CARTESIAN_POINT('Ctrl Pts',(3.75989728477033,0.590234121215191,6.71675110447512));
#68476=CARTESIAN_POINT('Ctrl Pts',(1.55189462906941,3.47517294104057,6.91471816372975));
#68477=CARTESIAN_POINT('Ctrl Pts',(-2.07011190883012,3.19371892858329,7.1126852229844));
#68478=CARTESIAN_POINT('Ctrl Pts',(-3.805942529344,0.0023180169775348,7.31065228223903));
#68479=CARTESIAN_POINT('Ctrl Pts',(-2.07400065351091,-3.19119494846509,
7.50861934149368));
#68480=CARTESIAN_POINT('Ctrl Pts',(1.5476603571224,-3.4770607312591,7.70658640074832));
#68481=CARTESIAN_POINT('Ctrl Pts',(3.75917552904779,-0.594813627685692,
7.90455346000295));
#68482=CARTESIAN_POINT('Ctrl Pts',(2.54552980900885,2.82939603119107,8.1025205192576));
#68483=CARTESIAN_POINT('Ctrl Pts',(-0.987467344283091,3.67561044642204,
8.30048757851224));
#68484=CARTESIAN_POINT('Ctrl Pts',(-3.62073675046792,1.17280403038332,8.49845463776687));
#68485=CARTESIAN_POINT('Ctrl Pts',(-2.95498331987074,-2.39859906803078,
8.69642169702152));
#68486=CARTESIAN_POINT('Ctrl Pts',(0.403193815184867,-3.78452621305085,
8.89438875627614));
#68487=CARTESIAN_POINT('Ctrl Pts',(3.39400218094999,-1.72219427056852,9.0923558155308));
#68488=CARTESIAN_POINT('Ctrl Pts',(3.29237619572427,1.90930953375835,9.29032287478543));
#68489=CARTESIAN_POINT('Ctrl Pts',(0.190912054474585,3.80115199608339,9.48828993404008));
#68490=CARTESIAN_POINT('Ctrl Pts',(-3.0845010013012,2.22958684128793,9.68625699329472));
#68491=CARTESIAN_POINT('Ctrl Pts',(-3.549480726884,-1.3734593111379,9.88422405254936));
#68492=CARTESIAN_POINT('Ctrl Pts',(-0.780362316170466,-3.72508235685782,
10.082191111804));
#68493=CARTESIAN_POINT('Ctrl Pts',(2.6997807504167,-2.68260839660801,10.2801581710586));
#68494=CARTESIAN_POINT('Ctrl Pts',(3.72002712642615,0.80411571836772,10.4781252303133));
#68495=CARTESIAN_POINT('Ctrl Pts',(1.35078255368256,3.55817234019647,10.6760922895679));
#68496=CARTESIAN_POINT('Ctrl Pts',(-2.24922326994444,3.07021148975323,10.8740593488226));
#68497=CARTESIAN_POINT('Ctrl Pts',(-3.79985642608623,-0.215162847637767,
11.0720264080772));
#68498=CARTESIAN_POINT('Ctrl Pts',(-1.88826241961219,-3.30449223702413,
11.2699934673318));
#68499=CARTESIAN_POINT('Ctrl Pts',(1.74381591738736,-3.38294397768258,11.4679605265865));
#68500=CARTESIAN_POINT('Ctrl Pts',(3.78702189743871,-0.379037014277084,
11.6659275858411));
#68501=CARTESIAN_POINT('Ctrl Pts',(2.37969485505221,2.97022832568649,11.8638946450958));
#68502=CARTESIAN_POINT('Ctrl Pts',(-1.1958836268722,3.61317952236688,12.0618617043504));
#68503=CARTESIAN_POINT('Ctrl Pts',(-3.68183652508766,0.963993626743878,
12.2598287636051));
#68504=CARTESIAN_POINT('Ctrl Pts',(-2.81309572015205,-2.56353201250435,
12.4577958228597));
#68505=CARTESIAN_POINT('Ctrl Pts',(0.61878835158859,-3.75530356773067,12.6557628821143));
#68506=CARTESIAN_POINT('Ctrl Pts',(3.48686537418057,-1.52544215629862,12.853729941369));
#68507=CARTESIAN_POINT('Ctrl Pts',(3.17789604102199,2.09432105044312,13.0516970006236));
#68508=CARTESIAN_POINT('Ctrl Pts',(-0.0266032173364325,3.80585025699904,
13.2496640598783));
#68509=CARTESIAN_POINT('Ctrl Pts',(-3.20686303837221,2.04969104086312,13.4476311191329));
#68510=CARTESIAN_POINT('Ctrl Pts',(-3.46519974620323,-1.57403768340705,
13.6455981783875));
#68511=CARTESIAN_POINT('Ctrl Pts',(-0.566230666680783,-3.76358695156398,
13.8435652376421));
#68512=CARTESIAN_POINT('Ctrl Pts',(2.84865769364129,-2.52395587408549,14.0415322968968));
#68513=CARTESIAN_POINT('Ctrl Pts',(3.66800060750612,1.01536961408498,14.2394993561514));
#68514=CARTESIAN_POINT('Ctrl Pts',(1.14525637075743,3.62954429028107,14.4374664154061));
#68515=CARTESIAN_POINT('Ctrl Pts',(-2.42098458543948,2.93667116765511,14.6354334746607));
#68516=CARTESIAN_POINT('Ctrl Pts',(-3.78135309486711,-0.431940599864457,
14.8334005339154));
#68517=CARTESIAN_POINT('Ctrl Pts',(-1.696353693388,-3.4069910561669,15.03136759317));
#68518=CARTESIAN_POINT('Ctrl Pts',(1.93427300977863,-3.27777238891207,15.2293346524246));
#68519=CARTESIAN_POINT('Ctrl Pts',(3.80249297873402,-0.162021778014253,
15.4273017116793));
#68520=CARTESIAN_POINT('Ctrl Pts',(2.2060834984687,3.10135446340087,15.6252687709339));
#68521=CARTESIAN_POINT('Ctrl Pts',(-1.40039198296493,3.53894139594313,15.8232358301886));
#68522=CARTESIAN_POINT('Ctrl Pts',(-3.73090473895306,0.75203307023697,16.0212028894432));
#68523=CARTESIAN_POINT('Ctrl Pts',(-2.6620154439432,-2.72008780852388,16.2191699486979));
#68524=CARTESIAN_POINT('Ctrl Pts',(0.832360802113325,-3.71380928494957,
16.4171370079525));
#68525=CARTESIAN_POINT('Ctrl Pts',(3.56833413631518,-1.32370517921483,16.6151040672071));
#68526=CARTESIAN_POINT('Ctrl Pts',(3.05303110985611,2.27248871331039,16.8130711264618));
#68527=CARTESIAN_POINT('Ctrl Pts',(-0.244031554753848,3.79811170322264,
17.0110381857164));
#68528=CARTESIAN_POINT('Ctrl Pts',(-3.31874564019015,1.86309722923718,17.2090052449711));
#68529=CARTESIAN_POINT('Ctrl Pts',(-3.36959513369136,-1.76947239166818,
17.4069723042257));
#68530=CARTESIAN_POINT('Ctrl Pts',(-0.350248680105062,-3.78979284024299,
17.6049393634804));
#68531=CARTESIAN_POINT('Ctrl Pts',(2.98822575042405,-2.3570555306091,17.8029064227349));
#68532=CARTESIAN_POINT('Ctrl Pts',(3.60398774105126,1.2233054697109,18.0008734819896));
#68533=CARTESIAN_POINT('Ctrl Pts',(0.935987701844621,3.68905556096245,18.1988405412443));
#68534=CARTESIAN_POINT('Ctrl Pts',(-2.58483457110589,2.79353434736147,18.3968076004989));
#68535=CARTESIAN_POINT('Ctrl Pts',(-3.75049300115066,-0.647306850104539,
18.5947746597535));
#68536=CARTESIAN_POINT('Ctrl Pts',(-1.49890159705929,-3.49835645871106,
18.7927417190082));
#68537=CARTESIAN_POINT('Ctrl Pts',(2.1184092557461,-3.16188964624663,18.9907087782628));
#68538=CARTESIAN_POINT('Ctrl Pts',(3.80553821630163,0.0555229154508125,
19.1886758375175));
#68539=CARTESIAN_POINT('Ctrl Pts',(2.02526306905968,3.2223459483698,19.3866428967721));
#68540=CARTESIAN_POINT('Ctrl Pts',(-1.60032411708034,3.45313866361654,19.5846099560268));
#68541=CARTESIAN_POINT('Ctrl Pts',(-3.76778104621707,0.537615008756083,
19.7825770152813));
#68542=CARTESIAN_POINT('Ctrl Pts',(-2.50223619364232,-2.86775486070528,
19.980544074536));
#68543=CARTESIAN_POINT('Ctrl Pts',(1.04321325149407,-3.66017896034874,20.1785111337906));
#68544=CARTESIAN_POINT('Ctrl Pts',(3.63814224250802,-1.11764257844405,20.3764781930453));
#68545=CARTESIAN_POINT('Ctrl Pts',(2.91818943772608,2.44323030339269,20.5744452522999));
#68546=CARTESIAN_POINT('Ctrl Pts',(-0.460662442187536,3.77796162291654,
20.7724123115546));
#68547=CARTESIAN_POINT('Ctrl Pts',(-3.41978319510662,1.67041516047321,20.9703793708092));
#68548=CARTESIAN_POINT('Ctrl Pts',(-3.2629793075386,-1.95912479144318,21.1683464300639));
#68549=CARTESIAN_POINT('Ctrl Pts',(-0.133122145626393,-3.80361438689783,
21.3663134893184));
#68550=CARTESIAN_POINT('Ctrl Pts',(3.11802883817059,-2.18245276563067,21.5642805485732));
#68551=CARTESIAN_POINT('Ctrl Pts',(3.52819770926901,1.42724378933009,21.7622476078277));
#68552=CARTESIAN_POINT('Ctrl Pts',(0.723660398246818,3.73651168041552,21.9602146670825));
#68553=CARTESIAN_POINT('Ctrl Pts',(-2.74023779549696,2.64126877352578,22.158181726337));
#68554=CARTESIAN_POINT('Ctrl Pts',(-3.70737699001511,-0.860557821287339,
22.3561487855917));
#68555=CARTESIAN_POINT('Ctrl Pts',(-1.29655136755524,-3.57828987942048,
22.5541158448463));
#68556=CARTESIAN_POINT('Ctrl Pts',(2.29562293209663,-3.03567443305511,22.752082904101));
#68557=CARTESIAN_POINT('Ctrl Pts',(3.79614765886846,0.272886170297954,22.9500499633556));
#68558=CARTESIAN_POINT('Ctrl Pts',(1.83782445454307,3.3328074027996,23.1480170226103));
#68559=CARTESIAN_POINT('Ctrl Pts',(-1.79502668798453,3.35605171284586,23.3459840818649));
#68560=CARTESIAN_POINT('Ctrl Pts',(-3.79234494192839,0.321440120866347,
23.5439511411195));
#68561=CARTESIAN_POINT('Ctrl Pts',(-2.33428009828589,-3.00605062043518,
23.7419182003742));
#68562=CARTESIAN_POINT('Ctrl Pts',(1.25065667292649,-3.59458784790924,23.9398852596288));
#68563=CARTESIAN_POINT('Ctrl Pts',(3.6960615727801,-0.90792772845131,24.1378523188835));
#68564=CARTESIAN_POINT('Ctrl Pts',(2.77381166227548,2.60598786875474,24.3358193781381));
#68565=CARTESIAN_POINT('Ctrl Pts',(-0.675787969966405,3.74546586281613,
24.5337864373928));
#68566=CARTESIAN_POINT('Ctrl Pts',(-3.5096455310805,1.47227448393265,24.7317534966474));
#68567=CARTESIAN_POINT('Ctrl Pts',(-3.14570066854468,-2.1423751337686,24.9297205559021));
#68568=CARTESIAN_POINT('Ctrl Pts',(0.0844394074013012,-3.80500642527053,
25.1276876151567));
#68569=CARTESIAN_POINT('Ctrl Pts',(3.23764278439912,-2.00071814869078,25.3256546744113));
#68570=CARTESIAN_POINT('Ctrl Pts',(3.44087817996476,1.6265181402354,25.523621733666));
#68571=CARTESIAN_POINT('Ctrl Pts',(0.50896830631917,3.77175757081959,25.7215887929206));
#68572=CARTESIAN_POINT('Ctrl Pts',(-2.88668642961947,2.4803720218796,25.9195558521752));
#68573=CARTESIAN_POINT('Ctrl Pts',(-3.65214595660994,-1.07099664868295,
26.1175229114299));
#68574=CARTESIAN_POINT('Ctrl Pts',(-1.08996424799818,-3.64653011066113,
26.3154899706845));
#68575=CARTESIAN_POINT('Ctrl Pts',(2.46533493731419,-2.89953919730883,26.5134570299392));
#68576=CARTESIAN_POINT('Ctrl Pts',(3.77435199303925,0.489357683614875,26.7114240891938));
#68577=CARTESIAN_POINT('Ctrl Pts',(1.64438016964158,3.43237785908865,26.9093911484484));
#68578=CARTESIAN_POINT('Ctrl Pts',(-1.98386344368891,3.24799780582855,27.1073582077031));
#68579=CARTESIAN_POINT('Ctrl Pts',(-3.80451615581926,0.104214826116698,
27.3053252669577));
#68580=CARTESIAN_POINT('Ctrl Pts',(-2.15869600732759,-3.13452316275066,
27.5032923262124));
#68581=CARTESIAN_POINT('Ctrl Pts',(1.45401317967913,-3.51725028725448,27.701259385467));
#68582=CARTESIAN_POINT('Ctrl Pts',(3.74190285747308,-0.695245938576497,
27.8992264447217));
#68583=CARTESIAN_POINT('Ctrl Pts',(2.6203695833697,2.76022954777739,28.0971935039762));
#68584=CARTESIAN_POINT('Ctrl Pts',(-0.888705147656408,3.70073061305487,
28.295160563231));
#68585=CARTESIAN_POINT('Ctrl Pts',(-3.58803899461921,1.26932268669724,28.4931276224855));
#68586=CARTESIAN_POINT('Ctrl Pts',(-3.01814246160937,-2.31862459042054,
28.6910946817402));
#68587=CARTESIAN_POINT('Ctrl Pts',(0.301725028063924,-3.79396440643719,
28.8890617409948));
#68588=CARTESIAN_POINT('Ctrl Pts',(3.34667671285774,-1.8124455549031,29.0870288002495));
#68589=CARTESIAN_POINT('Ctrl Pts',(3.34231449720922,1.8204773307068,29.2849958595041));
#68590=CARTESIAN_POINT('Ctrl Pts',(0.292613000107598,3.79467805512411,29.4829629187588));
#68591=CARTESIAN_POINT('Ctrl Pts',(-3.023701906425,2.31136987324706,29.6809299780134));
#68592=CARTESIAN_POINT('Ctrl Pts',(-3.58498038573646,-1.27793565712721,
29.878897037268));
#68593=CARTESIAN_POINT('Ctrl Pts',(-0.879815326883564,-3.70285415597931,
30.0768640965227));
#68594=CARTESIAN_POINT('Ctrl Pts',(2.62699068395643,-2.75392880377806,30.2748311557773));
#68595=CARTESIAN_POINT('Ctrl Pts',(3.74022244301854,0.70423006653559,30.4727982150319));
#68596=CARTESIAN_POINT('Ctrl Pts',(1.44556235449795,3.52073193940277,30.6707652742866));
#68597=CARTESIAN_POINT('Ctrl Pts',(-2.16621730060395,3.12933004274663,30.8687323335412));
#68598=CARTESIAN_POINT('Ctrl Pts',(-3.80425491461396,-0.113351023408669,
31.0666993927959));
#68599=CARTESIAN_POINT('Ctrl Pts',(-1.9760576970998,-3.25275266314625,31.2646664520505));
#68600=CARTESIAN_POINT('Ctrl Pts',(1.65261824030163,-3.42841900322799,31.4626335113052));
#68601=CARTESIAN_POINT('Ctrl Pts',(3.77551629574763,-0.480292213570351,
31.6606005705598));
#68602=CARTESIAN_POINT('Ctrl Pts',(2.45836462134124,2.90545130718283,31.8585676298145));
#68603=CARTESIAN_POINT('Ctrl Pts',(-1.0987182013029,3.64390206015446,32.0565346890691));
#68604=CARTESIAN_POINT('Ctrl Pts',(-3.65470741038376,1.06222297770173,32.2545017483237));
#68605=CARTESIAN_POINT('Ctrl Pts',(-2.88072152335954,-2.4872972107748,32.4524688075784));
#68606=CARTESIAN_POINT('Ctrl Pts',(0.518024667143807,-3.77052441367253,
32.650435866833));
#68607=CARTESIAN_POINT('Ctrl Pts',(3.44477432083465,-1.61825022428116,32.8484029260877));
#68608=CARTESIAN_POINT('Ctrl Pts',(3.23282874888886,2.00848753798692,33.0463699853423));
#68609=CARTESIAN_POINT('Ctrl Pts',(0.0753014887309373,3.80519823342296,
33.2443370445969));
#68610=CARTESIAN_POINT('Ctrl Pts',(-3.15083648467107,2.1348145953959,33.4423041038516));
#68611=CARTESIAN_POINT('Ctrl Pts',(-3.50609976207099,-1.48069860822725,
33.6402711631062));
#68612=CARTESIAN_POINT('Ctrl Pts',(-0.666791331988793,-3.74707795879318,
33.8382382223608));
#68613=CARTESIAN_POINT('Ctrl Pts',(2.78006191089306,-2.59931908033378,34.0362052816155));
#68614=CARTESIAN_POINT('Ctrl Pts',(3.69387053796041,0.916801155928787,34.2341723408701));
#68615=CARTESIAN_POINT('Ctrl Pts',(1.24202070877136,3.59758091881176,34.4321394001247));
#68616=CARTESIAN_POINT('Ctrl Pts',(-2.34149235969762,3.0004362081648,34.6301064593794));
#68617=CARTESIAN_POINT('Ctrl Pts',(-3.79156207268276,-0.330546463261181,
34.828073518634));
#68618=CARTESIAN_POINT('Ctrl Pts',(-1.78696199451318,-3.36035276851525,
35.0260405778887));
#68619=CARTESIAN_POINT('Ctrl Pts',(1.84582284769266,-3.32838428188693,35.2240076371433));
#68620=CARTESIAN_POINT('Ctrl Pts',(3.79679204988465,-0.263768978904437,
35.421974696398));
#68621=CARTESIAN_POINT('Ctrl Pts',(2.28832616929499,3.04117858234319,35.6199417556526));
#68622=CARTESIAN_POINT('Ctrl Pts',(-1.30514082959193,3.5751659222856,35.8179088149073));
#68623=CARTESIAN_POINT('Ctrl Pts',(-3.70943295180687,0.851652095669924,
36.0158758741619));
#68624=CARTESIAN_POINT('Ctrl Pts',(-2.73388685593464,-2.64784175641783,
36.2138429334166));
#68625=CARTESIAN_POINT('Ctrl Pts',(0.732631374839026,-3.7347631354025,36.4118099926711));
#68626=CARTESIAN_POINT('Ctrl Pts',(3.53161527805439,-1.41876657738429,36.6097770519258));
#68627=CARTESIAN_POINT('Ctrl Pts',(3.11277826536447,2.18993404682541,36.8077441111804));
#68628=CARTESIAN_POINT('Ctrl Pts',(-0.14225523522422,3.80328436424815,37.0057111704351));
#68629=CARTESIAN_POINT('Ctrl Pts',(-3.26767635523122,1.95128192038049,37.2036782296897));
#68630=CARTESIAN_POINT('Ctrl Pts',(-3.41575870887161,-1.6786205797561,37.4016452889444));
#68631=CARTESIAN_POINT('Ctrl Pts',(-0.451594402129131,-3.77906146290628,
37.599612348199));
#68632=CARTESIAN_POINT('Ctrl Pts',(2.92405992033173,-2.43620673106119,37.7975794074536));
#68633=CARTESIAN_POINT('Ctrl Pts',(3.63542572274911,1.12635998382311,37.9955464667083));
#68634=CARTESIAN_POINT('Ctrl Pts',(1.03446251089667,3.6627049053714,38.1935135259629));
#68635=CARTESIAN_POINT('Ctrl Pts',(-2.50919648981435,2.86167773530498,38.3914805852176));
#68636=CARTESIAN_POINT('Ctrl Pts',(-3.76632481410217,-0.546547375939128,
38.5894476444722));
#68637=CARTESIAN_POINT('Ctrl Pts',(-1.59232210767045,-3.45719070782108,
38.7874147037269));
#68638=CARTESIAN_POINT('Ctrl Pts',(2.03356109694112,-3.21705406573836,38.9853817629815));
#68639=CARTESIAN_POINT('Ctrl Pts',(3.80457448616929,-0.0471873108411222,
39.1833488222361));
#68640=CARTESIAN_POINT('Ctrl Pts',(2.11292542611656,3.16852227003697,39.3813158814907));
#68641=CARTESIAN_POINT('Ctrl Pts',(-1.51168002663127,3.4916201787766,39.5792829407454));
#68642=CARTESIAN_POINT('Ctrl Pts',(-2.99782464886751,1.59432608031001,39.7112609802485));
#68643=CARTESIAN_POINT('Ctrl Pts',(-3.17710367210759,0.540490350682096,
39.7772500000001));
#68644=CARTESIAN_POINT('Ctrl Pts',(-1.5381664219189,3.09873914818289,-0.273375352461296));
#68645=CARTESIAN_POINT('Ctrl Pts',(-2.56600887472297,2.58853397365147,-0.207386332709749));
#68646=CARTESIAN_POINT('Ctrl Pts',(-4.05671251203569,0.474086867995491,
-0.0754082932066554));
#68647=CARTESIAN_POINT('Ctrl Pts',(-2.60361682937877,-3.15189259095719,
0.122558766047985));
#68648=CARTESIAN_POINT('Ctrl Pts',(1.22513252537504,-3.89630794309404,0.320525825302625));
#68649=CARTESIAN_POINT('Ctrl Pts',(3.93587326585702,-1.0954670419336,0.518492884557265));
#68650=CARTESIAN_POINT('Ctrl Pts',(3.06135775202903,2.70601531294549,0.716459943811906));
#68651=CARTESIAN_POINT('Ctrl Pts',(-0.60297533165843,4.04061139995257,0.914427003066545));
#68652=CARTESIAN_POINT('Ctrl Pts',(-3.71766316244039,1.69430097743274,1.11239406232119));
#68653=CARTESIAN_POINT('Ctrl Pts',(-3.44514262222338,-2.19612375129681,
1.31036112157583));
#68654=CARTESIAN_POINT('Ctrl Pts',(-0.0335240391561582,-4.08537052403247,
1.50832818083047));
#68655=CARTESIAN_POINT('Ctrl Pts',(3.40860472436144,-2.25234246581983,1.70629524008511));
#68656=CARTESIAN_POINT('Ctrl Pts',(3.74501244174315,1.63295131323175,1.90426229933975));
#68657=CARTESIAN_POINT('Ctrl Pts',(0.669154320712261,4.03036001053543,2.10222935859439));
#68658=CARTESIAN_POINT('Ctrl Pts',(-3.01639662638699,2.75553286572625,2.30019641784903));
#68659=CARTESIAN_POINT('Ctrl Pts',(-3.95356995084275,-1.02999661459724,
2.49816347710367));
#68660=CARTESIAN_POINT('Ctrl Pts',(-1.28845915062283,-3.87704413221449,
2.69613053635831));
#68661=CARTESIAN_POINT('Ctrl Pts',(2.55062641281451,-3.19153714179847,2.89409759561295));
#68662=CARTESIAN_POINT('Ctrl Pts',(4.06571716282525,0.40192985907169,3.09206465486759));
#68663=CARTESIAN_POINT('Ctrl Pts',(1.87634238533256,3.62917919702857,3.29003171412223));
#68664=CARTESIAN_POINT('Ctrl Pts',(-2.02265571893201,3.54971367363674,3.48799877337687));
#68665=CARTESIAN_POINT('Ctrl Pts',(-4.07871751654587,0.235937616871581,
3.68596583263151));
#68666=CARTESIAN_POINT('Ctrl Pts',(-2.41846872316541,-3.29281217562152,
3.88393289188615));
#68667=CARTESIAN_POINT('Ctrl Pts',(1.44536018243879,-3.82132661091504,4.08189995114079));
#68668=CARTESIAN_POINT('Ctrl Pts',(3.99225373752058,-0.868051371420758,
4.27986701039543));
#68669=CARTESIAN_POINT('Ctrl Pts',(2.90161792429393,2.87614611818334,4.47783406965007));
#68670=CARTESIAN_POINT('Ctrl Pts',(-0.83281787993789,3.99975217604782,4.67580112890471));
#68671=CARTESIAN_POINT('Ctrl Pts',(-3.80843430838976,1.47899668802168,4.87376818815935));
#68672=CARTESIAN_POINT('Ctrl Pts',(-3.31400786333022,-2.38934195223343,
5.071735247414));
#68673=CARTESIAN_POINT('Ctrl Pts',(0.199966362968053,-4.0806392316963,5.26970230666863));
#68674=CARTESIAN_POINT('Ctrl Pts',(3.53174187035313,-2.05387498297495,5.46766936592327));
#68675=CARTESIAN_POINT('Ctrl Pts',(3.64558194437578,1.84427095927526,5.66563642517792));
#68676=CARTESIAN_POINT('Ctrl Pts',(0.437761561822023,4.06201525104653,5.86360348443255));
#68677=CARTESIAN_POINT('Ctrl Pts',(-3.16892388304534,2.57866719605973,6.0615705436872));
#68678=CARTESIAN_POINT('Ctrl Pts',(-3.88825435606022,-1.25422531753642,
6.25953760294183));
#68679=CARTESIAN_POINT('Ctrl Pts',(-1.064814172197,-3.94433440054288,6.45750466219648));
#68680=CARTESIAN_POINT('Ctrl Pts',(2.72882807636051,-3.04057567152293,6.65547172145111));
#68681=CARTESIAN_POINT('Ctrl Pts',(4.03610725518979,0.633593962406071,6.85343878070576));
#68682=CARTESIAN_POINT('Ctrl Pts',(1.66590007579409,3.73046646172677,7.05140583996039));
#68683=CARTESIAN_POINT('Ctrl Pts',(-2.22218668795221,3.42833624495657,7.24937289921504));
#68684=CARTESIAN_POINT('Ctrl Pts',(-4.08553508037097,0.00248830338486328,
7.44733995846967));
#68685=CARTESIAN_POINT('Ctrl Pts',(-2.22636110800429,-3.4256268479451,7.64530701772432));
#68686=CARTESIAN_POINT('Ctrl Pts',(1.66135474531538,-3.73249293298914,7.84327407697896));
#68687=CARTESIAN_POINT('Ctrl Pts',(4.03533247777236,-0.638509889063205,
8.0412411362336));
#68688=CARTESIAN_POINT('Ctrl Pts',(2.73252978799657,3.03724942049667,8.23920819548824));
#68689=CARTESIAN_POINT('Ctrl Pts',(-1.06000877435344,3.94562852824358,8.43717525474288));
#68690=CARTESIAN_POINT('Ctrl Pts',(-3.88672369505666,1.2589606836121,8.63514231399753));
#68691=CARTESIAN_POINT('Ctrl Pts',(-3.17206261580721,-2.57480520544648,
8.83310937325215));
#68692=CARTESIAN_POINT('Ctrl Pts',(0.432813281710421,-4.0625454763942,9.03107643250681));
#68693=CARTESIAN_POINT('Ctrl Pts',(3.6433327267075,-1.8487102874972,9.22904349176143));
#68694=CARTESIAN_POINT('Ctrl Pts',(3.5342410826493,2.04957143186323,9.42701055101609));
#68695=CARTESIAN_POINT('Ctrl Pts',(0.204936855931924,4.08039262445131,9.62497761027071));
#68696=CARTESIAN_POINT('Ctrl Pts',(-3.31109493879501,2.39337698469798,9.82294466952537));
#68697=CARTESIAN_POINT('Ctrl Pts',(-3.81023305396172,-1.4743565237396,10.02091172878));
#68698=CARTESIAN_POINT('Ctrl Pts',(-0.837689374848039,-3.99873474937543,
10.2188787880347));
#68699=CARTESIAN_POINT('Ctrl Pts',(2.89811232831176,-2.87967845723847,10.4168458472893));
#68700=CARTESIAN_POINT('Ctrl Pts',(3.99330815107321,0.863187751979935,10.6148129065439));
#68701=CARTESIAN_POINT('Ctrl Pts',(1.45001388393906,3.81956317148701,10.8127799657986));
#68702=CARTESIAN_POINT('Ctrl Pts',(-2.41445594674516,3.2957556896443,11.0107470250532));
#68703=CARTESIAN_POINT('Ctrl Pts',(-4.07900187915454,-0.230969163417291,
11.2087140843079));
#68704=CARTESIAN_POINT('Ctrl Pts',(-2.02697815240034,-3.54724719385154,
11.4066811435625));
#68705=CARTESIAN_POINT('Ctrl Pts',(1.87192030601249,-3.63146216454668,11.6046482028171));
#68706=CARTESIAN_POINT('Ctrl Pts',(4.06522449901148,-0.406881871349422,
11.8026152620718));
#68707=CARTESIAN_POINT('Ctrl Pts',(2.55451224918252,3.18842755184626,12.0005823213264));
#68708=CARTESIAN_POINT('Ctrl Pts',(-1.28373575584969,3.8786112970687,12.198549380581));
#68709=CARTESIAN_POINT('Ctrl Pts',(-3.95231198775605,1.0348106281034,12.3965164398357));
#68710=CARTESIAN_POINT('Ctrl Pts',(-3.01975165429086,-2.75185447126179,
12.5944834990903));
#68711=CARTESIAN_POINT('Ctrl Pts',(0.664245846659203,-4.03117607402505,
12.792450558345));
#68712=CARTESIAN_POINT('Ctrl Pts',(3.74301784562183,-1.63750434868199,12.9904176175996));
#68713=CARTESIAN_POINT('Ctrl Pts',(3.41135097476238,2.24817428407668,13.1883846768543));
#68714=CARTESIAN_POINT('Ctrl Pts',(-0.0285575456909824,4.0854360295053,
13.3863517361089));
#68715=CARTESIAN_POINT('Ctrl Pts',(-3.44244594872354,2.20026566003127,13.5843187953636));
#68716=CARTESIAN_POINT('Ctrl Pts',(-3.71976061499961,-1.68966980552226,
13.7822858546182));
#68717=CARTESIAN_POINT('Ctrl Pts',(-0.607827163565885,-4.04006797267415,
13.9802529138728));
#68718=CARTESIAN_POINT('Ctrl Pts',(3.05792608522293,-2.70937098639317,14.1782199731274));
#68719=CARTESIAN_POINT('Ctrl Pts',(3.93745965453956,1.08996080363888,14.3761870323821));
#68720=CARTESIAN_POINT('Ctrl Pts',(1.22938931491277,3.89617825528739,14.5741540916367));
#68721=CARTESIAN_POINT('Ctrl Pts',(-2.59883521009326,3.15240521433642,14.7721211508914));
#68722=CARTESIAN_POINT('Ctrl Pts',(-4.05913925426817,-0.463671865714468,
14.970088210146));
#68723=CARTESIAN_POINT('Ctrl Pts',(-1.82097140711367,-3.65727579204391,
15.1680552694007));
#68724=CARTESIAN_POINT('Ctrl Pts',(2.07636877738867,-3.51856444944261,15.3660223286553));
#68725=CARTESIAN_POINT('Ctrl Pts',(4.08183211851069,-0.173924238938826,
15.5639893879099));
#68726=CARTESIAN_POINT('Ctrl Pts',(2.36814703683261,3.32918649170288,15.7619564471646));
#68727=CARTESIAN_POINT('Ctrl Pts',(-1.50326772634159,3.798919481581,15.9599235064192));
#68728=CARTESIAN_POINT('Ctrl Pts',(-4.0049848559175,0.807279002865442,16.1578905656739));
#68729=CARTESIAN_POINT('Ctrl Pts',(-2.85757270291564,-2.91991118566086,
16.3558576249285));
#68730=CARTESIAN_POINT('Ctrl Pts',(0.893507779043135,-3.98663353387107,
16.5538246841831));
#68731=CARTESIAN_POINT('Ctrl Pts',(3.83047147454269,-1.42094734853573,16.7517917434378));
#68732=CARTESIAN_POINT('Ctrl Pts',(3.27731320286931,2.43943051856256,16.9497588026924));
#68733=CARTESIAN_POINT('Ctrl Pts',(-0.261958626536699,4.07712898527615,
17.1477258619471));
#68734=CARTESIAN_POINT('Ctrl Pts',(-3.56254768202248,1.99996427415897,17.3456929212017));
#68735=CARTESIAN_POINT('Ctrl Pts',(-3.61713268637194,-1.8994615589097,17.5436599804563));
#68736=CARTESIAN_POINT('Ctrl Pts',(-0.375978685539757,-4.06819900110795,
17.741627039711));
#68737=CARTESIAN_POINT('Ctrl Pts',(3.20774710529583,-2.53020979230223,17.9395940989656));
#68738=CARTESIAN_POINT('Ctrl Pts',(3.86874426814577,1.31317206499575,18.1375611582203));
#68739=CARTESIAN_POINT('Ctrl Pts',(1.00474732899892,3.96006134920477,18.3355282174749));
#68740=CARTESIAN_POINT('Ctrl Pts',(-2.77472196066743,2.99875326187165,18.5334952767295));
#68741=CARTESIAN_POINT('Ctrl Pts',(-4.02601211309617,-0.694859374117405,
18.7314623359842));
#68742=CARTESIAN_POINT('Ctrl Pts',(-1.60901406408391,-3.75535308941463,
18.9294293952388));
#68743=CARTESIAN_POINT('Ctrl Pts',(2.2740320596552,-3.39416871652785,19.1273964544934));
#68744=CARTESIAN_POINT('Ctrl Pts',(4.0851010656413,0.0596017457147811,19.3253635137481));
#68745=CARTESIAN_POINT('Ctrl Pts',(2.17404315798984,3.45906626588641,19.5233305730027));
#68746=CARTESIAN_POINT('Ctrl Pts',(-1.7178872959552,3.70681349989336,19.7212976322574));
#68747=CARTESIAN_POINT('Ctrl Pts',(-4.04457017435047,0.577109339164211,
19.919264691512));
#68748=CARTESIAN_POINT('Ctrl Pts',(-2.68605573249723,-3.07842617038556,
20.1172317507667));
#68749=CARTESIAN_POINT('Ctrl Pts',(1.1198498932725,-3.92906341271473,20.3151988100213));
#68750=CARTESIAN_POINT('Ctrl Pts',(3.90540783118658,-1.19974695527949,20.513165869276));
#68751=CARTESIAN_POINT('Ctrl Pts',(3.13256577761639,2.62271514532222,20.7111329285306));
#68752=CARTESIAN_POINT('Ctrl Pts',(-0.494503675043983,4.0554986376479,20.9090999877852));
#68753=CARTESIAN_POINT('Ctrl Pts',(-3.671007668442,1.79312737496141,21.1070670470398));
#68754=CARTESIAN_POINT('Ctrl Pts',(-3.50268463716692,-2.10304622325587,
21.3050341062945));
#68755=CARTESIAN_POINT('Ctrl Pts',(-0.142901578712061,-4.08303590767917,
21.5030011655491));
#68756=CARTESIAN_POINT('Ctrl Pts',(3.34708580114849,-2.34278034060945,21.7009682248038));
#68757=CARTESIAN_POINT('Ctrl Pts',(3.78738654106464,1.53209212293465,21.8989352840584));
#68758=CARTESIAN_POINT('Ctrl Pts',(0.776822014656629,4.01100369510435,22.0969023433131));
#68759=CARTESIAN_POINT('Ctrl Pts',(-2.94154143309964,2.83530193841045,22.2948694025677));
#68760=CARTESIAN_POINT('Ctrl Pts',(-3.97972870900853,-0.923776210610116,
22.4928364618223));
#68761=CARTESIAN_POINT('Ctrl Pts',(-1.39179876070348,-3.84115858749677,
22.690803521077));
#68762=CARTESIAN_POINT('Ctrl Pts',(2.46426422576634,-3.25868146804872,22.8887705803316));
#68763=CARTESIAN_POINT('Ctrl Pts',(4.07502065808871,0.292932962887592,23.0867376395863));
#68764=CARTESIAN_POINT('Ctrl Pts',(1.97283490822794,3.57764245131808,23.2847046988409));
#68765=CARTESIAN_POINT('Ctrl Pts',(-1.92689312763407,3.60259433731756,23.4826717580955));
#68766=CARTESIAN_POINT('Ctrl Pts',(-4.07093858555621,0.345053788887412,
23.6806388173502));
#68767=CARTESIAN_POINT('Ctrl Pts',(-2.50576122877042,-3.22688142778547,
23.8786058766048));
#68768=CARTESIAN_POINT('Ctrl Pts',(1.34253254518328,-3.85865383906351,24.0765729358595));
#68769=CARTESIAN_POINT('Ctrl Pts',(3.96758203740061,-0.974626010884212,
24.2745399951141));
#68770=CARTESIAN_POINT('Ctrl Pts',(2.97758170681619,2.79742922409655,24.4725070543687));
#68771=CARTESIAN_POINT('Ctrl Pts',(-0.725432777006904,4.02061567059572,
24.6704741136234));
#68772=CARTESIAN_POINT('Ctrl Pts',(-3.76747148080772,1.58043086716773,24.868441172878));
#68773=CARTESIAN_POINT('Ctrl Pts',(-3.37679046244053,-2.29975852153367,
25.0664082321327));
#68774=CARTESIAN_POINT('Ctrl Pts',(0.090642504043137,-4.08453020812145,
25.2643752913873));
#68775=CARTESIAN_POINT('Ctrl Pts',(3.47548683969556,-2.14769511609513,25.4623423506419));
#68776=CARTESIAN_POINT('Ctrl Pts',(3.69365233529998,1.74600558719869,25.6603094098966));
#68777=CARTESIAN_POINT('Ctrl Pts',(0.546358189655095,4.04883882282225,25.8582764691512));
#68778=CARTESIAN_POINT('Ctrl Pts',(-3.09874849220967,2.6625853726452,26.0562435284059));
#68779=CARTESIAN_POINT('Ctrl Pts',(-3.92044028760904,-1.1496743173125,26.2542105876605));
#68780=CARTESIAN_POINT('Ctrl Pts',(-1.17003531640664,-3.91441188979357,
26.4521776469151));
#68781=CARTESIAN_POINT('Ctrl Pts',(2.64644363218947,-3.11254545127291,26.6501447061698));
#68782=CARTESIAN_POINT('Ctrl Pts',(4.05162383676031,0.525306929319951,26.8481117654244));
#68783=CARTESIAN_POINT('Ctrl Pts',(1.76517979889065,3.68452756295626,27.0460788246791));
#68784=CARTESIAN_POINT('Ctrl Pts',(-2.12960222897897,3.48660256280002,27.2440458839337));
#68785=CARTESIAN_POINT('Ctrl Pts',(-4.08400392244411,0.111870666651306,
27.4420129431883));
#68786=CARTESIAN_POINT('Ctrl Pts',(-2.31727836082527,-3.36479183353844,
27.639980002443));
#68787=CARTESIAN_POINT('Ctrl Pts',(1.56082804905753,-3.77563489838082,27.8379470616976));
#68788=CARTESIAN_POINT('Ctrl Pts',(4.01679091937884,-0.746320168956691,
28.0359141209523));
#68789=CARTESIAN_POINT('Ctrl Pts',(2.8128674497455,2.96300182159213,28.2338811802069));
#68790=CARTESIAN_POINT('Ctrl Pts',(-0.953991298834084,3.97259407520387,
28.4318482394615));
#68791=CARTESIAN_POINT('Ctrl Pts',(-3.85162389322325,1.36256980362389,28.6298152987162));
#68792=CARTESIAN_POINT('Ctrl Pts',(-3.23986156106973,-2.48895563433715,
28.8277823579708));
#68793=CARTESIAN_POINT('Ctrl Pts',(0.323890383860786,-4.07267701933735,
29.0257494172255));
#68794=CARTESIAN_POINT('Ctrl Pts',(3.59253063009277,-1.94559162118907,29.2237164764801));
#68795=CARTESIAN_POINT('Ctrl Pts',(3.58784795689867,1.95421342815309,29.4216835357347));
#68796=CARTESIAN_POINT('Ctrl Pts',(0.3141089671467,4.0734430941593,29.6196505949894));
#68797=CARTESIAN_POINT('Ctrl Pts',(-3.24582941440615,2.48116797036631,29.817617654244));
#68798=CARTESIAN_POINT('Ctrl Pts',(-3.8483405924925,-1.37181550099505,30.0155847134987));
#68799=CARTESIAN_POINT('Ctrl Pts',(-0.944448413111001,-3.97487361806236,
30.2135517727533));
#68800=CARTESIAN_POINT('Ctrl Pts',(2.81997495032113,-2.95623821167328,30.4115188320079));
#68801=CARTESIAN_POINT('Ctrl Pts',(4.0149870581406,0.755964289870477,30.6094858912626));
#68802=CARTESIAN_POINT('Ctrl Pts',(1.55175640846651,3.77937232002606,30.8074529505172));
#68803=CARTESIAN_POINT('Ctrl Pts',(-2.32535218414073,3.35921721600553,31.0054200097719));
#68804=CARTESIAN_POINT('Ctrl Pts',(-4.08372348990986,-0.121678028231323,
31.2033870690265));
#68805=CARTESIAN_POINT('Ctrl Pts',(-2.12122305581152,-3.49170672194696,
31.4013541282812));
#68806=CARTESIAN_POINT('Ctrl Pts',(1.77402305556549,-3.68027788120926,31.5993211875358));
#68807=CARTESIAN_POINT('Ctrl Pts',(4.05287367159691,-0.515575490759886,
31.7972882467904));
#68808=CARTESIAN_POINT('Ctrl Pts',(2.63896126213013,3.11889187718537,31.9952553060451));
#68809=CARTESIAN_POINT('Ctrl Pts',(-1.17943235355135,3.91159077716369,32.1932223652997));
#68810=CARTESIAN_POINT('Ctrl Pts',(-3.92318991116986,1.14025611398928,32.3911894245544));
#68811=CARTESIAN_POINT('Ctrl Pts',(-3.09234539137761,-2.67001930049665,
32.589156483809));
#68812=CARTESIAN_POINT('Ctrl Pts',(0.556079849812804,-4.04751507535492,
32.7871235430637));
#68813=CARTESIAN_POINT('Ctrl Pts',(3.69783469488094,-1.73713029273151,32.9850906023183));
#68814=CARTESIAN_POINT('Ctrl Pts',(3.47031915500144,2.15603526108631,33.183057661573));
#68815=CARTESIAN_POINT('Ctrl Pts',(0.0808332946286449,4.08473610690458,
33.3810247208275));
#68816=CARTESIAN_POINT('Ctrl Pts',(-3.38230356643229,2.29164257009446,33.5789917800823));
#68817=CARTESIAN_POINT('Ctrl Pts',(-3.76366523214165,-1.58947384536882,
33.7769588393368));
#68818=CARTESIAN_POINT('Ctrl Pts',(-0.715775227062298,-4.02234619453729,
33.9749258985915));
#68819=CARTESIAN_POINT('Ctrl Pts',(2.98429111185623,-2.79027053243799,34.1728929578461));
#68820=CARTESIAN_POINT('Ctrl Pts',(3.96523004455014,0.984151299025936,34.3708600171008));
#68821=CARTESIAN_POINT('Ctrl Pts',(1.3332621649195,3.86186678725603,34.5688270763554));
#68822=CARTESIAN_POINT('Ctrl Pts',(-2.51350331808985,3.22085456896936,34.76679413561));
#68823=CARTESIAN_POINT('Ctrl Pts',(-4.07009820508757,-0.354829102366696,
34.9647611948647));
#68824=CARTESIAN_POINT('Ctrl Pts',(-1.91823598480123,-3.60721135759169,
35.1627282541193));
#68825=CARTESIAN_POINT('Ctrl Pts',(1.98142088017778,-3.5728943986309,35.360695313374));
#68826=CARTESIAN_POINT('Ctrl Pts',(4.07571238742562,-0.283146003419342,
35.5586623726286));
#68827=CARTESIAN_POINT('Ctrl Pts',(2.45643142740698,3.26458996373172,35.7566294318833));
#68828=CARTESIAN_POINT('Ctrl Pts',(-1.4010192227053,3.8378051378937,35.9545964911379));
#68829=CARTESIAN_POINT('Ctrl Pts',(-3.98193570608205,0.914216251639095,
36.1525635503925));
#68830=CARTESIAN_POINT('Ctrl Pts',(-2.93472394014607,-2.84235778646424,
36.3505306096472));
#68831=CARTESIAN_POINT('Ctrl Pts',(0.786452018076432,-4.00912669829336,
36.5484976689018));
#68832=CARTESIAN_POINT('Ctrl Pts',(3.7910551716482,-1.52299215715173,36.7464647281564));
#68833=CARTESIAN_POINT('Ctrl Pts',(3.34144951020968,2.35081121247155,36.9444317874111));
#68834=CARTESIAN_POINT('Ctrl Pts',(-0.15270560430018,4.08268164087083,37.1423988466657));
#68835=CARTESIAN_POINT('Ctrl Pts',(-3.50772673987201,2.09462719837285,37.3403659059204));
#68836=CARTESIAN_POINT('Ctrl Pts',(-3.66668753497517,-1.80193558162018,
37.5383329651751));
#68837=CARTESIAN_POINT('Ctrl Pts',(-0.484769477671406,-4.05667927419883,
37.7363000244296));
#68838=CARTESIAN_POINT('Ctrl Pts',(3.13886751823373,-2.6151756065801,37.9342670836843));
#68839=CARTESIAN_POINT('Ctrl Pts',(3.90249175016692,1.20910475961097,38.1322341429389));
#68840=CARTESIAN_POINT('Ctrl Pts',(1.11045630484736,3.93177491897678,38.3302012021936));
#68841=CARTESIAN_POINT('Ctrl Pts',(-2.69352734667998,3.07190260655882,38.5281682614482));
#68842=CARTESIAN_POINT('Ctrl Pts',(-4.04300696435851,-0.586697896846368,
38.7261353207029));
#68843=CARTESIAN_POINT('Ctrl Pts',(-1.70929744208696,-3.71116321579617,
38.9241023799575));
#68844=CARTESIAN_POINT('Ctrl Pts',(2.18295077646978,-3.45338563041556,39.1220694392121));
#68845=CARTESIAN_POINT('Ctrl Pts',(4.08406653786445,-0.0506537900410035,
39.3200364984668));
#68846=CARTESIAN_POINT('Ctrl Pts',(2.26814537635562,3.40128858682585,39.5180035577214));
#68847=CARTESIAN_POINT('Ctrl Pts',(-1.62273122399537,3.74812194817393,39.7159706169761));
#68848=CARTESIAN_POINT('Ctrl Pts',(-3.21805115902793,1.71144863077568,39.8479486564791));
#68849=CARTESIAN_POINT('Ctrl Pts',(-3.41050039675936,0.580195909761704,
39.9139376762307));
#68850=CARTESIAN_POINT('Ctrl Pts',(-1.64343044862492,3.31080057131693,-0.136687676230652));
#68851=CARTESIAN_POINT('Ctrl Pts',(-2.74161303748949,2.76567963581706,-0.0706986564791052));
#68852=CARTESIAN_POINT('Ctrl Pts',(-4.33433259795114,0.50653088186967,0.0612793830239882));
#68853=CARTESIAN_POINT('Ctrl Pts',(-2.78179468292849,-3.3675915563884,0.259246442278628));
#68854=CARTESIAN_POINT('Ctrl Pts',(1.30897415722437,-4.16295078325229,0.457213501533269));
#68855=CARTESIAN_POINT('Ctrl Pts',(4.20522374878569,-1.17043504950046,0.655180560787908));
#68856=CARTESIAN_POINT('Ctrl Pts',(3.27086098885305,2.89120078059689,0.85314762004255));
#68857=CARTESIAN_POINT('Ctrl Pts',(-0.644239794664744,4.3171296103699,1.05111467929719));
#68858=CARTESIAN_POINT('Ctrl Pts',(-3.97208049260598,1.81025003261615,1.24908173855183));
#68859=CARTESIAN_POINT('Ctrl Pts',(-3.6809100787377,-2.3464149199974,1.44704879780647));
#68860=CARTESIAN_POINT('Ctrl Pts',(-0.0358182482239465,-4.3649518136884,
1.64501585706111));
#68861=CARTESIAN_POINT('Ctrl Pts',(3.64187171915626,-2.4064809479076,1.84298291631575));
#68862=CARTESIAN_POINT('Ctrl Pts',(4.00130141286111,1.74470191979564,2.04094997557039));
#68863=CARTESIAN_POINT('Ctrl Pts',(0.714947725952447,4.3061766697331,2.23891703482503));
#68864=CARTESIAN_POINT('Ctrl Pts',(-3.22282296004714,2.94410705447044,2.43688409407967));
#68865=CARTESIAN_POINT('Ctrl Pts',(-4.22413150189404,-1.10048417017061,
2.63485115333431));
#68866=CARTESIAN_POINT('Ctrl Pts',(-1.37663452391658,-4.14236865838933,
2.83281821258895));
#68867=CARTESIAN_POINT('Ctrl Pts',(2.72517788072432,-3.4099491719533,3.03078527184359));
#68868=CARTESIAN_POINT('Ctrl Pts',(4.34395347972042,0.429435826447155,3.22875233109823));
#68869=CARTESIAN_POINT('Ctrl Pts',(2.00474939782781,3.87754114959299,3.42671939035288));
#68870=CARTESIAN_POINT('Ctrl Pts',(-2.16107564708849,3.79263742337901,3.62468644960751));
#68871=CARTESIAN_POINT('Ctrl Pts',(-4.3578435093316,0.252083947495701,3.82265350886216));
#68872=CARTESIAN_POINT('Ctrl Pts',(-2.58397601329671,-3.51815493688139,
4.02062056811679));
#68873=CARTESIAN_POINT('Ctrl Pts',(1.54427303782037,-4.08283812273295,4.21858762737144));
#68874=CARTESIAN_POINT('Ctrl Pts',(4.26546260364518,-0.927456245588602,
4.41655468662607));
#68875=CARTESIAN_POINT('Ctrl Pts',(3.10018940675568,3.07297444409173,4.61452174588072));
#68876=CARTESIAN_POINT('Ctrl Pts',(-0.889811559104096,4.27347419590019,
4.81248880513536));
#68877=CARTESIAN_POINT('Ctrl Pts',(-4.06906353877317,1.58021144908221,5.01045586439));
#68878=CARTESIAN_POINT('Ctrl Pts',(-3.54080114607145,-2.55285595922618,
5.20842292364463));
#68879=CARTESIAN_POINT('Ctrl Pts',(0.213651010007477,-4.35989673656813,
5.40638998289928));
#68880=CARTESIAN_POINT('Ctrl Pts',(3.77343572432226,-2.19443139350223,5.60435704215391));
#68881=CARTESIAN_POINT('Ctrl Pts',(3.89506641477059,1.97048317190964,5.80232410140856));
#68882=CARTESIAN_POINT('Ctrl Pts',(0.467719662634615,4.33999822855348,6.0002911606632));
#68883=CARTESIAN_POINT('Ctrl Pts',(-3.385788380606,2.75513762781778,6.19825821991784));
#68884=CARTESIAN_POINT('Ctrl Pts',(-4.15434605104423,-1.3400579071959,6.39622527917248));
#68885=CARTESIAN_POINT('Ctrl Pts',(-1.13768445844283,-4.21426391906537,
6.59419233842712));
#68886=CARTESIAN_POINT('Ctrl Pts',(2.9155747296568,-3.24865669196893,6.79215939768177));
#68887=CARTESIAN_POINT('Ctrl Pts',(4.31231722560926,0.676953803596954,6.99012645693639));
#68888=CARTESIAN_POINT('Ctrl Pts',(1.77990552251878,3.98575998241297,7.18809351619104));
#68889=CARTESIAN_POINT('Ctrl Pts',(-2.3742614670743,3.66295356132985,7.38606057544568));
#68890=CARTESIAN_POINT('Ctrl Pts',(-4.36512763139796,0.00265858979218909,
7.58402763470032));
#68891=CARTESIAN_POINT('Ctrl Pts',(-2.37872156249766,-3.66005874742512,
7.78199469395497));
#68892=CARTESIAN_POINT('Ctrl Pts',(1.77504913350835,-3.98792513471919,7.97996175320959));
#68893=CARTESIAN_POINT('Ctrl Pts',(4.31148942649693,-0.682206150440716,
8.17792881246424));
#68894=CARTESIAN_POINT('Ctrl Pts',(2.9195297669843,3.24510280980227,8.37589587171889));
#68895=CARTESIAN_POINT('Ctrl Pts',(-1.1325502044238,4.21564661006512,8.57386293097352));
#68896=CARTESIAN_POINT('Ctrl Pts',(-4.15271063964539,1.34511733684088,8.77182999022817));
#68897=CARTESIAN_POINT('Ctrl Pts',(-3.38914191174368,-2.75101134286219,
8.9697970494828));
#68898=CARTESIAN_POINT('Ctrl Pts',(0.462432748235978,-4.34056473973755,
9.16776410873744));
#68899=CARTESIAN_POINT('Ctrl Pts',(3.89266327246501,-1.97522630442588,9.36573116799208));
#68900=CARTESIAN_POINT('Ctrl Pts',(3.77610596957432,2.1898333299681,9.56369822724672));
#68901=CARTESIAN_POINT('Ctrl Pts',(0.218961657389264,4.35963325281924,9.76166528650137));
#68902=CARTESIAN_POINT('Ctrl Pts',(-3.53768887628882,2.55716712810804,9.95963234575601));
#68903=CARTESIAN_POINT('Ctrl Pts',(-4.07098538103943,-1.57525373634129,
10.1575994050106));
#68904=CARTESIAN_POINT('Ctrl Pts',(-0.895016433525613,-4.27238714189304,
10.3555664642653));
#68905=CARTESIAN_POINT('Ctrl Pts',(3.09644390620682,-3.07674851786892,10.5535335235199));
#68906=CARTESIAN_POINT('Ctrl Pts',(4.26658917572028,0.922259785592155,10.7515005827746));
#68907=CARTESIAN_POINT('Ctrl Pts',(1.54924521419557,4.08095400277755,10.9494676420292));
#68908=CARTESIAN_POINT('Ctrl Pts',(-2.57968862354588,3.52129988953538,11.1474347012839));
#68909=CARTESIAN_POINT('Ctrl Pts',(-4.35814733222285,-0.246775479196811,
11.3454017605385));
#68910=CARTESIAN_POINT('Ctrl Pts',(-2.16569388518849,-3.79000215067897,
11.5433688197931));
#68911=CARTESIAN_POINT('Ctrl Pts',(2.00002469463763,-3.87998035141077,11.7413358790478));
#68912=CARTESIAN_POINT('Ctrl Pts',(4.34342710058424,-0.434726728421767,
11.9393029383024));
#68913=CARTESIAN_POINT('Ctrl Pts',(2.72932964331282,3.40662677800604,12.1372699975571));
#68914=CARTESIAN_POINT('Ctrl Pts',(-1.37158788482718,4.14404307177052,12.3352370568117));
#68915=CARTESIAN_POINT('Ctrl Pts',(-4.22278745042444,1.10562762946293,12.5332041160663));
#68916=CARTESIAN_POINT('Ctrl Pts',(-3.22640758842968,-2.94017693001924,
12.731171175321));
#68917=CARTESIAN_POINT('Ctrl Pts',(0.709703341729812,-4.30704858031942,
12.9291382345756));
#68918=CARTESIAN_POINT('Ctrl Pts',(3.9991703170631,-1.74956654106536,13.1271052938302));
#68919=CARTESIAN_POINT('Ctrl Pts',(3.64480590850277,2.40202751771026,13.3250723530849));
#68920=CARTESIAN_POINT('Ctrl Pts',(-0.0305118740455286,4.36502180201155,
13.5230394123395));
#68921=CARTESIAN_POINT('Ctrl Pts',(-3.67802885907486,2.35084027919942,13.7210064715942));
#68922=CARTESIAN_POINT('Ctrl Pts',(-3.97432148379599,-1.80530192763748,
13.9189735308488));
#68923=CARTESIAN_POINT('Ctrl Pts',(-0.649423660450986,-4.31654899378432,
14.1169405901034));
#68924=CARTESIAN_POINT('Ctrl Pts',(3.26719447680457,-2.89478609870085,14.3149076493581));
#68925=CARTESIAN_POINT('Ctrl Pts',(4.20691870157299,1.16455199319278,14.5128747086127));
#68926=CARTESIAN_POINT('Ctrl Pts',(1.31352225906811,4.16281222029371,14.7108417678674));
#68927=CARTESIAN_POINT('Ctrl Pts',(-2.77668583474704,3.36813926101774,14.908808827122));
#68928=CARTESIAN_POINT('Ctrl Pts',(-4.33692541366922,-0.495403131564479,
15.1067758863766));
#68929=CARTESIAN_POINT('Ctrl Pts',(-1.94558912083935,-3.90756052792091,
15.3047429456313));
#68930=CARTESIAN_POINT('Ctrl Pts',(2.21846454499872,-3.75935650997316,15.5027100048859));
#68931=CARTESIAN_POINT('Ctrl Pts',(4.36117125828737,-0.185826699863394,
15.7006770641406));
#68932=CARTESIAN_POINT('Ctrl Pts',(2.53021057519652,3.55701852000488,15.8986441233952));
#68933=CARTESIAN_POINT('Ctrl Pts',(-1.60614346971826,4.05889756721887,16.0966111826499));
#68934=CARTESIAN_POINT('Ctrl Pts',(-4.27906497288195,0.862524935493907,
16.2945782419045));
#68935=CARTESIAN_POINT('Ctrl Pts',(-3.05312996188807,-3.11973456279783,
16.4925453011591));
#68936=CARTESIAN_POINT('Ctrl Pts',(0.954654755972941,-4.25945778279257,
16.6905123604138));
#68937=CARTESIAN_POINT('Ctrl Pts',(4.0926088127702,-1.51818951785662,16.8884794196684));
#68938=CARTESIAN_POINT('Ctrl Pts',(3.50159529588251,2.60637232381472,17.0864464789231));
#68939=CARTESIAN_POINT('Ctrl Pts',(-0.279885698319549,4.35614626732967,
17.2844135381777));
#68940=CARTESIAN_POINT('Ctrl Pts',(-3.8063497238548,2.13683131908076,17.4823805974323));
#68941=CARTESIAN_POINT('Ctrl Pts',(-3.86467023905251,-2.02945072615123,
17.680347656687));
#68942=CARTESIAN_POINT('Ctrl Pts',(-0.401708690974452,-4.34660516197292,
17.8783147159416));
#68943=CARTESIAN_POINT('Ctrl Pts',(3.42726846016761,-2.70336405399536,18.0762817751962));
#68944=CARTESIAN_POINT('Ctrl Pts',(4.13350079524027,1.4030386602806,18.2742488344509));
#68945=CARTESIAN_POINT('Ctrl Pts',(1.07350695615322,4.23106713744709,18.4722158937055));
#68946=CARTESIAN_POINT('Ctrl Pts',(-2.96460935022899,3.20397217638182,18.6701829529602));
#68947=CARTESIAN_POINT('Ctrl Pts',(-4.30153122504168,-0.742411898130265,
18.8681500122148));
#68948=CARTESIAN_POINT('Ctrl Pts',(-1.71912653110853,-4.0123497201182,19.0661170714695));
#68949=CARTESIAN_POINT('Ctrl Pts',(2.42965486356431,-3.62644778680905,19.2640841307241));
#68950=CARTESIAN_POINT('Ctrl Pts',(4.36466391498096,0.0636805759787443,
19.4620511899788));
#68951=CARTESIAN_POINT('Ctrl Pts',(2.32282324692002,3.69578658340303,19.6600182492334));
#68952=CARTESIAN_POINT('Ctrl Pts',(-1.83545047483007,3.96048833617019,19.857985308488));
#68953=CARTESIAN_POINT('Ctrl Pts',(-4.32135930248387,0.616603669572335,
20.0559523677426));
#68954=CARTESIAN_POINT('Ctrl Pts',(-2.86987527135214,-3.28909748006584,
20.2539194269973));
#68955=CARTESIAN_POINT('Ctrl Pts',(1.19648653505093,-4.19794786508072,20.4518864862519));
#68956=CARTESIAN_POINT('Ctrl Pts',(4.17267341986514,-1.28185133211493,20.6498535455066));
#68957=CARTESIAN_POINT('Ctrl Pts',(3.34694211750671,2.80219998725174,20.8478206047612));
#68958=CARTESIAN_POINT('Ctrl Pts',(-0.52834490790043,4.33303565237925,21.0457876640159));
#68959=CARTESIAN_POINT('Ctrl Pts',(-3.92223214177738,1.91583958944961,21.2437547232705));
#68960=CARTESIAN_POINT('Ctrl Pts',(-3.74238996679523,-2.24696765506856,
21.4417217825251));
#68961=CARTESIAN_POINT('Ctrl Pts',(-0.152681011797728,-4.36245742846052,
21.6396888417798));
#68962=CARTESIAN_POINT('Ctrl Pts',(3.57614276412638,-2.50310791558824,21.8376559010344));
#68963=CARTESIAN_POINT('Ctrl Pts',(4.04657537286026,1.6369404565392,22.0356229602891));
#68964=CARTESIAN_POINT('Ctrl Pts',(0.829983631066443,4.28549570979318,22.2335900195437));
#68965=CARTESIAN_POINT('Ctrl Pts',(-3.14284507070233,3.02933510329512,22.4315570787983));
#68966=CARTESIAN_POINT('Ctrl Pts',(-4.25208042800194,-0.986994599932894,
22.629524138053));
#68967=CARTESIAN_POINT('Ctrl Pts',(-1.48704615385173,-4.10402729557307,
22.8274911973076));
#68968=CARTESIAN_POINT('Ctrl Pts',(2.63290551943605,-3.48168850304234,23.0254582565623));
#68969=CARTESIAN_POINT('Ctrl Pts',(4.35389365730897,0.312979755477227,23.2234253158169));
#68970=CARTESIAN_POINT('Ctrl Pts',(2.1078453619128,3.82247749983655,23.4213923750715));
#68971=CARTESIAN_POINT('Ctrl Pts',(-2.0587595672836,3.84913696178925,23.6193594343262));
#68972=CARTESIAN_POINT('Ctrl Pts',(-4.34953222918403,0.368667456908485,
23.8173264935808));
#68973=CARTESIAN_POINT('Ctrl Pts',(-2.67724235925495,-3.44771223513577,
24.0152935528355));
#68974=CARTESIAN_POINT('Ctrl Pts',(1.43440841744006,-4.12271983021779,24.2132606120901));
#68975=CARTESIAN_POINT('Ctrl Pts',(4.23910250202112,-1.04132429331712,24.4112276713448));
#68976=CARTESIAN_POINT('Ctrl Pts',(3.1813517513569,2.98887057943837,24.6091947305994));
#68977=CARTESIAN_POINT('Ctrl Pts',(-0.7750775840474,4.29576547837532,24.807161789854));
#68978=CARTESIAN_POINT('Ctrl Pts',(-4.02529743053493,1.68858725040281,25.0051288491087));
#68979=CARTESIAN_POINT('Ctrl Pts',(-3.60788025633637,-2.45714190929875,
25.2030959083633));
#68980=CARTESIAN_POINT('Ctrl Pts',(0.0968456006849734,-4.36405399097236,
25.401062967618));
#68981=CARTESIAN_POINT('Ctrl Pts',(3.713330894992,-2.29467208349948,25.5990300268726));
#68982=CARTESIAN_POINT('Ctrl Pts',(3.9464264906352,1.86549303416197,25.7969970861273));
#68983=CARTESIAN_POINT('Ctrl Pts',(0.583748072991018,4.32592007482491,25.9949641453819));
#68984=CARTESIAN_POINT('Ctrl Pts',(-3.31081055479986,2.8447987234108,26.1929312046365));
#68985=CARTESIAN_POINT('Ctrl Pts',(-4.18873461860814,-1.22835198594205,
26.3908982638912));
#68986=CARTESIAN_POINT('Ctrl Pts',(-1.2501063848151,-4.18229366892601,26.5888653231458));
#68987=CARTESIAN_POINT('Ctrl Pts',(2.82755232706474,-3.32555170523698,26.7868323824005));
#68988=CARTESIAN_POINT('Ctrl Pts',(4.32889568048136,0.561256175025024,26.984799441655));
#68989=CARTESIAN_POINT('Ctrl Pts',(1.88597942813973,3.93667726682387,27.1827665009098));
#68990=CARTESIAN_POINT('Ctrl Pts',(-2.27534101426903,3.72520731977148,27.3807335601643));
#68991=CARTESIAN_POINT('Ctrl Pts',(-4.36349168906895,0.119526507185921,
27.578700619419));
#68992=CARTESIAN_POINT('Ctrl Pts',(-2.47586071432294,-3.59506050432623,
27.7766676786736));
#68993=CARTESIAN_POINT('Ctrl Pts',(1.66764291843593,-4.03401950950716,27.9746347379283));
#68994=CARTESIAN_POINT('Ctrl Pts',(4.2916789812846,-0.797394399336888,28.1726017971829));
#68995=CARTESIAN_POINT('Ctrl Pts',(3.0053653161213,3.16577409540686,28.3705688564375));
#68996=CARTESIAN_POINT('Ctrl Pts',(-1.01927745001176,4.24445753735287,28.5685359156922));
#68997=CARTESIAN_POINT('Ctrl Pts',(-4.11520879182729,1.45581692055054,28.7665029749468));
#68998=CARTESIAN_POINT('Ctrl Pts',(-3.4615806605301,-2.65928667825375,28.9644700342015));
#68999=CARTESIAN_POINT('Ctrl Pts',(0.346055739657655,-4.35138963223751,
29.1624370934562));
#69000=CARTESIAN_POINT('Ctrl Pts',(3.83838454732779,-2.07873768747504,29.3604041527107));
#69001=CARTESIAN_POINT('Ctrl Pts',(3.83338141658813,2.08794952559938,29.5583712119654));
#69002=CARTESIAN_POINT('Ctrl Pts',(0.335604934185799,4.35220813319449,29.75633827122));
#69003=CARTESIAN_POINT('Ctrl Pts',(-3.4679569223873,2.65096606748557,29.9543053304747));
#69004=CARTESIAN_POINT('Ctrl Pts',(-4.11170079924854,-1.46569534486288,
30.1522723897293));
#69005=CARTESIAN_POINT('Ctrl Pts',(-1.00908149933844,-4.24689308014541,
30.350239448984));
#69006=CARTESIAN_POINT('Ctrl Pts',(3.01295921668583,-3.1585476195685,30.5482065082386));
#69007=CARTESIAN_POINT('Ctrl Pts',(4.28975167326265,0.80769851320537,30.7461735674933));
#69008=CARTESIAN_POINT('Ctrl Pts',(1.65795046243508,4.03801270064934,30.9441406267478));
#69009=CARTESIAN_POINT('Ctrl Pts',(-2.48448706767751,3.58910438926444,31.1421076860026));
#69010=CARTESIAN_POINT('Ctrl Pts',(-4.36319206520576,-0.130005033053983,
31.3400747452571));
#69011=CARTESIAN_POINT('Ctrl Pts',(-2.26638841452324,-3.73066078074767,
31.5380418045118));
#69012=CARTESIAN_POINT('Ctrl Pts',(1.89542787082935,-3.93213675919053,31.7360088637665));
#69013=CARTESIAN_POINT('Ctrl Pts',(4.3302310474462,-0.550858767949419,31.9339759230211));
#69014=CARTESIAN_POINT('Ctrl Pts',(2.81955790291901,3.33233244718791,32.1319429822757));
#69015=CARTESIAN_POINT('Ctrl Pts',(-1.26014650579978,4.17927949417292,32.3299100415304));
#69016=CARTESIAN_POINT('Ctrl Pts',(-4.19167241195597,1.21828925027683,32.527877100785));
#69017=CARTESIAN_POINT('Ctrl Pts',(-3.30396925939567,-2.8527413902185,32.7258441600396));
#69018=CARTESIAN_POINT('Ctrl Pts',(0.594135032481799,-4.32450573703732,
32.9238112192943));
#69019=CARTESIAN_POINT('Ctrl Pts',(3.95089506892724,-1.85601036118186,33.1217782785489));
#69020=CARTESIAN_POINT('Ctrl Pts',(3.70780956111402,2.30358298418572,33.3197453378036));
#69021=CARTESIAN_POINT('Ctrl Pts',(0.0863651005263536,4.3642739803862,33.5177123970582));
#69022=CARTESIAN_POINT('Ctrl Pts',(-3.61377064819352,2.44847054479303,33.7156794563129));
#69023=CARTESIAN_POINT('Ctrl Pts',(-4.02123070221231,-1.69824908251039,
33.9136465155675));
#69024=CARTESIAN_POINT('Ctrl Pts',(-0.764759122135802,-4.2976144302814,
34.1116135748221));
#69025=CARTESIAN_POINT('Ctrl Pts',(3.18852031281941,-2.98122198454221,34.3095806340768));
#69026=CARTESIAN_POINT('Ctrl Pts',(4.23658955113988,1.05150144212309,34.5075476933314));
#69027=CARTESIAN_POINT('Ctrl Pts',(1.42450362106763,4.12615265570029,34.705514752586));
#69028=CARTESIAN_POINT('Ctrl Pts',(-2.68551427648209,3.44127292977391,34.9034818118407));
#69029=CARTESIAN_POINT('Ctrl Pts',(-4.34863433749239,-0.37911174147221,
35.1014488710953));
#69030=CARTESIAN_POINT('Ctrl Pts',(-2.04950997508928,-3.85406994666813,
35.29941593035));
#69031=CARTESIAN_POINT('Ctrl Pts',(2.1170189126629,-3.81740451537487,35.4973829896046));
#69032=CARTESIAN_POINT('Ctrl Pts',(4.3546327249666,-0.302523027934251,35.6953500488593));
#69033=CARTESIAN_POINT('Ctrl Pts',(2.62453668551897,3.48800134512025,35.8933171081139));
#69034=CARTESIAN_POINT('Ctrl Pts',(-1.49689761581866,4.10044435350182,36.0912841673685));
#69035=CARTESIAN_POINT('Ctrl Pts',(-4.25443846035722,0.976780407608266,
36.2892512266232));
#69036=CARTESIAN_POINT('Ctrl Pts',(-3.1355610243575,-3.03687381651065,36.4872182858778));
#69037=CARTESIAN_POINT('Ctrl Pts',(0.840272661313841,-4.28349026118421,
36.6851853451324));
#69038=CARTESIAN_POINT('Ctrl Pts',(4.05049506524201,-1.62721773691917,36.8831524043871));
#69039=CARTESIAN_POINT('Ctrl Pts',(3.5701207550549,2.51168837811768,37.0811194636417));
#69040=CARTESIAN_POINT('Ctrl Pts',(-0.163155973376139,4.36207891749352,
37.2790865228964));
#69041=CARTESIAN_POINT('Ctrl Pts',(-3.7477771245128,2.23797247636521,37.477053582151));
#69042=CARTESIAN_POINT('Ctrl Pts',(-3.91761636107874,-1.92525058348425,
37.6750206414057));
#69043=CARTESIAN_POINT('Ctrl Pts',(-0.51794455321368,-4.3342970854914,37.8729877006603));
#69044=CARTESIAN_POINT('Ctrl Pts',(3.35367511613573,-2.79414448209901,38.0709547599149));
#69045=CARTESIAN_POINT('Ctrl Pts',(4.16955777758475,1.29184953539883,38.2689218191696));
#69046=CARTESIAN_POINT('Ctrl Pts',(1.18645009879805,4.20084493258216,38.4668888784242));
#69047=CARTESIAN_POINT('Ctrl Pts',(-2.87785820354561,3.28212747781266,38.6648559376789));
#69048=CARTESIAN_POINT('Ctrl Pts',(-4.31968911461486,-0.626848417753602,
38.8628229969335));
#69049=CARTESIAN_POINT('Ctrl Pts',(-1.82627277650346,-3.96513572377127,
39.0607900561882));
#69050=CARTESIAN_POINT('Ctrl Pts',(2.33234045599844,-3.68971719509276,39.2587571154427));
#69051=CARTESIAN_POINT('Ctrl Pts',(4.36355858955962,-0.0541202692408854,
39.4567241746975));
#69052=CARTESIAN_POINT('Ctrl Pts',(2.42336532659467,3.63405490361473,39.654691233952));
#69053=CARTESIAN_POINT('Ctrl Pts',(-1.73378242135946,4.00462371757127,39.8526582932068));
#69054=CARTESIAN_POINT('Ctrl Pts',(-3.43827766918834,1.82857118124135,39.9846363327098));
#69055=CARTESIAN_POINT('Ctrl Pts',(-3.64389712141114,0.619901468841313,
40.0506253524613));
#69056=CARTESIAN_POINT('Ctrl Pts',(-1.74869447533093,3.52286199445097,-8.32667268468867E-15));
#69057=CARTESIAN_POINT('Ctrl Pts',(-2.91721720025602,2.94282529798265,0.0659890197515384));
#69058=CARTESIAN_POINT('Ctrl Pts',(-4.61195268386658,0.53897489574385,0.197967059254632));
#69059=CARTESIAN_POINT('Ctrl Pts',(-2.95997253647821,-3.5832905218196,0.395934118509272));
#69060=CARTESIAN_POINT('Ctrl Pts',(1.39281578907369,-4.42959362341053,0.593901177763913));
#69061=CARTESIAN_POINT('Ctrl Pts',(4.47457423171435,-1.24540305706733,0.791868237018553));
#69062=CARTESIAN_POINT('Ctrl Pts',(3.48036422567708,3.07638624824828,0.989835296273193));
#69063=CARTESIAN_POINT('Ctrl Pts',(-0.685504257671056,4.59364782078722,
1.18780235552783));
#69064=CARTESIAN_POINT('Ctrl Pts',(-4.22649782277157,1.92619908779956,1.38576941478248));
#69065=CARTESIAN_POINT('Ctrl Pts',(-3.91667753525201,-2.49670608869799,
1.58373647403711));
#69066=CARTESIAN_POINT('Ctrl Pts',(-0.0381124572917341,-4.64453310334433,
1.78170353329176));
#69067=CARTESIAN_POINT('Ctrl Pts',(3.87513871395109,-2.56061942999538,1.9796705925464));
#69068=CARTESIAN_POINT('Ctrl Pts',(4.25759038397908,1.85645252635955,2.17763765180103));
#69069=CARTESIAN_POINT('Ctrl Pts',(0.76074113119263,4.58199332893075,2.37560471105568));
#69070=CARTESIAN_POINT('Ctrl Pts',(-3.42924929370728,3.13268124321463,2.57357177031031));
#69071=CARTESIAN_POINT('Ctrl Pts',(-4.49469305294534,-1.17097172574399,
2.77153882956496));
#69072=CARTESIAN_POINT('Ctrl Pts',(-1.46480989721034,-4.40769318456417,
2.9695058888196));
#69073=CARTESIAN_POINT('Ctrl Pts',(2.89972934863413,-3.62836120210814,3.16747294807423));
#69074=CARTESIAN_POINT('Ctrl Pts',(4.6221897966156,0.456941793822625,3.36544000732888));
#69075=CARTESIAN_POINT('Ctrl Pts',(2.13315641032305,4.12590310215742,3.56340706658351));
#69076=CARTESIAN_POINT('Ctrl Pts',(-2.29949557524497,4.03556117312128,3.76137412583816));
#69077=CARTESIAN_POINT('Ctrl Pts',(-4.63696950211734,0.268230278119817,
3.9593411850928));
#69078=CARTESIAN_POINT('Ctrl Pts',(-2.74948330342801,-3.74349769814126,
4.15730824434744));
#69079=CARTESIAN_POINT('Ctrl Pts',(1.64318589320195,-4.34434963455086,4.35527530360208));
#69080=CARTESIAN_POINT('Ctrl Pts',(4.53867146976977,-0.986861119756444,
4.55324236285672));
#69081=CARTESIAN_POINT('Ctrl Pts',(3.29876088921743,3.26980277000011,4.75120942211136));
#69082=CARTESIAN_POINT('Ctrl Pts',(-0.946805238270306,4.54719621575256,
4.949176481366));
#69083=CARTESIAN_POINT('Ctrl Pts',(-4.32969276915656,1.68142621014276,5.14714354062063));
#69084=CARTESIAN_POINT('Ctrl Pts',(-3.76759442881268,-2.71636996621894,
5.34511059987529));
#69085=CARTESIAN_POINT('Ctrl Pts',(0.227335657046906,-4.63915424143996,
5.54307765912991));
#69086=CARTESIAN_POINT('Ctrl Pts',(4.01512957829139,-2.33498780402952,5.74104471838457));
#69087=CARTESIAN_POINT('Ctrl Pts',(4.14455088516541,2.09669538454401,5.9390117776392));
#69088=CARTESIAN_POINT('Ctrl Pts',(0.4976777634472,4.61798120606043,6.13697883689384));
#69089=CARTESIAN_POINT('Ctrl Pts',(-3.60265287816667,2.93160805957583,6.33494589614848));
#69090=CARTESIAN_POINT('Ctrl Pts',(-4.42043774602824,-1.42589049685537,
6.53291295540313));
#69091=CARTESIAN_POINT('Ctrl Pts',(-1.21055474468865,-4.48419343758787,
6.73088001465776));
#69092=CARTESIAN_POINT('Ctrl Pts',(3.10232138295309,-3.45673771241492,6.92884707391241));
#69093=CARTESIAN_POINT('Ctrl Pts',(4.58852719602873,0.720313644787832,7.12681413316704));
#69094=CARTESIAN_POINT('Ctrl Pts',(1.89391096924347,4.24105350309916,7.32478119242169));
#69095=CARTESIAN_POINT('Ctrl Pts',(-2.52633624619639,3.89757087770312,7.52274825167632));
#69096=CARTESIAN_POINT('Ctrl Pts',(-4.64472018242493,0.00282887619951857,
7.72071531093096));
#69097=CARTESIAN_POINT('Ctrl Pts',(-2.53108201699104,-3.89449064690514,
7.91868237018561));
#69098=CARTESIAN_POINT('Ctrl Pts',(1.88874352170134,-4.24335733644923,8.11664942944024));
#69099=CARTESIAN_POINT('Ctrl Pts',(4.58764637522149,-0.725902411818228,
8.31461648869489));
#69100=CARTESIAN_POINT('Ctrl Pts',(3.10652974597202,3.45295619910787,8.51258354794951));
#69101=CARTESIAN_POINT('Ctrl Pts',(-1.20509163449415,4.48566469188666,8.71055060720418));
#69102=CARTESIAN_POINT('Ctrl Pts',(-4.41869758423413,1.43127399006965,8.9085176664588));
#69103=CARTESIAN_POINT('Ctrl Pts',(-3.60622120768015,-2.92721748027788,
9.10648472571345));
#69104=CARTESIAN_POINT('Ctrl Pts',(0.492052214761531,-4.61858400308089,
9.30445178496808));
#69105=CARTESIAN_POINT('Ctrl Pts',(4.14199381822252,-2.10174232135456,9.50241884422273));
#69106=CARTESIAN_POINT('Ctrl Pts',(4.01797085649934,2.33009522807297,9.70038590347737));
#69107=CARTESIAN_POINT('Ctrl Pts',(0.232986458846607,4.63887388118718,9.89835296273201));
#69108=CARTESIAN_POINT('Ctrl Pts',(-3.76428281378263,2.72095727151808,10.0963200219866));
#69109=CARTESIAN_POINT('Ctrl Pts',(-4.33173770811715,-1.67615094894297,
10.2942870812413));
#69110=CARTESIAN_POINT('Ctrl Pts',(-0.952343492203188,-4.54603953441066,
10.4922541404959));
#69111=CARTESIAN_POINT('Ctrl Pts',(3.29477548410189,-3.27381857849937,10.6902211997506));
#69112=CARTESIAN_POINT('Ctrl Pts',(4.53987020036735,0.981331819204367,10.8881882590052));
#69113=CARTESIAN_POINT('Ctrl Pts',(1.64847654445207,4.34234483406809,11.0861553182599));
#69114=CARTESIAN_POINT('Ctrl Pts',(-2.7449213003466,3.74684408942645,11.2841223775145));
#69115=CARTESIAN_POINT('Ctrl Pts',(-4.63729278529116,-0.262581794976337,
11.4820894367692));
#69116=CARTESIAN_POINT('Ctrl Pts',(-2.30440961797664,-4.03275710750639,
11.6800564960238));
#69117=CARTESIAN_POINT('Ctrl Pts',(2.12812908326276,-4.12849853827486,11.8780235552784));
#69118=CARTESIAN_POINT('Ctrl Pts',(4.62162970215701,-0.462571585494106,
12.0759906145331));
#69119=CARTESIAN_POINT('Ctrl Pts',(2.90414703744313,3.62482600416581,12.2739576737877));
#69120=CARTESIAN_POINT('Ctrl Pts',(-1.45944001380466,4.40947484647234,12.4719247330423));
#69121=CARTESIAN_POINT('Ctrl Pts',(-4.49326291309284,1.17644463082245,12.669891792297));
#69122=CARTESIAN_POINT('Ctrl Pts',(-3.43306352256849,-3.12849938877669,
12.8678588515516));
#69123=CARTESIAN_POINT('Ctrl Pts',(0.755160836800423,-4.58292108661379,
13.0658259108062));
#69124=CARTESIAN_POINT('Ctrl Pts',(4.25532278850436,-1.86162873344873,13.2637929700609));
#69125=CARTESIAN_POINT('Ctrl Pts',(3.87826084224315,2.55588075134383,13.4617600293155));
#69126=CARTESIAN_POINT('Ctrl Pts',(-0.0324662024000749,4.6446075745178,
13.6597270885702));
#69127=CARTESIAN_POINT('Ctrl Pts',(-3.91361176942619,2.50141489836758,13.8576941478248));
#69128=CARTESIAN_POINT('Ctrl Pts',(-4.22888235259237,-1.9209340497527,14.0556612070795));
#69129=CARTESIAN_POINT('Ctrl Pts',(-0.691020157336088,-4.59303001489449,
14.2536282663341));
#69130=CARTESIAN_POINT('Ctrl Pts',(3.4764628683862,-3.08020121100853,14.4515953255888));
#69131=CARTESIAN_POINT('Ctrl Pts',(4.47637774860644,1.23914318274667,14.6495623848434));
#69132=CARTESIAN_POINT('Ctrl Pts',(1.39765520322344,4.42944618530002,14.847529444098));
#69133=CARTESIAN_POINT('Ctrl Pts',(-2.95453645940081,3.58387330769906,15.0454965033527));
#69134=CARTESIAN_POINT('Ctrl Pts',(-4.61471157307029,-0.527134397414488,
15.2434635626073));
#69135=CARTESIAN_POINT('Ctrl Pts',(-2.07020683456502,-4.15784526379792,
15.4414306218619));
#69136=CARTESIAN_POINT('Ctrl Pts',(2.36056031260876,-4.00014857050371,15.6393976811166));
#69137=CARTESIAN_POINT('Ctrl Pts',(4.64051039806405,-0.197729160787965,
15.8373647403712));
#69138=CARTESIAN_POINT('Ctrl Pts',(2.69227411356042,3.78485054830688,16.0353317996259));
#69139=CARTESIAN_POINT('Ctrl Pts',(-1.70901921309492,4.31887565285675,16.2332988588805));
#69140=CARTESIAN_POINT('Ctrl Pts',(-4.5531450898464,0.917770868122375,16.4312659181351));
#69141=CARTESIAN_POINT('Ctrl Pts',(-3.2486872208605,-3.3195579399348,16.6292329773898));
#69142=CARTESIAN_POINT('Ctrl Pts',(1.01580173290275,-4.53228203171407,16.8272000366444));
#69143=CARTESIAN_POINT('Ctrl Pts',(4.35474615099769,-1.61543168717751,17.0251670958991));
#69144=CARTESIAN_POINT('Ctrl Pts',(3.72587738889572,2.77331412906689,17.2231341551537));
#69145=CARTESIAN_POINT('Ctrl Pts',(-0.297812770102405,4.63516354938317,
17.4211012144083));
#69146=CARTESIAN_POINT('Ctrl Pts',(-4.05015176568713,2.27369836400256,17.619068273663));
#69147=CARTESIAN_POINT('Ctrl Pts',(-4.11220779173309,-2.15943989339276,
17.8170353329176));
#69148=CARTESIAN_POINT('Ctrl Pts',(-0.427438696409145,-4.62501132283787,
18.0150023921723));
#69149=CARTESIAN_POINT('Ctrl Pts',(3.64678981503939,-2.87651831568849,18.2129694514269));
#69150=CARTESIAN_POINT('Ctrl Pts',(4.39825732233478,1.49290525556546,18.4109365106816));
#69151=CARTESIAN_POINT('Ctrl Pts',(1.14226658330751,4.5020729256894,18.6089035699362));
#69152=CARTESIAN_POINT('Ctrl Pts',(-3.15449673979053,3.409191090892,18.8068706291908));
#69153=CARTESIAN_POINT('Ctrl Pts',(-4.57705033698718,-0.789964422143125,
19.0048376884455));
#69154=CARTESIAN_POINT('Ctrl Pts',(-1.82923899813315,-4.26934635082178,
19.2028047477001));
#69155=CARTESIAN_POINT('Ctrl Pts',(2.58527766747342,-3.85872685709026,19.4007718069548));
#69156=CARTESIAN_POINT('Ctrl Pts',(4.64422676432063,0.0677594062427062,
19.5987388662094));
#69157=CARTESIAN_POINT('Ctrl Pts',(2.47160333585018,3.93250690091964,19.796705925464));
#69158=CARTESIAN_POINT('Ctrl Pts',(-1.95301365370493,4.214163172447,19.9946729847187));
#69159=CARTESIAN_POINT('Ctrl Pts',(-4.59814843061727,0.656097999980467,
20.1926400439733));
#69160=CARTESIAN_POINT('Ctrl Pts',(-3.05369481020705,-3.49976878974612,
20.390607103228));
#69161=CARTESIAN_POINT('Ctrl Pts',(1.27312317682936,-4.46683231744671,20.5885741624826));
#69162=CARTESIAN_POINT('Ctrl Pts',(4.4399390085437,-1.36395570895038,20.7865412217372));
#69163=CARTESIAN_POINT('Ctrl Pts',(3.56131845739703,2.98168482918127,20.9845082809919));
#69164=CARTESIAN_POINT('Ctrl Pts',(-0.562186140756878,4.6105726671106,21.1824753402465));
#69165=CARTESIAN_POINT('Ctrl Pts',(-4.17345661511275,2.03855180393781,21.3804423995011));
#69166=CARTESIAN_POINT('Ctrl Pts',(-3.98209529642355,-2.39088908688126,
21.5784094587558));
#69167=CARTESIAN_POINT('Ctrl Pts',(-0.162460444883393,-4.64187894924185,
21.7763765180104));
#69168=CARTESIAN_POINT('Ctrl Pts',(3.80519972710427,-2.66343549056703,21.9743435772651));
#69169=CARTESIAN_POINT('Ctrl Pts',(4.30576420465589,1.74178879014377,22.1723106365197));
#69170=CARTESIAN_POINT('Ctrl Pts',(0.883145247476255,4.55998772448201,22.3702776957744));
#69171=CARTESIAN_POINT('Ctrl Pts',(-3.34414870830501,3.22336826817979,22.568244755029));
#69172=CARTESIAN_POINT('Ctrl Pts',(-4.52443214699536,-1.05021298925567,
22.7662118142837));
#69173=CARTESIAN_POINT('Ctrl Pts',(-1.58229354699997,-4.36689600364936,
22.9641788735382));
#69174=CARTESIAN_POINT('Ctrl Pts',(2.80154681310576,-3.70469553803595,23.1621459327929));
#69175=CARTESIAN_POINT('Ctrl Pts',(4.63276665652923,0.333026548066865,23.3601129920475));
#69176=CARTESIAN_POINT('Ctrl Pts',(2.24285581559766,4.06731254835503,23.5580800513022));
#69177=CARTESIAN_POINT('Ctrl Pts',(-2.19062600693313,4.09567958626095,23.7560471105568));
#69178=CARTESIAN_POINT('Ctrl Pts',(-4.62812587281185,0.392281124929548,
23.9540141698115));
#69179=CARTESIAN_POINT('Ctrl Pts',(-2.84872348973948,-3.66854304248606,
24.1519812290661));
#69180=CARTESIAN_POINT('Ctrl Pts',(1.52628428969684,-4.38678582137206,24.3499482883208));
#69181=CARTESIAN_POINT('Ctrl Pts',(4.51062296664163,-1.10802257575002,24.5479153475754));
#69182=CARTESIAN_POINT('Ctrl Pts',(3.38512179589761,3.18031193478019,24.74588240683));
#69183=CARTESIAN_POINT('Ctrl Pts',(-0.824722391087892,4.57091528615491,
24.9438494660847));
#69184=CARTESIAN_POINT('Ctrl Pts',(-4.28312338026216,1.7967436336379,25.1418165253393));
#69185=CARTESIAN_POINT('Ctrl Pts',(-3.83897005023221,-2.61452529706382,
25.3397835845939));
#69186=CARTESIAN_POINT('Ctrl Pts',(0.103048697326808,-4.64357777382328,
25.5377506438486));
#69187=CARTESIAN_POINT('Ctrl Pts',(3.95117495028843,-2.44164905090382,25.7357177031032));
#69188=CARTESIAN_POINT('Ctrl Pts',(4.19920064597042,1.98498048112526,25.9336847623579));
#69189=CARTESIAN_POINT('Ctrl Pts',(0.621137956326939,4.60300132682757,26.1316518216125));
#69190=CARTESIAN_POINT('Ctrl Pts',(-3.52287261739005,3.0270120741764,26.3296188808671));
#69191=CARTESIAN_POINT('Ctrl Pts',(-4.45702894960724,-1.30702965457161,
26.5275859401218));
#69192=CARTESIAN_POINT('Ctrl Pts',(-1.33017745322355,-4.45017544805846,
26.7255529993764));
#69193=CARTESIAN_POINT('Ctrl Pts',(3.00866102194002,-3.53855795920106,26.9235200586311));
#69194=CARTESIAN_POINT('Ctrl Pts',(4.60616752420241,0.597205420730102,27.1214871178857));
#69195=CARTESIAN_POINT('Ctrl Pts',(2.0067790573888,4.18882697069147,27.3194541771403));
#69196=CARTESIAN_POINT('Ctrl Pts',(-2.42107979955908,3.96381207674295,27.517421236395));
#69197=CARTESIAN_POINT('Ctrl Pts',(-4.64297945569379,0.127182347720528,
27.7153882956496));
#69198=CARTESIAN_POINT('Ctrl Pts',(-2.63444306782062,-3.82532917511402,
27.9133553549043));
#69199=CARTESIAN_POINT('Ctrl Pts',(1.77445778781432,-4.2924041206335,28.1113224141589));
#69200=CARTESIAN_POINT('Ctrl Pts',(4.56656704319037,-0.848468629717082,
28.3092894734136));
#69201=CARTESIAN_POINT('Ctrl Pts',(3.19786318249711,3.3685463692216,28.5072565326682));
#69202=CARTESIAN_POINT('Ctrl Pts',(-1.08456360118944,4.51632099950187,28.7052235919229));
#69203=CARTESIAN_POINT('Ctrl Pts',(-4.37879369043133,1.5490640374772,28.9031906511775));
#69204=CARTESIAN_POINT('Ctrl Pts',(-3.68329975999046,-2.82961772217035,
29.1011577104321));
#69205=CARTESIAN_POINT('Ctrl Pts',(0.368221095454519,-4.63010224513767,
29.2991247696868));
#69206=CARTESIAN_POINT('Ctrl Pts',(4.08423846456282,-2.21188375376102,29.4970918289414));
#69207=CARTESIAN_POINT('Ctrl Pts',(4.07891487627758,2.22168562304567,29.695058888196));
#69208=CARTESIAN_POINT('Ctrl Pts',(0.357100901224898,4.63097317222967,29.8930259474507));
#69209=CARTESIAN_POINT('Ctrl Pts',(-3.69008443036845,2.82076416460482,30.0909930067053));
#69210=CARTESIAN_POINT('Ctrl Pts',(-4.37506100600459,-1.55957518873072,
30.28896006596));
#69211=CARTESIAN_POINT('Ctrl Pts',(-1.07371458556588,-4.51891254222846,
30.4869271252146));
#69212=CARTESIAN_POINT('Ctrl Pts',(3.20594348305053,-3.36085702746372,30.6848941844692));
#69213=CARTESIAN_POINT('Ctrl Pts',(4.5645162883847,0.859432736540255,30.8828612437239));
#69214=CARTESIAN_POINT('Ctrl Pts',(1.76414451640364,4.29665308127263,31.0808283029785));
#69215=CARTESIAN_POINT('Ctrl Pts',(-2.64362195121429,3.81899156252335,31.2787953622332));
#69216=CARTESIAN_POINT('Ctrl Pts',(-4.64266064050165,-0.138332037876641,
31.4767624214878));
#69217=CARTESIAN_POINT('Ctrl Pts',(-2.41155377323495,-3.96961483954837,
31.6747294807425));
#69218=CARTESIAN_POINT('Ctrl Pts',(2.0168326860932,-4.1839956371718,31.8726965399971));
#69219=CARTESIAN_POINT('Ctrl Pts',(4.60758842329548,-0.586142045138947,
32.0706635992517));
#69220=CARTESIAN_POINT('Ctrl Pts',(3.00015454370789,3.54577301719043,32.2686306585064));
#69221=CARTESIAN_POINT('Ctrl Pts',(-1.34086065804823,4.44696821118217,32.466597717761));
#69222=CARTESIAN_POINT('Ctrl Pts',(-4.46015491274207,1.29632238656436,32.6645647770157));
#69223=CARTESIAN_POINT('Ctrl Pts',(-3.51559312741374,-3.03546347994035,
32.8625318362703));
#69224=CARTESIAN_POINT('Ctrl Pts',(0.632190215150794,-4.60149639871972,
33.0604988955249));
#69225=CARTESIAN_POINT('Ctrl Pts',(4.20395544297353,-1.97489042963221,33.2584659547796));
#69226=CARTESIAN_POINT('Ctrl Pts',(3.9452999672266,2.45113070728511,33.4564330140342));
#69227=CARTESIAN_POINT('Ctrl Pts',(0.0918969064240613,4.64381185386782,
33.6544000732888));
#69228=CARTESIAN_POINT('Ctrl Pts',(-3.84523772995475,2.6052985194916,33.8523671325435));
#69229=CARTESIAN_POINT('Ctrl Pts',(-4.27879617228297,-1.80702431965196,
34.0503341917981));
#69230=CARTESIAN_POINT('Ctrl Pts',(-0.813743017209305,-4.5728826660255,
34.2483012510528));
#69231=CARTESIAN_POINT('Ctrl Pts',(3.39274951378259,-3.17217343664643,34.4462683103074));
#69232=CARTESIAN_POINT('Ctrl Pts',(4.50794905772962,1.11885158522024,34.6442353695621));
#69233=CARTESIAN_POINT('Ctrl Pts',(1.51574507721577,4.39043852414456,34.8422024288167));
#69234=CARTESIAN_POINT('Ctrl Pts',(-2.85752523487432,3.66169129057847,35.0401694880713));
#69235=CARTESIAN_POINT('Ctrl Pts',(-4.62717046989721,-0.403394380577725,
35.238136547326));
#69236=CARTESIAN_POINT('Ctrl Pts',(-2.18078396537732,-4.10092853574456,
35.4361036065806));
#69237=CARTESIAN_POINT('Ctrl Pts',(2.25261694514802,-4.06191463211884,35.6340706658352));
#69238=CARTESIAN_POINT('Ctrl Pts',(4.63355306250759,-0.321900052449153,
35.8320377250899));
#69239=CARTESIAN_POINT('Ctrl Pts',(2.79264194363096,3.71141272650878,36.0300047843445));
#69240=CARTESIAN_POINT('Ctrl Pts',(-1.59277600893202,4.36308356910993,36.2279718435992));
#69241=CARTESIAN_POINT('Ctrl Pts',(-4.5269412146324,1.03934456357744,36.4259389028538));
#69242=CARTESIAN_POINT('Ctrl Pts',(-3.33639810856892,-3.23138984655706,
36.6239059621085));
#69243=CARTESIAN_POINT('Ctrl Pts',(0.894093304551245,-4.55785382407507,
36.8218730213631));
#69244=CARTESIAN_POINT('Ctrl Pts',(4.30993495883582,-1.73144331668662,37.0198400806178));
#69245=CARTESIAN_POINT('Ctrl Pts',(3.79879199990011,2.67256554376382,37.2178071398723));
#69246=CARTESIAN_POINT('Ctrl Pts',(-0.173606342452101,4.6414761941162,37.415774199127));
#69247=CARTESIAN_POINT('Ctrl Pts',(-3.98782750915358,2.38131775435758,37.6137412583816));
#69248=CARTESIAN_POINT('Ctrl Pts',(-4.16854518718231,-2.04856558534832,
37.8117083176363));
#69249=CARTESIAN_POINT('Ctrl Pts',(-0.55111962875595,-4.61191489678395,
38.0096753768909));
#69250=CARTESIAN_POINT('Ctrl Pts',(3.56848271403773,-2.97311335761792,38.2076424361456));
#69251=CARTESIAN_POINT('Ctrl Pts',(4.43662380500257,1.37459431118669,38.4056094954002));
#69252=CARTESIAN_POINT('Ctrl Pts',(1.26244389274874,4.46991494618754,38.6035765546549));
#69253=CARTESIAN_POINT('Ctrl Pts',(-3.06218906041124,3.4923523490665,38.8015436139095));
#69254=CARTESIAN_POINT('Ctrl Pts',(-4.59637126487122,-0.666998938660841,
38.9995106731641));
#69255=CARTESIAN_POINT('Ctrl Pts',(-1.94324811091996,-4.21910823174637,
39.1974777324188));
#69256=CARTESIAN_POINT('Ctrl Pts',(2.4817301355271,-3.92604875976996,39.3954447916734));
#69257=CARTESIAN_POINT('Ctrl Pts',(4.64305064125478,-0.0575867484407697,
39.5934118509281));
#69258=CARTESIAN_POINT('Ctrl Pts',(2.57858527683373,3.86682122040361,39.7913789101827));
#69259=CARTESIAN_POINT('Ctrl Pts',(-1.84483361872357,4.26112548696861,39.9893459694374));
#69260=CARTESIAN_POINT('Ctrl Pts',(-3.65850417934875,1.94569373170701,40.1213240089404));
#69261=CARTESIAN_POINT('Ctrl Pts',(-3.87729384606291,0.659607027920921,
40.187313028692));
#69262=CARTESIAN_POINT('Ctrl Pts',(-3.936306081373,-0.00286452337122285,
38.970836477965));
#69263=CARTESIAN_POINT('Ctrl Pts',(-3.93786941330146,-0.191350950945783,
38.9803945430314));
#69264=CARTESIAN_POINT('Ctrl Pts',(-3.92549888185612,-0.379633084980762,
38.9899526080978));
#69265=CARTESIAN_POINT('Ctrl Pts',(-3.89848703846934,-0.56579193955387,
38.9995106731641));
#69266=CARTESIAN_POINT('Ctrl Pts',(-3.83491032379214,-1.00394672271177,
39.0220071154428));
#69267=CARTESIAN_POINT('Ctrl Pts',(-3.69022485851434,-1.43033913477847,
39.0445035577214));
#69268=CARTESIAN_POINT('Ctrl Pts',(-3.48038110743657,-1.82358747408649,
39.0670000000001));
#69269=CARTESIAN_POINT('Ctrl Pts',(-1.87556985610737,-2.62720998907027,
-1.05818132034585E-16));
#69270=CARTESIAN_POINT('Ctrl Pts',(-1.9427166798522,-2.5898538427666,-1.35022482623698E-16));
#69271=CARTESIAN_POINT('Ctrl Pts',(-2.00831539040545,-2.5500067025529,-6.43752826549732E-16));
#69272=CARTESIAN_POINT('Ctrl Pts',(-2.07220966857289,-2.50769818664921,
-4.83987849797529E-16));
#69273=CARTESIAN_POINT('Ctrl Pts',(-2.15789934851274,-2.4509575317659,-2.74928550691976E-16));
#69274=CARTESIAN_POINT('Ctrl Pts',(-2.24052477232639,-2.38979204336152,
1.62088651626145E-16));
#69275=CARTESIAN_POINT('Ctrl Pts',(-2.31999371269407,-2.32459267939733,
2.08166817117217E-16));
#69276=CARTESIAN_POINT('Ctrl Pts',(-2.36987291826283,-2.2836698677545,2.37088082181609E-16));
#69277=CARTESIAN_POINT('Ctrl Pts',(-2.41850829062763,-2.24115685284336,
3.30045642536614E-16));
#69278=CARTESIAN_POINT('Ctrl Pts',(-2.46587282390372,-2.19714092437569,
2.84494650060196E-16));
#69279=CARTESIAN_POINT('Ctrl Pts',(-2.4883641183387,-2.17623973231232,2.62864524885711E-16));
#69280=CARTESIAN_POINT('Ctrl Pts',(-2.510568802024,-2.15499955403746,8.37311985777155E-16));
#69281=CARTESIAN_POINT('Ctrl Pts',(-2.5324836784513,-2.13342923122307,7.84095011141517E-16));
#69282=CARTESIAN_POINT('Ctrl Pts',(-2.54647144194973,-2.11966138840117,
7.50127835566776E-16));
#69283=CARTESIAN_POINT('Ctrl Pts',(-2.56034150716028,-2.10575853776106,
3.74260074904971E-16));
#69284=CARTESIAN_POINT('Ctrl Pts',(-2.57408203118947,-2.09173447001254,
3.95516952522712E-16));
#69285=CARTESIAN_POINT('Ctrl Pts',(-2.64826407279405,-2.0160216387569,5.10278120035181E-16));
#69286=CARTESIAN_POINT('Ctrl Pts',(-2.7187510730238,-1.93670300009748,2.04203257333887E-16));
#69287=CARTESIAN_POINT('Ctrl Pts',(-2.78544558437692,-1.85418677655769,
2.77555756156289E-16));
#69288=CARTESIAN_POINT('Ctrl Pts',(-2.84956847381101,-1.77485223206203,
3.48079912886359E-16));
#69289=CARTESIAN_POINT('Ctrl Pts',(-2.91018592724737,-1.69256114185943,
6.22909331617954E-16));
#69290=CARTESIAN_POINT('Ctrl Pts',(-2.96718958630348,-1.6076387700055,6.66133814775094E-16));
#69291=CARTESIAN_POINT('Ctrl Pts',(-2.99212868714053,-1.57048523231941,
6.85044526156343E-16));
#69292=CARTESIAN_POINT('Ctrl Pts',(-3.01637577769413,-1.53282762334849,
4.45074375543263E-16));
#69293=CARTESIAN_POINT('Ctrl Pts',(-3.03992022985205,-1.49469135800012,
5.68989300120393E-16));
#69294=CARTESIAN_POINT('Ctrl Pts',(-3.05141389032931,-1.47607443360345,
6.2948066605246E-16));
#69295=CARTESIAN_POINT('Ctrl Pts',(-3.06274009074011,-1.4573434260494,6.80345639867992E-16));
#69296=CARTESIAN_POINT('Ctrl Pts',(-3.07389750346823,-1.43850120933943,
7.21644966006352E-16));
#69297=CARTESIAN_POINT('Ctrl Pts',(-3.08183764567037,-1.42509219743621,
7.51035518312842E-16));
#69298=CARTESIAN_POINT('Ctrl Pts',(-3.08969120442884,-1.41162864596677,
2.83354860342952E-16));
#69299=CARTESIAN_POINT('Ctrl Pts',(-3.09745337754263,-1.39811946780493,
3.05311331771918E-16));
#69300=CARTESIAN_POINT('Ctrl Pts',(-3.15286735703586,-1.30167774837181,
4.62058088082708E-16));
#69301=CARTESIAN_POINT('Ctrl Pts',(-3.20369221394891,-1.20280340881569,
3.53144865346304E-16));
#69302=CARTESIAN_POINT('Ctrl Pts',(-3.24982252344817,-1.10192599424532,
2.91433543964104E-16));
#69303=CARTESIAN_POINT('Ctrl Pts',(-3.29668794246923,-0.999441047690232,
2.28738821853768E-16));
#69304=CARTESIAN_POINT('Ctrl Pts',(-3.33870858667038,-0.89488801034169,
4.07726271026068E-16));
#69305=CARTESIAN_POINT('Ctrl Pts',(-3.37574011869655,-0.788675562609922,
4.44089209850063E-16));
#69306=CARTESIAN_POINT('Ctrl Pts',(-3.41269905543875,-0.682671329941954,
4.8038086407617E-16));
#69307=CARTESIAN_POINT('Ctrl Pts',(-3.44468892653223,-0.575013374954663,
3.12016465250824E-16));
#69308=CARTESIAN_POINT('Ctrl Pts',(-3.47152479256147,-0.466078071083872,
3.60822483003176E-16));
#69309=CARTESIAN_POINT('Ctrl Pts',(-3.4892663919142,-0.394059284191032,
3.93088883946656E-16));
#69310=CARTESIAN_POINT('Ctrl Pts',(-3.50475445309811,-0.321481607985789,
4.80650587058393E-16));
#69311=CARTESIAN_POINT('Ctrl Pts',(-3.51792389739043,-0.248449242265856,
5.55111512312578E-16));
#69312=CARTESIAN_POINT('Ctrl Pts',(-3.5218708993275,-0.226560779657458,
5.77428127174312E-16));
#69313=CARTESIAN_POINT('Ctrl Pts',(-3.52560956225353,-0.204631457077295,
4.94393150946916E-16));
#69314=CARTESIAN_POINT('Ctrl Pts',(-3.52913795503785,-0.182664042150726,
4.9960036108132E-16));
#69315=CARTESIAN_POINT('Ctrl Pts',(-3.5316576994674,-0.166976369384047,
5.03319005668721E-16));
#69316=CARTESIAN_POINT('Ctrl Pts',(-3.53407007612331,-0.151269688065101,
5.28418406579064E-16));
#69317=CARTESIAN_POINT('Ctrl Pts',(-3.53637257048778,-0.13555860296056,
5.27355936696949E-16));
#69318=CARTESIAN_POINT('Ctrl Pts',(-3.55317264707207,-0.020923172337153,
5.19603659139405E-16));
#69319=CARTESIAN_POINT('Ctrl Pts',(-3.56415658297867,0.094128556090517,
-4.9767199959817E-17));
#69320=CARTESIAN_POINT('Ctrl Pts',(-3.56918101522632,0.209171118706935,
2.77555756156289E-17));
#69321=CARTESIAN_POINT('Ctrl Pts',(-3.57215568325829,0.277280989924882,
7.3652208486252E-17));
#69322=CARTESIAN_POINT('Ctrl Pts',(-3.57304069866554,0.345388280413459,
7.34761168187773E-16));
#69323=CARTESIAN_POINT('Ctrl Pts',(-3.57179877131075,0.41340886664328,6.38378239159465E-16));
#69324=CARTESIAN_POINT('Ctrl Pts',(-3.56977179011697,0.524426993867594,
4.8231769589789E-16));
#69325=CARTESIAN_POINT('Ctrl Pts',(-3.56208205365773,0.635213960545909,
-1.88046607578939E-16));
#69326=CARTESIAN_POINT('Ctrl Pts',(-3.54899330987584,0.745485199930978,
-1.94289029309402E-16));
#69327=CARTESIAN_POINT('Ctrl Pts',(-3.53565885377793,0.857826538790079,
-2.00648638749126E-16));
#69328=CARTESIAN_POINT('Ctrl Pts',(-3.51672067583019,0.969633285182107,
-2.00357306609628E-17));
#69329=CARTESIAN_POINT('Ctrl Pts',(-3.49240358880244,1.08060745715161,-1.94289029309402E-16));
#69330=CARTESIAN_POINT('Ctrl Pts',(-3.48412425558681,1.11839126517991,-2.53617727758628E-16));
#69331=CARTESIAN_POINT('Ctrl Pts',(-3.4752209384603,1.15607853650087,5.93380374341007E-16));
#69332=CARTESIAN_POINT('Ctrl Pts',(-3.46570115451279,1.19365736151579,6.66133814775094E-16));
#69333=CARTESIAN_POINT('Ctrl Pts',(-3.46167353792751,1.20955615708932,6.96914236362872E-16));
#69334=CARTESIAN_POINT('Ctrl Pts',(-3.45753549723059,1.22543555138734,-2.22777472105693E-16));
#69335=CARTESIAN_POINT('Ctrl Pts',(-3.4532915411,1.24128055545267,-2.22044604925031E-16));
#69336=CARTESIAN_POINT('Ctrl Pts',(-3.42380202789225,1.35138100001027,-2.16952211003276E-16));
#69337=CARTESIAN_POINT('Ctrl Pts',(-3.38916062108469,1.45999026507038,-2.84426430466537E-16));
#69338=CARTESIAN_POINT('Ctrl Pts',(-3.34966883438784,1.56681514734322,-2.22044604925031E-16));
#69339=CARTESIAN_POINT('Ctrl Pts',(-3.30890722121856,1.67707489733847,-1.57656942218446E-16));
#69340=CARTESIAN_POINT('Ctrl Pts',(-3.26297826095999,1.78543436725715,5.85977744875059E-16));
#69341=CARTESIAN_POINT('Ctrl Pts',(-3.21215817004056,1.89157452147116,6.66133814775094E-16));
#69342=CARTESIAN_POINT('Ctrl Pts',(-3.16086111688722,1.99871083378222,7.47042174123448E-16));
#69343=CARTESIAN_POINT('Ctrl Pts',(-3.10458042918179,2.10358677819699,2.69205069416314E-16));
#69344=CARTESIAN_POINT('Ctrl Pts',(-3.04354725425783,2.20586614535285,3.88578058618805E-16));
#69345=CARTESIAN_POINT('Ctrl Pts',(-3.00375166655634,2.27255557336927,4.66413076490916E-16));
#69346=CARTESIAN_POINT('Ctrl Pts',(-2.96193450734188,2.33814088750178,-9.37256318242688E-17));
#69347=CARTESIAN_POINT('Ctrl Pts',(-2.91814875486367,2.40252454053732,-1.11022302462516E-16));
#69348=CARTESIAN_POINT('Ctrl Pts',(-2.90371986817841,2.42374113226987,-1.16722140572999E-16));
#69349=CARTESIAN_POINT('Ctrl Pts',(-2.88907713976851,2.44482719670223,-2.28029434941039E-16));
#69350=CARTESIAN_POINT('Ctrl Pts',(-2.8742222712953,2.46577912801777,-2.22044604925031E-16));
#69351=CARTESIAN_POINT('Ctrl Pts',(-2.86397378277113,2.48023402730104,-2.17915624459887E-16));
#69352=CARTESIAN_POINT('Ctrl Pts',(-2.85362431940418,2.49462508162952,1.10039211875577E-16));
#69353=CARTESIAN_POINT('Ctrl Pts',(-2.84317441430392,2.50895108865281,1.11022302462516E-16));
#69354=CARTESIAN_POINT('Ctrl Pts',(-2.83348355348938,2.52223650500433,1.11933984813188E-16));
#69355=CARTESIAN_POINT('Ctrl Pts',(-2.82371242472869,2.53545759866695,6.11899018834777E-16));
#69356=CARTESIAN_POINT('Ctrl Pts',(-2.81386191454734,2.54861341598892,6.10622663543836E-16));
#69357=CARTESIAN_POINT('Ctrl Pts',(-2.74041062887734,2.64671104530441,6.0110539638047E-16));
#69358=CARTESIAN_POINT('Ctrl Pts',(-2.66254789228831,2.74118288830179,-5.41748258519085E-16));
#69359=CARTESIAN_POINT('Ctrl Pts',(-2.58056320353906,2.83169462033826,-4.9960036108132E-16));
#69360=CARTESIAN_POINT('Ctrl Pts',(-2.49844011931886,2.9223591420477,-4.57381315259579E-16));
#69361=CARTESIAN_POINT('Ctrl Pts',(-2.41218077165145,3.00905100116057,5.07174156750596E-17));
#69362=CARTESIAN_POINT('Ctrl Pts',(-2.32202629791708,3.09141791323186,-5.55111512312578E-17));
#69363=CARTESIAN_POINT('Ctrl Pts',(-2.23357416200924,3.17222953576213,-1.5973386196413E-16));
#69364=CARTESIAN_POINT('Ctrl Pts',(-2.14137210639717,3.24887870479941,2.73547190358871E-16));
#69365=CARTESIAN_POINT('Ctrl Pts',(-2.04560675719255,3.32100584191314,2.77555756156289E-16));
#69366=CARTESIAN_POINT('Ctrl Pts',(-1.95012832424157,3.39291688366318,2.8155231215381E-16));
#69367=CARTESIAN_POINT('Ctrl Pts',(-1.85110753907348,3.46033371771341,1.62536897696253E-16));
#69368=CARTESIAN_POINT('Ctrl Pts',(-1.74869447533108,3.5228619944509,1.66533453693773E-16));
#69369=CARTESIAN_POINT('Origin',(0.,0.,0.));
#69370=CARTESIAN_POINT('Origin',(-1.73205080756888,-3.,-8.));
#69371=CARTESIAN_POINT('',(-1.73205080756888,-3.,-8.));
#69372=CARTESIAN_POINT('',(1.73205080756888,-3.,-8.));
#69373=CARTESIAN_POINT('',(-0.86602540378444,-3.,-8.));
#69374=CARTESIAN_POINT('',(-1.73205080756888,-3.,-4.));
#69375=CARTESIAN_POINT('',(-1.73205080756888,-3.,-8.));
#69376=CARTESIAN_POINT('',(1.73205080756888,-3.,-4.));
#69377=CARTESIAN_POINT('',(-1.73205080756888,-3.,-4.));
#69378=CARTESIAN_POINT('',(1.73205080756888,-3.,-8.));
#69379=CARTESIAN_POINT('Origin',(-3.46410161513775,4.24230095489963E-16,
-8.));
#69380=CARTESIAN_POINT('',(-3.46410161513775,4.24230095489963E-16,-8.));
#69381=CARTESIAN_POINT('',(-3.03108891324554,-0.749999999999999,-8.));
#69382=CARTESIAN_POINT('',(-3.46410161513775,5.55111512312578E-16,-4.));
#69383=CARTESIAN_POINT('',(-3.46410161513775,4.24230095489963E-16,-8.));
#69384=CARTESIAN_POINT('',(-3.46410161513775,4.24230095489963E-16,-4.));
#69385=CARTESIAN_POINT('Origin',(-1.73205080756888,3.,-8.));
#69386=CARTESIAN_POINT('',(-1.73205080756888,3.,-8.));
#69387=CARTESIAN_POINT('',(-2.1650635094611,2.25,-8.));
#69388=CARTESIAN_POINT('',(-1.73205080756888,3.,-4.));
#69389=CARTESIAN_POINT('',(-1.73205080756888,3.,-8.));
#69390=CARTESIAN_POINT('',(-1.73205080756888,3.,-4.));
#69391=CARTESIAN_POINT('Origin',(1.73205080756888,3.,-8.));
#69392=CARTESIAN_POINT('',(1.73205080756888,3.,-8.));
#69393=CARTESIAN_POINT('',(0.866025403784439,3.,-8.));
#69394=CARTESIAN_POINT('',(1.73205080756888,3.,-4.));
#69395=CARTESIAN_POINT('',(1.73205080756888,3.,-8.));
#69396=CARTESIAN_POINT('',(1.73205080756888,3.,-4.));
#69397=CARTESIAN_POINT('Origin',(3.46410161513775,0.,-8.));
#69398=CARTESIAN_POINT('',(3.46410161513775,0.,-8.));
#69399=CARTESIAN_POINT('',(3.03108891324554,0.75,-8.));
#69400=CARTESIAN_POINT('',(3.46410161513775,0.,-4.));
#69401=CARTESIAN_POINT('',(3.46410161513775,0.,-8.));
#69402=CARTESIAN_POINT('',(3.46410161513775,0.,-4.));
#69403=CARTESIAN_POINT('Origin',(1.73205080756888,-3.,-8.));
#69404=CARTESIAN_POINT('',(2.1650635094611,-2.25,-8.));
#69405=CARTESIAN_POINT('',(1.73205080756888,-3.,-4.));
#69406=CARTESIAN_POINT('Origin',(0.,5.55111512312578E-16,-4.));
#69407=CARTESIAN_POINT('Origin',(0.,0.,0.));
#69408=CARTESIAN_POINT('',(-6.5,-7.9602041944578E-16,0.));
#69409=CARTESIAN_POINT('Origin',(0.,0.,0.));
#69410=CARTESIAN_POINT('Origin',(0.,0.,-8.));
#69411=CARTESIAN_POINT('',(-6.5,-7.9602041944578E-16,-8.));
#69412=CARTESIAN_POINT('',(-6.5,-7.9602041944578E-16,-8.));
#69413=CARTESIAN_POINT('Origin',(0.,0.,-8.));
#69414=CARTESIAN_POINT('Origin',(0.,0.,-8.));
#69415=CARTESIAN_POINT('Origin',(0.,0.,40.));
#69477=UNCERTAINTY_MEASURE_WITH_UNIT(LENGTH_MEASURE(0.01),#69492,
'DISTANCE_ACCURACY_VALUE',
'Maximum model space distance between geometric entities at asserted c
onnectivities');
#69478=UNCERTAINTY_MEASURE_WITH_UNIT(LENGTH_MEASURE(0.01),#69492,
'DISTANCE_ACCURACY_VALUE',
'Maximum model space distance between geometric entities at asserted c
onnectivities');
#69490=(
GEOMETRIC_REPRESENTATION_CONTEXT(3)
GLOBAL_UNCERTAINTY_ASSIGNED_CONTEXT((#69477))
GLOBAL_UNIT_ASSIGNED_CONTEXT((#69492,#69494,#69495))
REPRESENTATION_CONTEXT('','3D')
);
#69491=(
GEOMETRIC_REPRESENTATION_CONTEXT(3)
GLOBAL_UNCERTAINTY_ASSIGNED_CONTEXT((#69478))
GLOBAL_UNIT_ASSIGNED_CONTEXT((#69492,#69494,#69495))
REPRESENTATION_CONTEXT('','3D')
);
#69492=(
LENGTH_UNIT()
NAMED_UNIT(*)
SI_UNIT(.MILLI.,.METRE.)
);
#69494=(
NAMED_UNIT(*)
PLANE_ANGLE_UNIT()
SI_UNIT($,.RADIAN.)
);
#69495=(
NAMED_UNIT(*)
SI_UNIT($,.STERADIAN.)
SOLID_ANGLE_UNIT()
);
#69507=SHAPE_DEFINITION_REPRESENTATION(#69519,#69581);
#69519=PRODUCT_DEFINITION_SHAPE('',$,#69594);
#69581=SHAPE_REPRESENTATION('',(#15724),#69490);
#69582=PRODUCT_DEFINITION_CONTEXT('part definition',#69620,'design');
#69594=PRODUCT_DEFINITION('Socket head cap screw M8x40',
'Socket head cap screw M8x40',#69606,#69582);
#69606=PRODUCT_DEFINITION_FORMATION('',$,#69633);
#69620=APPLICATION_CONTEXT(
'Core Data for Automotive Mechanical Design Process');
#69621=PRODUCT_CONTEXT('part definition',#69620,'mechanical');
#69633=PRODUCT('Socket head cap screw M8x40',
'Socket head cap screw M8x40',$,(#69621));
#69640=PRESENTATION_STYLE_ASSIGNMENT((#69650));
#69650=SURFACE_STYLE_USAGE(.BOTH.,#69660);
#69660=SURFACE_SIDE_STYLE('',(#69670));
#69670=SURFACE_STYLE_FILL_AREA(#69680);
#69680=FILL_AREA_STYLE('Dark gray',(#69690));
#69690=FILL_AREA_STYLE_COLOUR('Dark gray',#69700);
#69700=COLOUR_RGB('Dark gray',0.250980392156863,0.282352941176471,0.32156862745098);
ENDSEC;
END-ISO-10303-21;
